ISO-10303-21;
HEADER;
/* Generated by software containing ST-Developer
 * from STEP Tools, Inc. (www.steptools.com) 
 */

FILE_DESCRIPTION(
/* description */ (''),
/* implementation_level */ '2;1');

FILE_NAME(
/* name */ 'Screw_02.step',
/* time_stamp */ '2026-10-05T21:25:27-07:00',
/* author */ (''),
/* organization */ (''),
/* preprocessor_version */ 'ST-DEVELOPER v20.2',
/* originating_system */ 'Autodesk Translation Framework v15.15.0.0',
/* authorisation */ '');

FILE_SCHEMA (('AUTOMOTIVE_DESIGN { 1 0 10303 214 3 1 1 }'));
ENDSEC;

DATA;
#10=MECHANICAL_DESIGN_GEOMETRIC_PRESENTATION_REPRESENTATION('',(#35),#12118);
#25=B_SPLINE_SURFACE_WITH_KNOTS('',3,3,((#11379,#11380,#11381,#11382,#11383,
#11384,#11385,#11386,#11387,#11388,#11389,#11390,#11391,#11392,#11393,#11394,
#11395,#11396,#11397,#11398,#11399,#11400,#11401,#11402,#11403,#11404,#11405,
#11406,#11407,#11408,#11409,#11410,#11411,#11412,#11413,#11414,#11415,#11416,
#11417,#11418,#11419,#11420),(#11421,#11422,#11423,#11424,#11425,#11426,
#11427,#11428,#11429,#11430,#11431,#11432,#11433,#11434,#11435,#11436,#11437,
#11438,#11439,#11440,#11441,#11442,#11443,#11444,#11445,#11446,#11447,#11448,
#11449,#11450,#11451,#11452,#11453,#11454,#11455,#11456,#11457,#11458,#11459,
#11460,#11461,#11462),(#11463,#11464,#11465,#11466,#11467,#11468,#11469,
#11470,#11471,#11472,#11473,#11474,#11475,#11476,#11477,#11478,#11479,#11480,
#11481,#11482,#11483,#11484,#11485,#11486,#11487,#11488,#11489,#11490,#11491,
#11492,#11493,#11494,#11495,#11496,#11497,#11498,#11499,#11500,#11501,#11502,
#11503,#11504),(#11505,#11506,#11507,#11508,#11509,#11510,#11511,#11512,
#11513,#11514,#11515,#11516,#11517,#11518,#11519,#11520,#11521,#11522,#11523,
#11524,#11525,#11526,#11527,#11528,#11529,#11530,#11531,#11532,#11533,#11534,
#11535,#11536,#11537,#11538,#11539,#11540,#11541,#11542,#11543,#11544,#11545,
#11546)),.UNSPECIFIED.,.F.,.F.,.F.,(4,4),(4,1,1,1,1,1,1,1,1,1,1,1,1,1,1,
1,1,1,1,1,1,1,1,1,1,1,1,1,1,1,1,1,1,1,1,1,1,1,1,4),(-0.000255169100126093,
0.0463066876673497),(8.31044341387851,9.3071677964662,10.3037486701926,
11.300329543919,12.2969104176454,13.2934912913718,14.2900721650982,15.2866530388247,
16.2832339125511,17.2798147862775,18.2763956600039,19.2729765337303,20.2695574074567,
21.2661382811831,22.2627191549095,23.2593000286359,24.2558809023623,25.2524617760888,
26.2490426498152,27.2456235235416,28.242204397268,29.2387852709944,30.2353661447208,
31.2319470184472,32.2285278921736,33.2251087659,34.2216896396264,35.2182705133528,
36.2148513870793,37.2114322608057,38.2080131345321,39.2045940082585,40.2011748819849,
41.1977557557113,42.1943366294377,43.1909175031641,44.1874983768905,45.1840792506169,
46.1806601243433,47.1772409980698),.UNSPECIFIED.);
#26=B_SPLINE_SURFACE_WITH_KNOTS('',3,3,((#11723,#11724,#11725,#11726,#11727,
#11728,#11729,#11730,#11731,#11732,#11733,#11734,#11735,#11736,#11737,#11738,
#11739,#11740,#11741,#11742,#11743,#11744,#11745,#11746,#11747,#11748,#11749,
#11750,#11751,#11752,#11753,#11754,#11755,#11756,#11757,#11758,#11759,#11760,
#11761,#11762,#11763,#11764),(#11765,#11766,#11767,#11768,#11769,#11770,
#11771,#11772,#11773,#11774,#11775,#11776,#11777,#11778,#11779,#11780,#11781,
#11782,#11783,#11784,#11785,#11786,#11787,#11788,#11789,#11790,#11791,#11792,
#11793,#11794,#11795,#11796,#11797,#11798,#11799,#11800,#11801,#11802,#11803,
#11804,#11805,#11806),(#11807,#11808,#11809,#11810,#11811,#11812,#11813,
#11814,#11815,#11816,#11817,#11818,#11819,#11820,#11821,#11822,#11823,#11824,
#11825,#11826,#11827,#11828,#11829,#11830,#11831,#11832,#11833,#11834,#11835,
#11836,#11837,#11838,#11839,#11840,#11841,#11842,#11843,#11844,#11845,#11846,
#11847,#11848),(#11849,#11850,#11851,#11852,#11853,#11854,#11855,#11856,
#11857,#11858,#11859,#11860,#11861,#11862,#11863,#11864,#11865,#11866,#11867,
#11868,#11869,#11870,#11871,#11872,#11873,#11874,#11875,#11876,#11877,#11878,
#11879,#11880,#11881,#11882,#11883,#11884,#11885,#11886,#11887,#11888,#11889,
#11890)),.UNSPECIFIED.,.F.,.F.,.F.,(4,4),(4,1,1,1,1,1,1,1,1,1,1,1,1,1,1,
1,1,1,1,1,1,1,1,1,1,1,1,1,1,1,1,1,1,1,1,1,1,1,1,4),(-0.000278939256451637,
0.046334532407048),(11.6151018031581,12.6120023928371,13.6085832665635,
14.6051641402899,15.6017450140163,16.5983258877427,17.5949067614691,18.5914876351955,
19.5880685089219,20.5846493826483,21.5812302563748,22.5778111301012,23.5743920038276,
24.570972877554,25.5675537512804,26.5641346250068,27.5607154987332,28.5572963724596,
29.553877246186,30.5504581199124,31.5470389936388,32.5436198673653,33.5402007410917,
34.5367816148181,35.5333624885445,36.5299433622709,37.5265242359973,38.5231051097237,
39.5196859834501,40.5162668571765,41.5128477309029,42.5094286046293,43.5060094783558,
44.5025903520822,45.4991712258086,46.495752099535,47.4923329732614,48.4889138469878,
49.4854947207142,50.4820755944406),.UNSPECIFIED.);
#29=SHAPE_REPRESENTATION_RELATIONSHIP('SRR','None',#12137,#32);
#32=ADVANCED_BREP_SHAPE_REPRESENTATION('',(#38),#12117);
#35=STYLED_ITEM('',(#12159),#38);
#38=MANIFOLD_SOLID_BREP('Body1',#2408);
#57=FACE_BOUND('',#509,.T.);
#88=PLANE('',#2714);
#89=PLANE('',#2715);
#90=PLANE('',#2716);
#91=PLANE('',#2717);
#92=PLANE('',#2718);
#93=PLANE('',#2719);
#94=PLANE('',#2720);
#95=PLANE('',#2721);
#96=PLANE('',#2722);
#241=CIRCLE('',#2697,1.5555);
#242=CIRCLE('',#2704,1.954);
#243=CIRCLE('',#2711,1.954);
#244=CIRCLE('',#2713,1.5555);
#352=FACE_OUTER_BOUND('',#492,.T.);
#353=FACE_OUTER_BOUND('',#493,.T.);
#354=FACE_OUTER_BOUND('',#494,.T.);
#355=FACE_OUTER_BOUND('',#495,.T.);
#356=FACE_OUTER_BOUND('',#496,.T.);
#357=FACE_OUTER_BOUND('',#497,.T.);
#358=FACE_OUTER_BOUND('',#498,.T.);
#359=FACE_OUTER_BOUND('',#499,.T.);
#360=FACE_OUTER_BOUND('',#500,.T.);
#361=FACE_OUTER_BOUND('',#501,.T.);
#362=FACE_OUTER_BOUND('',#502,.T.);
#363=FACE_OUTER_BOUND('',#503,.T.);
#364=FACE_OUTER_BOUND('',#504,.T.);
#365=FACE_OUTER_BOUND('',#505,.T.);
#366=FACE_OUTER_BOUND('',#506,.T.);
#367=FACE_OUTER_BOUND('',#507,.T.);
#368=FACE_OUTER_BOUND('',#508,.T.);
#369=FACE_OUTER_BOUND('',#510,.T.);
#370=FACE_OUTER_BOUND('',#511,.T.);
#371=FACE_OUTER_BOUND('',#512,.T.);
#372=FACE_OUTER_BOUND('',#513,.T.);
#373=FACE_OUTER_BOUND('',#514,.T.);
#374=FACE_OUTER_BOUND('',#515,.T.);
#375=FACE_OUTER_BOUND('',#516,.T.);
#376=FACE_OUTER_BOUND('',#517,.T.);
#492=EDGE_LOOP('',(#2063,#2064,#2065,#2066));
#493=EDGE_LOOP('',(#2067,#2068,#2069,#2070));
#494=EDGE_LOOP('',(#2071,#2072,#2073,#2074));
#495=EDGE_LOOP('',(#2075,#2076,#2077,#2078));
#496=EDGE_LOOP('',(#2079,#2080,#2081,#2082));
#497=EDGE_LOOP('',(#2083,#2084,#2085,#2086));
#498=EDGE_LOOP('',(#2087,#2088,#2089,#2090));
#499=EDGE_LOOP('',(#2091,#2092,#2093,#2094));
#500=EDGE_LOOP('',(#2095,#2096,#2097,#2098));
#501=EDGE_LOOP('',(#2099,#2100,#2101,#2102));
#502=EDGE_LOOP('',(#2103,#2104,#2105,#2106));
#503=EDGE_LOOP('',(#2107,#2108,#2109,#2110));
#504=EDGE_LOOP('',(#2111,#2112,#2113,#2114));
#505=EDGE_LOOP('',(#2115,#2116,#2117,#2118));
#506=EDGE_LOOP('',(#2119,#2120,#2121,#2122,#2123,#2124,#2125,#2126,#2127,
#2128,#2129,#2130,#2131,#2132,#2133,#2134));
#507=EDGE_LOOP('',(#2135,#2136,#2137,#2138,#2139,#2140,#2141,#2142,#2143,
#2144,#2145,#2146,#2147,#2148,#2149,#2150));
#508=EDGE_LOOP('',(#2151,#2152,#2153,#2154));
#509=EDGE_LOOP('',(#2155,#2156,#2157,#2158,#2159,#2160));
#510=EDGE_LOOP('',(#2161,#2162,#2163,#2164));
#511=EDGE_LOOP('',(#2165,#2166,#2167,#2168));
#512=EDGE_LOOP('',(#2169,#2170,#2171,#2172));
#513=EDGE_LOOP('',(#2173,#2174,#2175,#2176));
#514=EDGE_LOOP('',(#2177,#2178,#2179,#2180));
#515=EDGE_LOOP('',(#2181,#2182,#2183,#2184));
#516=EDGE_LOOP('',(#2185,#2186,#2187,#2188,#2189,#2190));
#517=EDGE_LOOP('',(#2191,#2192,#2193,#2194));
#626=LINE('',#8079,#764);
#627=LINE('',#8346,#765);
#628=LINE('',#8370,#766);
#629=LINE('',#8684,#767);
#630=LINE('',#9000,#768);
#631=LINE('',#9348,#769);
#632=LINE('',#9534,#770);
#633=LINE('',#9636,#771);
#634=LINE('',#10020,#772);
#635=LINE('',#10404,#773);
#636=LINE('',#10609,#774);
#637=LINE('',#10813,#775);
#638=LINE('',#12070,#776);
#639=LINE('',#12072,#777);
#640=LINE('',#12074,#778);
#641=LINE('',#12076,#779);
#642=LINE('',#12078,#780);
#643=LINE('',#12079,#781);
#644=LINE('',#12082,#782);
#645=LINE('',#12084,#783);
#646=LINE('',#12085,#784);
#647=LINE('',#12088,#785);
#648=LINE('',#12089,#786);
#649=LINE('',#12092,#787);
#650=LINE('',#12093,#788);
#651=LINE('',#12096,#789);
#652=LINE('',#12097,#790);
#653=LINE('',#12100,#791);
#654=LINE('',#12101,#792);
#655=LINE('',#12103,#793);
#764=VECTOR('',#3342,1.5555);
#765=VECTOR('',#3347,1.5555);
#766=VECTOR('',#3350,1.5555);
#767=VECTOR('',#3353,1.5555);
#768=VECTOR('',#3356,1.5555);
#769=VECTOR('',#3359,1.5555);
#770=VECTOR('',#3362,1.954);
#771=VECTOR('',#3367,1.954);
#772=VECTOR('',#3370,1.954);
#773=VECTOR('',#3373,1.954);
#774=VECTOR('',#3376,1.954);
#775=VECTOR('',#3379,1.954);
#776=VECTOR('',#3390,10.);
#777=VECTOR('',#3391,10.);
#778=VECTOR('',#3392,10.);
#779=VECTOR('',#3393,9.99999999999999);
#780=VECTOR('',#3394,10.);
#781=VECTOR('',#3395,10.);
#782=VECTOR('',#3398,10.);
#783=VECTOR('',#3399,10.);
#784=VECTOR('',#3400,10.);
#785=VECTOR('',#3403,10.);
#786=VECTOR('',#3404,10.);
#787=VECTOR('',#3407,10.);
#788=VECTOR('',#3408,10.);
#789=VECTOR('',#3411,10.);
#790=VECTOR('',#3412,9.99999999999999);
#791=VECTOR('',#3415,10.);
#792=VECTOR('',#3416,10.);
#793=VECTOR('',#3419,10.);
#838=B_SPLINE_CURVE_WITH_KNOTS('',3,(#8081,#8082,#8083,#8084,#8085,#8086,
#8087,#8088,#8089,#8090,#8091,#8092,#8093,#8094,#8095,#8096,#8097,#8098,
#8099,#8100,#8101,#8102,#8103,#8104,#8105,#8106,#8107,#8108,#8109,#8110,
#8111,#8112,#8113,#8114,#8115,#8116,#8117,#8118,#8119,#8120,#8121,#8122,
#8123,#8124,#8125,#8126,#8127,#8128,#8129,#8130,#8131,#8132,#8133,#8134,
#8135,#8136,#8137,#8138,#8139,#8140,#8141,#8142,#8143,#8144,#8145,#8146,
#8147,#8148,#8149,#8150,#8151,#8152,#8153,#8154,#8155,#8156,#8157,#8158,
#8159,#8160,#8161,#8162,#8163,#8164,#8165,#8166,#8167,#8168,#8169,#8170,
#8171,#8172,#8173,#8174,#8175,#8176,#8177,#8178,#8179,#8180,#8181,#8182,
#8183,#8184,#8185,#8186,#8187,#8188,#8189,#8190,#8191,#8192,#8193,#8194,
#8195,#8196,#8197,#8198,#8199,#8200,#8201,#8202,#8203,#8204,#8205,#8206,
#8207,#8208,#8209,#8210,#8211,#8212,#8213,#8214,#8215,#8216,#8217,#8218,
#8219,#8220,#8221,#8222,#8223,#8224,#8225,#8226,#8227,#8228),
 .UNSPECIFIED.,.F.,.F.,(4,3,3,3,3,3,3,3,3,3,3,3,3,3,3,3,3,3,3,3,3,3,3,3,
3,3,3,3,3,3,3,3,3,3,3,3,3,3,3,3,3,3,3,3,3,3,3,3,3,4),(10.3761213044057,
10.4916473343449,10.6020836926387,10.7124212898676,10.8227045964878,10.932977995856,
11.0433574182079,11.153799603579,11.2644299007573,11.300329543919,11.412228455198,
11.5239351693938,11.6355347254555,11.7470696766159,11.8585824834668,11.9701986021098,
12.0818627300226,12.1937439049619,12.2969104176454,12.4084748637133,12.5198380200048,
12.6310887295725,12.7422701582708,12.8534253726942,12.9646803676604,13.0759808484134,
13.1874988487555,13.2934912913718,13.4052296275761,13.5167698094669,13.6281993328827,
13.7395610570682,13.8508977444198,13.9623346136356,14.07381749289,14.185516391903,
14.2900721650982,14.4018025327098,14.5133353791798,14.6247579576194,14.7361131396909,
14.8474437006735,14.9588751530412,15.0703529943081,15.1820475712269,15.2866530388247,
15.4088138904717,15.5306080160374,15.6518307149658,15.7079632679489),
 .UNSPECIFIED.);
#839=B_SPLINE_CURVE_WITH_KNOTS('',3,(#8231,#8232,#8233,#8234,#8235,#8236,
#8237,#8238,#8239,#8240,#8241,#8242,#8243,#8244,#8245,#8246,#8247,#8248,
#8249,#8250,#8251,#8252,#8253,#8254,#8255,#8256,#8257,#8258,#8259,#8260,
#8261,#8262,#8263,#8264,#8265,#8266,#8267,#8268,#8269,#8270,#8271,#8272,
#8273,#8274,#8275,#8276,#8277,#8278,#8279,#8280,#8281,#8282,#8283,#8284,
#8285,#8286,#8287,#8288,#8289,#8290,#8291,#8292,#8293,#8294,#8295,#8296,
#8297,#8298,#8299,#8300,#8301,#8302,#8303,#8304,#8305,#8306,#8307,#8308,
#8309,#8310,#8311,#8312,#8313,#8314,#8315,#8316,#8317,#8318,#8319,#8320,
#8321,#8322,#8323,#8324,#8325,#8326,#8327,#8328,#8329,#8330,#8331,#8332,
#8333,#8334,#8335,#8336,#8337,#8338,#8339,#8340,#8341,#8342),
 .UNSPECIFIED.,.F.,.F.,(4,3,3,3,3,3,3,3,3,3,3,3,3,3,3,3,3,3,3,3,3,3,3,3,
3,3,3,3,3,3,3,3,3,3,3,3,3,4),(11.6154215191107,11.7297194433804,11.8439615074736,
11.9581751212632,12.0723949424661,12.1866556269815,12.3010886611519,12.4156103002373,
12.5303749287406,12.6120023928371,12.722600396268,12.8333482550549,12.9435980012706,
13.0537674854308,13.1639012473881,13.275071752182,13.3853379846654,13.4969606256144,
13.6085832665635,13.7204465169992,13.8321110831576,13.9436645730413,14.0551496181406,
14.16660875264,14.2781656624489,14.3897674585362,14.5015817699047,14.6051641402899,
14.7170632550792,14.8287701821625,14.9403699566644,15.0519051314419,15.1634181667176,
15.2750345195736,15.3866988852361,15.4985803008964,15.6017450140163,15.7079632679489),
 .UNSPECIFIED.);
#840=B_SPLINE_CURVE_WITH_KNOTS('',3,(#8347,#8348,#8349,#8350,#8351,#8352,
#8353,#8354,#8355,#8356),.UNSPECIFIED.,.F.,.F.,(4,1,1,1,1,1,1,4),(15.7079632679489,
16.2832339125511,17.2798147862775,18.2763956600039,19.2729765337303,20.2695574074567,
21.2661382811831,21.9911485751285),.UNSPECIFIED.);
#841=B_SPLINE_CURVE_WITH_KNOTS('',3,(#8357,#8358,#8359,#8360,#8361,#8362,
#8363,#8364,#8365,#8366),.UNSPECIFIED.,.F.,.F.,(4,1,1,1,1,1,1,4),(15.7079720007471,
16.5983258877427,17.5949067614691,18.5914876351955,19.5880685089219,20.5846493826483,
21.5812302563748,21.9911424371547),.UNSPECIFIED.);
#842=B_SPLINE_CURVE_WITH_KNOTS('',3,(#8371,#8372,#8373,#8374,#8375,#8376,
#8377,#8378,#8379,#8380,#8381,#8382,#8383,#8384,#8385,#8386,#8387,#8388,
#8389,#8390,#8391,#8392,#8393,#8394,#8395,#8396,#8397,#8398,#8399,#8400,
#8401,#8402,#8403,#8404,#8405,#8406,#8407,#8408,#8409,#8410,#8411,#8412,
#8413,#8414,#8415,#8416,#8417,#8418,#8419,#8420,#8421,#8422,#8423,#8424,
#8425,#8426,#8427,#8428,#8429,#8430,#8431,#8432,#8433,#8434,#8435,#8436,
#8437,#8438,#8439,#8440,#8441,#8442,#8443,#8444,#8445,#8446,#8447,#8448,
#8449,#8450,#8451,#8452,#8453,#8454,#8455,#8456,#8457,#8458,#8459,#8460,
#8461,#8462,#8463,#8464,#8465,#8466,#8467,#8468,#8469,#8470,#8471,#8472,
#8473,#8474,#8475,#8476,#8477,#8478,#8479,#8480,#8481,#8482,#8483,#8484,
#8485,#8486,#8487,#8488,#8489,#8490,#8491,#8492,#8493,#8494,#8495,#8496,
#8497,#8498,#8499,#8500,#8501,#8502,#8503,#8504,#8505,#8506,#8507,#8508,
#8509,#8510,#8511,#8512,#8513,#8514,#8515,#8516,#8517,#8518,#8519,#8520,
#8521,#8522,#8523,#8524,#8525,#8526,#8527,#8528,#8529,#8530,#8531,#8532,
#8533,#8534,#8535,#8536,#8537,#8538,#8539,#8540,#8541,#8542),
 .UNSPECIFIED.,.F.,.F.,(4,3,3,3,3,3,3,3,3,3,3,3,3,3,3,3,3,3,3,3,3,3,3,3,
3,3,3,3,3,3,3,3,3,3,3,3,3,3,3,3,3,3,3,3,3,3,3,3,3,3,3,3,3,3,3,3,3,4),(21.9911485751285,
22.1309179503358,22.2627191549095,22.374427659155,22.4859378873352,22.5973374041085,
22.708669121392,22.8199758541662,22.9313830961258,23.0428364782555,23.154506491853,
23.2593000286359,23.3710083890299,23.4825184720439,23.5939178429524,23.7052494139272,
23.8165560002028,23.9279630965552,24.0394163333242,24.1510862038984,24.2558809023623,
24.3675891950941,24.479099207913,24.5904985071345,24.7018300050549,24.8131365170312,
24.9245435377139,25.0359966979394,25.1476664914795,25.2524617760888,25.3641701458249,
25.4756802374145,25.5870796164264,25.698411195018,25.8097177884088,25.9211248910232,
26.0325781335982,26.1442480091204,26.2490426498152,26.3607509985506,26.4722610688441,
26.5836604263951,26.6949919833986,26.8062985551115,26.9177056360823,27.0291588569969,
27.1408287111152,27.2456235235416,27.3573318547298,27.4688419071979,27.5802412467662,
27.69157278566,27.8028793391663,27.9142864019217,28.0257396045859,28.1374094406313,
28.242204397268,28.2743338823081),.UNSPECIFIED.);
#843=B_SPLINE_CURVE_WITH_KNOTS('',3,(#8543,#8544,#8545,#8546,#8547,#8548,
#8549,#8550,#8551,#8552,#8553,#8554,#8555,#8556,#8557,#8558,#8559,#8560,
#8561,#8562,#8563,#8564,#8565,#8566,#8567,#8568,#8569,#8570,#8571,#8572,
#8573,#8574,#8575,#8576,#8577,#8578,#8579,#8580,#8581,#8582,#8583,#8584,
#8585,#8586,#8587,#8588,#8589,#8590,#8591,#8592,#8593,#8594,#8595,#8596,
#8597,#8598,#8599,#8600,#8601,#8602,#8603,#8604,#8605,#8606,#8607,#8608,
#8609,#8610,#8611,#8612,#8613,#8614,#8615,#8616,#8617,#8618,#8619,#8620,
#8621,#8622,#8623,#8624,#8625,#8626,#8627,#8628,#8629,#8630,#8631,#8632,
#8633,#8634,#8635,#8636,#8637,#8638,#8639,#8640,#8641,#8642,#8643,#8644,
#8645,#8646,#8647,#8648,#8649,#8650,#8651,#8652,#8653,#8654,#8655,#8656,
#8657,#8658,#8659,#8660,#8661,#8662,#8663,#8664,#8665,#8666,#8667,#8668,
#8669,#8670,#8671,#8672,#8673,#8674,#8675,#8676,#8677,#8678,#8679,#8680),
 .UNSPECIFIED.,.F.,.F.,(4,2,2,2,2,2,2,2,2,2,2,2,2,2,2,2,2,2,2,2,2,2,2,2,
2,2,2,2,2,2,2,2,2,2,2,2,2,2,2,2,2,2,2,2,2,2,2,2,2,2,2,2,2,2,2,2,2,2,2,2,
2,2,2,2,2,2,2,2,4),(-1.96132285312146,-1.95620459237246,-1.95112567209526,
-1.94407886899802,-1.93468750571801,-1.89450594179228,-1.87724383315922,
-1.87143625996712,-1.86694093922326,-1.86026887903385,-1.83789122879064,
-1.81618308493092,-1.80542210271837,-1.79582903054646,-1.78805500328292,
-1.77835298749607,-1.74007387301098,-1.72193674407494,-1.71607184312288,
-1.71158118248237,-1.70498599765907,-1.67367749172583,-1.6513893744781,
-1.64126210789743,-1.63347268309289,-1.62422921768041,-1.58433775584925,
-1.56641843112916,-1.56056655351619,-1.55607455783141,-1.54946145498585,
-1.52436713357013,-1.50423730261349,-1.48998255539148,-1.48165848150001,
-1.47358902532616,-1.46108025679645,-1.4282076135,-1.41086123200036,-1.40504615407646,
-1.40054983866323,-1.39388294241964,-1.37115429218779,-1.3496453589913,
-1.3389271195264,-1.32935873731568,-1.32158243299074,-1.31184947095414,
-1.27375464582685,-1.25550601013682,-1.24963320639476,-1.24514198355881,
-1.23855416260086,-1.20717250984067,-1.18487207018713,-1.17476070399432,
-1.16696998774258,-1.15771014629021,-1.11807295920766,-1.0999546380503,
-1.09408914514634,-1.0895968159218,-1.0840808169788,-1.05331978181438,-1.02917947127776,
-1.01912619633388,-1.01133793422825,-1.00203406270535,-0.980953657893252),
 .UNSPECIFIED.);
#844=B_SPLINE_CURVE_WITH_KNOTS('',3,(#8685,#8686,#8687,#8688,#8689,#8690,
#8691,#8692,#8693,#8694,#8695,#8696,#8697,#8698,#8699,#8700,#8701,#8702,
#8703,#8704,#8705,#8706,#8707,#8708,#8709,#8710,#8711,#8712,#8713,#8714,
#8715,#8716,#8717,#8718,#8719,#8720,#8721,#8722,#8723,#8724,#8725,#8726,
#8727,#8728,#8729,#8730,#8731,#8732,#8733,#8734,#8735,#8736,#8737,#8738,
#8739,#8740,#8741,#8742,#8743,#8744,#8745,#8746,#8747,#8748,#8749,#8750,
#8751,#8752,#8753,#8754,#8755,#8756,#8757,#8758,#8759,#8760,#8761,#8762,
#8763,#8764,#8765,#8766,#8767,#8768,#8769,#8770,#8771,#8772,#8773,#8774,
#8775,#8776,#8777,#8778,#8779,#8780,#8781,#8782,#8783,#8784,#8785,#8786,
#8787,#8788,#8789,#8790,#8791,#8792,#8793,#8794,#8795,#8796,#8797,#8798,
#8799,#8800,#8801,#8802,#8803,#8804,#8805,#8806,#8807,#8808,#8809,#8810,
#8811,#8812,#8813,#8814,#8815,#8816,#8817,#8818,#8819,#8820,#8821,#8822,
#8823,#8824,#8825,#8826,#8827,#8828,#8829,#8830,#8831,#8832,#8833,#8834,
#8835,#8836,#8837,#8838,#8839,#8840,#8841,#8842,#8843,#8844,#8845,#8846,
#8847,#8848,#8849,#8850,#8851,#8852,#8853,#8854,#8855,#8856),
 .UNSPECIFIED.,.F.,.F.,(4,3,3,3,3,3,3,3,3,3,3,3,3,3,3,3,3,3,3,3,3,3,3,3,
3,3,3,3,3,3,3,3,3,3,3,3,3,3,3,3,3,3,3,3,3,3,3,3,3,3,3,3,3,3,3,3,3,4),(28.2743338828609,
28.3854499463252,28.4963720118464,28.6071867805496,28.717938100074,28.8286697232354,
28.9395040413308,29.0503910293875,29.1614837232968,29.2387852709944,29.3504936415298,
29.4620037336245,29.5734031129625,29.6847346917019,29.7960412850625,29.9074483873677,
30.0189016294807,30.1305715042882,30.2353661447208,30.3470744333655,30.4585844436019,
30.5699837411555,30.6813152383203,30.7926217504515,30.9040287727149,31.0154819353028,
31.1271517324974,31.2319470184472,31.3436553843173,31.4551654707913,31.5665648439344,
31.6778964159218,31.7892030019896,31.9006100962241,32.012063329828,32.123733195506,
32.2285278921736,32.3402364003461,32.4517466310075,32.5631461493833,32.6744778673927,
32.785784600018,32.8971918404589,33.0086452203188,33.1203152304052,33.2251087659,
33.3368166944272,33.4483263452669,33.5597252840978,33.6710564238063,33.7823625803406,
33.893769252746,34.0052220680331,34.1168915267853,34.2216896396264,34.3523579101859,
34.481718471605,34.5575191891205),.UNSPECIFIED.);
#845=B_SPLINE_CURVE_WITH_KNOTS('',3,(#8857,#8858,#8859,#8860,#8861,#8862,
#8863,#8864,#8865,#8866,#8867,#8868,#8869,#8870,#8871,#8872,#8873,#8874,
#8875,#8876,#8877,#8878,#8879,#8880,#8881,#8882,#8883,#8884,#8885,#8886,
#8887,#8888,#8889,#8890,#8891,#8892,#8893,#8894,#8895,#8896,#8897,#8898,
#8899,#8900,#8901,#8902,#8903,#8904,#8905,#8906,#8907,#8908,#8909,#8910,
#8911,#8912,#8913,#8914,#8915,#8916,#8917,#8918,#8919,#8920,#8921,#8922,
#8923,#8924,#8925,#8926,#8927,#8928,#8929,#8930,#8931,#8932,#8933,#8934,
#8935,#8936,#8937,#8938,#8939,#8940,#8941,#8942,#8943,#8944,#8945,#8946,
#8947,#8948,#8949,#8950,#8951,#8952,#8953,#8954,#8955,#8956,#8957,#8958,
#8959,#8960,#8961,#8962,#8963,#8964,#8965,#8966,#8967,#8968,#8969,#8970,
#8971,#8972,#8973,#8974,#8975,#8976,#8977,#8978,#8979,#8980,#8981,#8982,
#8983,#8984,#8985,#8986,#8987,#8988,#8989,#8990,#8991,#8992,#8993,#8994,
#8995,#8996),.UNSPECIFIED.,.F.,.F.,(4,2,2,2,2,2,2,2,2,2,2,2,2,2,2,2,2,2,
2,2,2,2,2,2,2,2,2,2,2,2,2,2,2,2,2,2,2,2,2,2,2,2,2,2,2,2,2,2,2,2,2,2,2,2,
2,2,2,2,2,2,2,2,2,2,2,2,2,2,2,4),(-0.980953657893252,-0.980813396397935,
-0.955825212739871,-0.943612668389274,-0.938075535682952,-0.933530523620638,
-0.926387108249715,-0.917187136880064,-0.891575066392669,-0.871442485613437,
-0.862182467834695,-0.854390254493591,-0.84427514937946,-0.82195729914483,
-0.790548017891759,-0.783957446457071,-0.779465309749546,-0.773592415631755,
-0.75534666273614,-0.717271876975574,-0.707538037175336,-0.699760128965384,
-0.690188684683091,-0.679464964866124,-0.657945149813074,-0.635181541542285,
-0.628511621408875,-0.624014213815331,-0.618198689398315,-0.600853494376346,
-0.567993231076083,-0.55548889750843,-0.547418543701117,-0.539090498054099,
-0.524821319297738,-0.504659878418917,-0.479565266719354,-0.472947877141004,
-0.468454504327042,-0.462602573191408,-0.444692631037342,-0.404807213794938,
-0.395563469735401,-0.387771635305561,-0.377638263679984,-0.355330862736666,
-0.32399450758584,-0.317395394883157,-0.312903502814609,-0.307038978128349,
-0.288918093124817,-0.249325569582235,-0.240067474399635,-0.232277288530633,
-0.222165390712545,-0.199853076120437,-0.168449642021253,-0.161861071291552,
-0.157370110224777,-0.151498510169382,-0.133253786386207,-0.0951955524731001,
-0.0854632416836036,-0.0776873239873771,-0.0681192646751081,-0.0392851986217844,
-0.0134167361551964,-0.00672038349945225,-0.0032887601749484,-0.000457478374081271),
 .UNSPECIFIED.);
#846=B_SPLINE_CURVE_WITH_KNOTS('',3,(#9001,#9002,#9003,#9004,#9005,#9006,
#9007,#9008,#9009,#9010,#9011,#9012,#9013,#9014,#9015,#9016,#9017,#9018,
#9019,#9020,#9021,#9022,#9023,#9024,#9025,#9026,#9027,#9028,#9029,#9030,
#9031,#9032,#9033,#9034,#9035,#9036,#9037,#9038,#9039,#9040,#9041,#9042,
#9043,#9044,#9045,#9046,#9047,#9048,#9049,#9050,#9051,#9052,#9053,#9054,
#9055,#9056,#9057,#9058,#9059,#9060,#9061,#9062,#9063,#9064,#9065,#9066,
#9067,#9068,#9069,#9070,#9071,#9072,#9073,#9074,#9075,#9076,#9077,#9078,
#9079,#9080,#9081,#9082,#9083,#9084,#9085,#9086,#9087,#9088,#9089,#9090,
#9091,#9092,#9093,#9094,#9095,#9096,#9097,#9098,#9099,#9100,#9101,#9102,
#9103,#9104,#9105,#9106,#9107,#9108,#9109,#9110,#9111,#9112,#9113,#9114,
#9115,#9116,#9117,#9118,#9119,#9120,#9121,#9122,#9123,#9124,#9125,#9126,
#9127,#9128,#9129,#9130,#9131,#9132,#9133,#9134,#9135,#9136,#9137,#9138,
#9139,#9140,#9141,#9142,#9143,#9144,#9145,#9146,#9147,#9148,#9149,#9150,
#9151,#9152,#9153,#9154,#9155,#9156,#9157,#9158,#9159,#9160,#9161,#9162,
#9163,#9164,#9165,#9166,#9167,#9168,#9169,#9170,#9171,#9172),
 .UNSPECIFIED.,.F.,.F.,(4,3,3,3,3,3,3,3,3,3,3,3,3,3,3,3,3,3,3,3,3,3,3,3,
3,3,3,3,3,3,3,3,3,3,3,3,3,3,3,3,3,3,3,3,3,3,3,3,3,3,3,3,3,3,3,3,3,4),(34.5575191894877,
34.6688302723381,34.7801258851517,34.8915360000216,35.0030001705123,35.1146924423315,
35.2182705133528,35.329979844159,35.4414909051851,35.5528912580536,35.6642238132373,
35.7755313842774,35.8869394583062,35.9983936704943,36.1100644998149,36.2148513870793,
36.3265566868323,36.4380637110229,36.5494600262282,36.6607885496869,36.7720921017016,
36.8834962086944,36.9949464756927,37.1066134484121,37.2114322608057,37.3231433221254,
37.4346560660442,37.5460580718723,37.6573922476748,37.76870140455,37.8801109978221,
37.9915666953808,38.1032389338652,38.2080131345321,38.3197270786042,38.4312428141906,
38.5426478756073,38.6539851650298,38.765297487747,38.8767103021909,38.9881692564661,
39.0998447680595,39.2045940082585,39.3162806032607,39.4277689172748,39.5391465312969,
39.6504563936481,39.7617413557063,39.8731271322649,39.9845591801971,40.0962083605028,
40.2011748819849,40.3134130635302,40.4254718990606,40.5373841223235,40.6492090027682,
40.7610153241071,40.8407044966673),.UNSPECIFIED.);
#847=B_SPLINE_CURVE_WITH_KNOTS('',3,(#9173,#9174,#9175,#9176,#9177,#9178,
#9179,#9180,#9181,#9182,#9183,#9184,#9185,#9186,#9187,#9188,#9189,#9190,
#9191,#9192,#9193,#9194,#9195,#9196,#9197,#9198,#9199,#9200,#9201,#9202,
#9203,#9204,#9205,#9206,#9207,#9208,#9209,#9210,#9211,#9212,#9213,#9214,
#9215,#9216,#9217,#9218,#9219,#9220,#9221,#9222,#9223,#9224,#9225,#9226,
#9227,#9228,#9229,#9230,#9231,#9232,#9233,#9234,#9235,#9236,#9237,#9238,
#9239,#9240,#9241,#9242,#9243,#9244,#9245,#9246,#9247,#9248,#9249,#9250,
#9251,#9252,#9253,#9254,#9255,#9256,#9257,#9258,#9259,#9260,#9261,#9262,
#9263,#9264,#9265,#9266,#9267,#9268,#9269,#9270,#9271,#9272,#9273,#9274,
#9275,#9276,#9277,#9278,#9279,#9280,#9281,#9282,#9283,#9284,#9285,#9286,
#9287,#9288,#9289,#9290,#9291,#9292,#9293,#9294,#9295,#9296,#9297,#9298,
#9299,#9300,#9301,#9302,#9303,#9304,#9305,#9306,#9307,#9308,#9309,#9310,
#9311,#9312,#9313,#9314,#9315,#9316,#9317,#9318,#9319,#9320,#9321,#9322,
#9323,#9324,#9325,#9326,#9327,#9328,#9329,#9330,#9331,#9332,#9333,#9334,
#9335,#9336,#9337,#9338,#9339,#9340,#9341,#9342,#9343,#9344),
 .UNSPECIFIED.,.F.,.F.,(4,3,3,3,3,3,3,3,3,3,3,3,3,3,3,3,3,3,3,3,3,3,3,3,
3,3,3,3,3,3,3,3,3,3,3,3,3,3,3,3,3,3,3,3,3,3,3,3,3,3,3,3,3,3,3,3,3,4),(34.557519189864,
34.6688316922454,34.7799480549331,34.8909555466978,35.0018977265956,35.1128180578458,
35.2238400790169,35.334912289609,35.4461940347629,35.5333624885445,35.6450709986202,
35.7565812311951,35.8679807514893,35.9793124714191,36.0906192059629,36.2020264483047,
36.3134798300591,36.4251498420039,36.5299433622709,36.6416512870095,36.7531609340692,
36.864559869128,36.9758910050783,37.0871971578746,37.1986038266028,37.3100566382399,
37.4217260934356,37.5265242359973,37.6382328481534,37.7497431759177,37.861142787168,
37.9724745937193,38.0837814104442,38.1951887274329,38.3066421798417,38.4183122548369,
38.5231051097237,38.634814450544,38.7463255216522,38.8577258846371,38.9690584499545,
39.0803660311285,39.1917741152101,39.3032283374232,39.4148991765908,39.5196859834501,
39.6313912609588,39.7428982629309,39.8542945559475,39.9656230572843,40.0769265872794,
40.1883306725875,40.2997809180481,40.4114478697587,40.5162668571765,40.6484523927198,
40.7791766765676,40.8407044966673),.UNSPECIFIED.);
#848=B_SPLINE_CURVE_WITH_KNOTS('',3,(#9349,#9350,#9351,#9352,#9353,#9354,
#9355,#9356,#9357,#9358,#9359,#9360,#9361,#9362,#9363,#9364,#9365,#9366,
#9367,#9368,#9369,#9370,#9371,#9372,#9373,#9374,#9375,#9376,#9377,#9378,
#9379,#9380,#9381,#9382,#9383,#9384,#9385,#9386,#9387,#9388,#9389,#9390,
#9391,#9392,#9393,#9394,#9395,#9396,#9397,#9398,#9399,#9400,#9401,#9402,
#9403,#9404,#9405,#9406,#9407,#9408,#9409,#9410,#9411,#9412,#9413,#9414,
#9415,#9416,#9417,#9418,#9419,#9420,#9421,#9422,#9423,#9424,#9425,#9426,
#9427,#9428,#9429,#9430,#9431,#9432,#9433,#9434,#9435,#9436,#9437,#9438,
#9439,#9440,#9441,#9442,#9443,#9444,#9445,#9446,#9447,#9448,#9449,#9450,
#9451,#9452,#9453,#9454,#9455,#9456,#9457,#9458,#9459,#9460,#9461,#9462,
#9463,#9464,#9465,#9466,#9467,#9468,#9469,#9470,#9471,#9472,#9473,#9474,
#9475,#9476,#9477,#9478,#9479,#9480,#9481,#9482,#9483,#9484,#9485,#9486,
#9487,#9488,#9489,#9490,#9491,#9492,#9493,#9494,#9495,#9496,#9497,#9498,
#9499,#9500,#9501,#9502,#9503,#9504,#9505,#9506,#9507,#9508,#9509,#9510,
#9511,#9512,#9513,#9514,#9515,#9516,#9517,#9518,#9519,#9520),
 .UNSPECIFIED.,.F.,.F.,(4,3,3,3,3,3,3,3,3,3,3,3,3,3,3,3,3,3,3,3,3,3,3,3,
3,3,3,3,3,3,3,3,3,3,3,3,3,3,3,3,3,3,3,3,3,3,3,3,3,3,3,3,3,3,3,3,3,4),(40.840704497049,
40.9675412582679,41.0954926672062,41.1977557557113,41.3094929575612,41.421032422769,
41.5324614834252,41.643822998072,41.755159728709,41.8665970369413,41.9780805721873,
42.0897804857431,42.1943366294377,42.3058933565765,42.4172516335834,42.5284991889107,
42.6396791835826,42.750834681469,42.8620926517494,42.9733975818198,43.0849224744629,
43.1909175031641,43.3028373726712,43.4145573215697,43.5261654134577,43.6377042144518,
43.7492161924285,43.8608241682442,43.972476138112,44.0843385386926,44.1874983768905,
44.2993486307196,44.4110045193044,44.5225519596468,44.6340335782541,44.7454919074656,
44.8570521214737,44.9686594749185,45.0804830762105,45.1840792506169,45.2946069224391,
45.4053635726771,45.5155858115154,45.6257438851437,45.7358823024636,45.8470767579335,
45.9573868777162,46.0690235010297,46.1806601243433,46.2985638342812,46.4122814276395,
46.5258600264502,46.6393375177506,46.7527516466314,46.8661750751564,46.9796037930555,
47.0931212124098,47.1238898038469),.UNSPECIFIED.);
#849=B_SPLINE_CURVE_WITH_KNOTS('',3,(#9521,#9522,#9523,#9524,#9525,#9526,
#9527,#9528,#9529,#9530),.UNSPECIFIED.,.F.,.F.,(4,1,1,1,1,1,1,4),(40.8407044966673,
41.5128477309029,42.5094286046293,43.5060094783558,44.5025903520822,45.4991712258086,
46.495752099535,47.1238898038469),.UNSPECIFIED.);
#850=B_SPLINE_CURVE_WITH_KNOTS('',3,(#9536,#9537,#9538,#9539,#9540,#9541,
#9542,#9543,#9544,#9545,#9546,#9547,#9548,#9549,#9550,#9551,#9552,#9553,
#9554,#9555,#9556,#9557,#9558,#9559,#9560,#9561,#9562,#9563,#9564,#9565,
#9566,#9567,#9568,#9569,#9570,#9571,#9572,#9573,#9574,#9575,#9576,#9577,
#9578,#9579,#9580,#9581,#9582,#9583,#9584,#9585,#9586,#9587,#9588,#9589,
#9590,#9591,#9592,#9593,#9594,#9595,#9596),.UNSPECIFIED.,.F.,.F.,(4,3,3,
3,3,3,3,3,3,3,3,3,3,3,3,3,3,3,3,3,4),(-4.0925417488383,-3.98632349490564,
-3.8806065760191,-3.77504892759528,-3.66961679425259,-3.56425173722768,
-3.45891795737562,-3.35357970118907,-3.24813369183657,-3.14262668426877,
-3.03694351958941,-2.98974262117923,-2.88522737486616,-2.78088717581065,
-2.67664451339593,-2.57246188586147,-2.4683018734843,-2.36405791614842,
-2.25977409419914,-2.15530886452125,-2.0655090872996),.UNSPECIFIED.);
#851=B_SPLINE_CURVE_WITH_KNOTS('',3,(#9599,#9600,#9601,#9602,#9603,#9604,
#9605,#9606,#9607,#9608,#9609,#9610,#9611,#9612,#9613,#9614,#9615,#9616,
#9617,#9618,#9619,#9620,#9621,#9622,#9623,#9624,#9625,#9626,#9627,#9628,
#9629,#9630,#9631,#9632),.UNSPECIFIED.,.F.,.F.,(4,3,3,3,3,3,3,3,3,3,3,4),
(0.,0.107961337641792,0.219038779652369,0.326921378979617,0.434806064728355,
0.542722047025971,0.656186753701081,0.764334836393998,0.872582285248723,
0.981026153163143,0.99658087372641,1.11419103802958),.UNSPECIFIED.);
#852=B_SPLINE_CURVE_WITH_KNOTS('',3,(#9637,#9638,#9639,#9640,#9641,#9642,
#9643,#9644,#9645,#9646,#9647,#9648,#9649,#9650,#9651,#9652,#9653,#9654,
#9655,#9656,#9657,#9658,#9659,#9660,#9661,#9662,#9663,#9664,#9665,#9666,
#9667,#9668,#9669,#9670,#9671,#9672,#9673,#9674,#9675,#9676,#9677,#9678,
#9679,#9680,#9681,#9682,#9683,#9684,#9685,#9686,#9687,#9688,#9689,#9690,
#9691,#9692,#9693,#9694,#9695,#9696,#9697,#9698,#9699,#9700,#9701,#9702,
#9703,#9704,#9705,#9706,#9707,#9708,#9709,#9710,#9711,#9712,#9713,#9714,
#9715,#9716,#9717,#9718,#9719,#9720,#9721,#9722,#9723,#9724,#9725,#9726,
#9727,#9728,#9729,#9730,#9731,#9732,#9733,#9734,#9735,#9736,#9737,#9738,
#9739,#9740,#9741,#9742,#9743,#9744,#9745,#9746,#9747,#9748,#9749,#9750,
#9751,#9752,#9753,#9754,#9755,#9756,#9757,#9758,#9759,#9760,#9761,#9762,
#9763,#9764,#9765,#9766,#9767,#9768,#9769,#9770,#9771,#9772,#9773,#9774,
#9775,#9776,#9777,#9778,#9779,#9780,#9781,#9782,#9783,#9784,#9785,#9786,
#9787,#9788,#9789,#9790,#9791,#9792,#9793,#9794,#9795,#9796,#9797,#9798,
#9799,#9800,#9801,#9802,#9803,#9804,#9805,#9806,#9807,#9808,#9809,#9810,
#9811,#9812,#9813,#9814,#9815,#9816,#9817,#9818,#9819,#9820,#9821,#9822,
#9823,#9824,#9825,#9826),.UNSPECIFIED.,.F.,.F.,(4,3,3,3,3,3,3,3,3,3,3,3,
3,3,3,3,3,3,3,3,3,3,3,3,3,3,3,3,3,3,3,3,3,3,3,3,3,3,3,3,3,3,3,3,3,3,3,3,
3,3,3,3,3,3,3,3,3,3,3,3,3,3,3,4),(-10.3757270556279,-10.2603201973078,-10.1445336437559,
-10.0282150027605,-9.96580873726409,-9.86028927215325,-9.75492847331709,
-9.64969134822421,-9.54452003581519,-9.43937844760692,-9.33423053922648,
-9.22897081685299,-9.12364803666882,-9.01814404094799,-8.96922786353768,
-8.86370563787302,-8.75834200872327,-8.65310196527416,-8.54792768174384,
-8.44278307461432,-8.33763210442475,-8.23236927738943,-8.12704336360686,
-8.02153622334535,-7.97264698981127,-7.86715075765798,-7.76181321062035,
-7.6565992534656,-7.55145104369272,-7.44633245870662,-7.34120741993228,
-7.23597021141746,-7.13066977480084,-7.02518762842015,-6.97606611608487,
-6.87052576919234,-6.76514418013918,-6.65988649813285,-6.55469478529848,
-6.44953298257136,-6.34436507518073,-6.23908581202828,-6.13374372441396,
-6.02822097903251,-5.97948524235845,-5.87394087033654,-5.76855477542758,
-5.66329190907334,-5.55809459516582,-5.45292678697872,-5.34775248164705,
-5.24246628022602,-5.137116936034,-5.03158652718211,-4.98290436863205,-4.87887809662516,
-4.77503069661956,-4.67128271432363,-4.56759611534961,-4.46393295588709,
-4.36019408038179,-4.25641481532146,-4.15247510001566,-4.09254174928664),
 .UNSPECIFIED.);
#853=B_SPLINE_CURVE_WITH_KNOTS('',3,(#9827,#9828,#9829,#9830,#9831,#9832,
#9833,#9834,#9835,#9836,#9837,#9838,#9839,#9840,#9841,#9842,#9843,#9844,
#9845,#9846,#9847,#9848,#9849,#9850,#9851,#9852,#9853,#9854,#9855,#9856,
#9857,#9858,#9859,#9860,#9861,#9862,#9863,#9864,#9865,#9866,#9867,#9868,
#9869,#9870,#9871,#9872,#9873,#9874,#9875,#9876,#9877,#9878,#9879,#9880,
#9881,#9882,#9883,#9884,#9885,#9886,#9887,#9888,#9889,#9890,#9891,#9892,
#9893,#9894,#9895,#9896,#9897,#9898,#9899,#9900,#9901,#9902,#9903,#9904,
#9905,#9906,#9907,#9908,#9909,#9910,#9911,#9912,#9913,#9914,#9915,#9916,
#9917,#9918,#9919,#9920,#9921,#9922,#9923,#9924,#9925,#9926,#9927,#9928,
#9929,#9930,#9931,#9932,#9933,#9934,#9935,#9936,#9937,#9938,#9939,#9940,
#9941,#9942,#9943,#9944,#9945,#9946,#9947,#9948,#9949,#9950,#9951,#9952,
#9953,#9954,#9955,#9956,#9957,#9958,#9959,#9960,#9961,#9962,#9963,#9964,
#9965,#9966,#9967,#9968,#9969,#9970,#9971,#9972,#9973,#9974,#9975,#9976,
#9977,#9978,#9979,#9980,#9981,#9982,#9983,#9984,#9985,#9986,#9987,#9988,
#9989,#9990,#9991,#9992,#9993,#9994,#9995,#9996,#9997,#9998,#9999,#10000,
#10001,#10002,#10003,#10004,#10005,#10006,#10007,#10008,#10009,#10010,#10011,
#10012,#10013,#10014,#10015,#10016),.UNSPECIFIED.,.F.,.F.,(4,3,3,3,3,3,
3,3,3,3,3,3,3,3,3,3,3,3,3,3,3,3,3,3,3,3,3,3,3,3,3,3,3,3,3,3,3,3,3,3,3,3,
3,3,3,3,3,3,3,3,3,3,3,3,3,3,3,3,3,3,3,3,3,4),(1.1141910384302,1.21724238536229,
1.32013451940758,1.42293952840389,1.52569615018617,1.62844303717372,1.73128762649966,
1.83418552892842,1.93726302853852,1.99316174745282,2.09882380530125,2.20432723759868,
2.30970630945701,2.41501904637471,2.52030130546123,2.6255888990106,2.73098582593673,
2.83644458423451,2.94208122698967,2.98974262117923,3.09543951511606,3.20098166055225,
3.30640502061617,3.41176548868121,3.51709885740447,3.62244087818947,3.72789690172061,
3.83341751346996,3.93911962813779,3.98632349490564,4.0917044614259,4.19692477051366,
4.30201914206295,4.40704637515871,4.51204277383473,4.61704459671652,4.72215786837924,
4.82733377201964,4.93269176979785,4.98290436863205,5.08844958739658,5.19383628319048,
5.29909938551099,5.40429670879907,5.50946430050027,5.61463816396031,5.71992358734267,
5.82527196030934,5.93080111180776,5.97948524235846,6.08502293419099,6.19040246033145,
6.29565896133579,6.40085004111363,6.50601175791134,6.61118012626058,6.71646067026086,
6.82180450898166,6.92732970844785,6.97606611608487,7.09145618049413,7.20651961582625,
7.32105406185355,7.39737634485402),.UNSPECIFIED.);
#854=B_SPLINE_CURVE_WITH_KNOTS('',3,(#10021,#10022,#10023,#10024,#10025,
#10026,#10027,#10028,#10029,#10030,#10031,#10032,#10033,#10034,#10035,#10036,
#10037,#10038,#10039,#10040,#10041,#10042,#10043,#10044,#10045,#10046,#10047,
#10048,#10049,#10050,#10051,#10052,#10053,#10054,#10055,#10056,#10057,#10058,
#10059,#10060,#10061,#10062,#10063,#10064,#10065,#10066,#10067,#10068,#10069,
#10070,#10071,#10072,#10073,#10074,#10075,#10076,#10077,#10078,#10079,#10080,
#10081,#10082,#10083,#10084,#10085,#10086,#10087,#10088,#10089,#10090,#10091,
#10092,#10093,#10094,#10095,#10096,#10097,#10098,#10099,#10100,#10101,#10102,
#10103,#10104,#10105,#10106,#10107,#10108,#10109,#10110,#10111,#10112,#10113,
#10114,#10115,#10116,#10117,#10118,#10119,#10120,#10121,#10122,#10123,#10124,
#10125,#10126,#10127,#10128,#10129,#10130,#10131,#10132,#10133,#10134,#10135,
#10136,#10137,#10138,#10139,#10140,#10141,#10142,#10143,#10144,#10145,#10146,
#10147,#10148,#10149,#10150,#10151,#10152,#10153,#10154,#10155,#10156,#10157,
#10158,#10159,#10160,#10161,#10162,#10163,#10164,#10165,#10166,#10167,#10168,
#10169,#10170,#10171,#10172,#10173,#10174,#10175,#10176,#10177,#10178,#10179,
#10180,#10181,#10182,#10183,#10184,#10185,#10186,#10187,#10188,#10189,#10190,
#10191,#10192,#10193,#10194,#10195,#10196,#10197,#10198,#10199,#10200,#10201,
#10202,#10203,#10204,#10205,#10206,#10207,#10208,#10209,#10210),
 .UNSPECIFIED.,.F.,.F.,(4,3,3,3,3,3,3,3,3,3,3,3,3,3,3,3,3,3,3,3,3,3,3,3,
3,3,3,3,3,3,3,3,3,3,3,3,3,3,3,3,3,3,3,3,3,3,3,3,3,3,3,3,3,3,3,3,3,3,3,3,
3,3,3,4),(-16.6589123631975,-16.5545511958811,-16.4502386019145,-16.3459373792312,
-16.2415362416226,-16.137085871038,-16.0324418402436,-15.9452939796226,
-15.8397770700368,-15.7344188085268,-15.6291841820779,-15.5240153429194,
-15.4188761990729,-15.3137307026416,-15.2084733274019,-15.1031528607631,
-14.9976511031837,-14.9487131058961,-14.8431960601418,-14.7378376610968,
-14.6326028957819,-14.5274339170148,-14.4222946330346,-14.3171489961608,
-14.2118914809822,-14.1065708744896,-14.0010689786592,-13.9521322321697,
-13.8466157393099,-13.7412578942317,-13.6360236817893,-13.5308552548952,
-13.4257165209662,-13.320571431498,-13.2153144560297,-13.1099943856376,
-13.0044930147749,-12.9555513584433,-12.8500342162662,-12.7446757247133,
-12.6394408730377,-12.5342718117636,-12.4291324492193,-12.323986737817,
-12.2187291546315,-12.1134084837545,-12.0079065297216,-11.9589704847169,
-11.8534526542618,-11.748093464529,-11.6428579035958,-11.5376881266243,
-11.4325480430808,-11.3274016065083,-11.2221432969162,-11.1168218978768,
-11.011319220686,-10.9623896109905,-10.8549891203279,-10.7477671220517,
-10.64071973154,-10.5337747634674,-10.4269036873047,-10.3757270560179),
 .UNSPECIFIED.);
#855=B_SPLINE_CURVE_WITH_KNOTS('',3,(#10211,#10212,#10213,#10214,#10215,
#10216,#10217,#10218,#10219,#10220,#10221,#10222,#10223,#10224,#10225,#10226,
#10227,#10228,#10229,#10230,#10231,#10232,#10233,#10234,#10235,#10236,#10237,
#10238,#10239,#10240,#10241,#10242,#10243,#10244,#10245,#10246,#10247,#10248,
#10249,#10250,#10251,#10252,#10253,#10254,#10255,#10256,#10257,#10258,#10259,
#10260,#10261,#10262,#10263,#10264,#10265,#10266,#10267,#10268,#10269,#10270,
#10271,#10272,#10273,#10274,#10275,#10276,#10277,#10278,#10279,#10280,#10281,
#10282,#10283,#10284,#10285,#10286,#10287,#10288,#10289,#10290,#10291,#10292,
#10293,#10294,#10295,#10296,#10297,#10298,#10299,#10300,#10301,#10302,#10303,
#10304,#10305,#10306,#10307,#10308,#10309,#10310,#10311,#10312,#10313,#10314,
#10315,#10316,#10317,#10318,#10319,#10320,#10321,#10322,#10323,#10324,#10325,
#10326,#10327,#10328,#10329,#10330,#10331,#10332,#10333,#10334,#10335,#10336,
#10337,#10338,#10339,#10340,#10341,#10342,#10343,#10344,#10345,#10346,#10347,
#10348,#10349,#10350,#10351,#10352,#10353,#10354,#10355,#10356,#10357,#10358,
#10359,#10360,#10361,#10362,#10363,#10364,#10365,#10366,#10367,#10368,#10369,
#10370,#10371,#10372,#10373,#10374,#10375,#10376,#10377,#10378,#10379,#10380,
#10381,#10382,#10383,#10384,#10385,#10386,#10387,#10388,#10389,#10390,#10391,
#10392,#10393,#10394,#10395,#10396,#10397,#10398,#10399,#10400),
 .UNSPECIFIED.,.F.,.F.,(4,3,3,3,3,3,3,3,3,3,3,3,3,3,3,3,3,3,3,3,3,3,3,3,
3,3,3,3,3,3,3,3,3,3,3,3,3,3,3,3,3,3,3,3,3,3,3,3,3,3,3,3,3,3,3,3,3,3,3,3,
3,3,3,4),(7.39737634520917,7.50456439630629,7.61181522811691,7.71924509232096,
7.82677710957531,7.93452849807945,7.97264698981128,8.07816920580473,8.18353281643424,
8.28877282842248,8.39394707248107,8.49909163221348,8.60424254715776,8.70950530751115,
8.81483114798237,8.92033820552726,8.96922786353769,9.07474698125424,9.18010750983923,
9.28534447958761,9.3905157080399,9.49565728357395,9.60080525053357,9.70606513833576,
9.81138814522112,9.91689245928984,9.96580873726409,10.0713229311903,10.1766784331036,
10.2819102485202,10.3870762463539,10.4922125229136,10.5973551303976,10.7026096036371,
10.8079271565927,10.913426012931,10.9623896109905,11.0679074212527,11.1732665931826,
11.278502139918,11.3836719049369,11.4888119787845,11.5939584079301,11.6992167135617,
11.8045381106151,11.9100407888698,11.9589704847169,12.0644875831434,12.1698460407086,
12.2750808729378,12.3802499237993,12.485389284951,12.590535003977,12.6957926083047,
12.8011133080766,12.9066153025981,12.9555513584433,13.0600577982311,13.1644187171345,
13.2686717663154,13.3728782799186,13.4770515526009,13.5812931985021,13.6805616523888),
 .UNSPECIFIED.);
#856=B_SPLINE_CURVE_WITH_KNOTS('',3,(#10405,#10406,#10407,#10408,#10409,
#10410,#10411,#10412,#10413,#10414,#10415),.UNSPECIFIED.,.F.,.F.,(4,1,1,
1,1,1,1,1,4),(-22.9420976703771,-22.9213600957074,-21.924779221981,-20.9281983482546,
-19.9316174745282,-18.9350366008018,-17.9384557270754,-16.941874853349,
-16.6589168227746),.UNSPECIFIED.);
#857=B_SPLINE_CURVE_WITH_KNOTS('',3,(#10416,#10417,#10418,#10419,#10420,
#10421,#10422,#10423,#10424,#10425,#10426,#10427,#10428,#10429,#10430,#10431,
#10432,#10433,#10434,#10435,#10436,#10437,#10438,#10439,#10440,#10441,#10442,
#10443,#10444,#10445,#10446,#10447,#10448,#10449,#10450,#10451,#10452,#10453,
#10454,#10455,#10456,#10457,#10458,#10459,#10460,#10461,#10462,#10463,#10464,
#10465,#10466,#10467,#10468,#10469,#10470,#10471,#10472,#10473,#10474,#10475,
#10476,#10477,#10478,#10479,#10480,#10481,#10482,#10483,#10484,#10485,#10486,
#10487,#10488,#10489,#10490,#10491,#10492,#10493,#10494,#10495,#10496,#10497,
#10498,#10499,#10500,#10501,#10502,#10503,#10504,#10505,#10506,#10507,#10508,
#10509,#10510,#10511,#10512,#10513,#10514,#10515,#10516,#10517,#10518,#10519,
#10520,#10521,#10522,#10523,#10524,#10525,#10526,#10527,#10528,#10529,#10530,
#10531,#10532,#10533,#10534,#10535,#10536,#10537,#10538,#10539,#10540,#10541,
#10542,#10543,#10544,#10545,#10546,#10547,#10548,#10549,#10550,#10551,#10552,
#10553,#10554,#10555,#10556,#10557,#10558,#10559,#10560,#10561,#10562,#10563,
#10564,#10565,#10566,#10567,#10568,#10569,#10570,#10571,#10572,#10573,#10574,
#10575,#10576,#10577,#10578,#10579,#10580,#10581,#10582,#10583,#10584,#10585,
#10586,#10587,#10588,#10589,#10590,#10591,#10592,#10593,#10594,#10595,#10596,
#10597,#10598,#10599,#10600,#10601,#10602,#10603,#10604,#10605),
 .UNSPECIFIED.,.F.,.F.,(4,3,3,3,3,3,3,3,3,3,3,3,3,3,3,3,3,3,3,3,3,3,3,3,
3,3,3,3,3,3,3,3,3,3,3,3,3,3,3,3,3,3,3,3,3,3,3,3,3,3,3,3,3,3,3,3,3,3,3,3,
3,3,3,4),(13.6805616528234,13.8163469424965,13.9521322321697,14.0576492724172,
14.1630076667916,14.2682424286898,14.3734114048201,14.4785506869449,14.5836963227474,
14.6889538380415,14.794274445328,14.8997763429847,14.9487131058961,15.0542300102651,
15.1595882677422,15.2648228919212,15.369991729905,15.4751308736699,15.5802763711125,
15.6855337490015,15.790854219229,15.8963559818009,15.9452939796226,16.0508108200795,
16.1561690120437,16.2614035686587,16.3665723378434,16.4717114116777,16.5768568381604,
16.6821141440126,16.7874345414828,16.8929362309438,16.941874853349,17.0473917665423,
17.1527500324105,17.2579846642936,17.3631535095492,17.4682926601413,17.5734381639534,
17.6786955474717,17.7840160229136,17.8895177900021,17.9384557270754,18.0439726204319,
18.1493308662541,18.2545654778812,18.3597343027628,18.4648734328942,18.5700189161903,
18.6752762792507,18.7805967342379,18.8860984810917,18.9350366008018,19.0405534775837,
19.1459117066389,19.251146301295,19.3563151090886,19.4614542220404,19.5665996880905,
19.6718570339202,19.7771774716605,19.8826792014212,19.9316174745282,19.9637469595683),
 .UNSPECIFIED.);
#858=B_SPLINE_CURVE_WITH_KNOTS('',3,(#10610,#10611,#10612,#10613,#10614,
#10615,#10616,#10617,#10618,#10619,#10620,#10621,#10622,#10623,#10624,#10625,
#10626,#10627,#10628,#10629,#10630,#10631,#10632,#10633,#10634,#10635,#10636,
#10637,#10638,#10639,#10640,#10641,#10642,#10643,#10644,#10645,#10646,#10647,
#10648,#10649,#10650,#10651,#10652,#10653,#10654,#10655,#10656,#10657,#10658,
#10659,#10660,#10661,#10662,#10663,#10664,#10665,#10666,#10667,#10668,#10669,
#10670,#10671,#10672,#10673,#10674,#10675,#10676,#10677,#10678,#10679,#10680,
#10681,#10682,#10683,#10684,#10685,#10686,#10687,#10688,#10689,#10690,#10691,
#10692,#10693,#10694,#10695,#10696,#10697,#10698,#10699,#10700,#10701,#10702,
#10703,#10704,#10705,#10706,#10707,#10708,#10709,#10710,#10711,#10712,#10713,
#10714,#10715,#10716,#10717,#10718,#10719,#10720,#10721,#10722,#10723,#10724,
#10725,#10726,#10727,#10728,#10729,#10730,#10731,#10732,#10733,#10734,#10735,
#10736,#10737,#10738,#10739,#10740,#10741,#10742,#10743,#10744,#10745,#10746,
#10747,#10748,#10749,#10750,#10751,#10752,#10753,#10754,#10755,#10756,#10757,
#10758,#10759,#10760,#10761,#10762,#10763,#10764,#10765,#10766,#10767,#10768,
#10769,#10770,#10771,#10772,#10773,#10774,#10775,#10776,#10777,#10778,#10779,
#10780,#10781,#10782,#10783,#10784,#10785,#10786,#10787,#10788,#10789,#10790,
#10791,#10792,#10793,#10794,#10795,#10796,#10797,#10798,#10799),
 .UNSPECIFIED.,.F.,.F.,(4,3,3,3,3,3,3,3,3,3,3,3,3,3,3,3,3,3,3,3,3,3,3,3,
3,3,3,3,3,3,3,3,3,3,3,3,3,3,3,3,3,3,3,3,3,3,3,3,3,3,3,3,3,3,3,3,3,3,3,3,
3,3,3,4),(-29.2252829771426,-29.1019668884045,-28.9772671757156,-28.9008453380659,
-28.7953311638248,-28.6899756819201,-28.584743886893,-28.4795779096737,
-28.3744416539223,-28.2692990674095,-28.1640446152455,-28.0587270834556,
-27.9532282482017,-27.9042644643395,-27.7987466448287,-27.6933874635457,
-27.5881519073483,-27.4829821328056,-27.3778420493868,-27.2726956106372,
-27.1674372954177,-27.0621158887715,-26.956613201017,-26.9076835906131,
-26.8021664914534,-26.696808033114,-26.5915732000532,-26.486404148325,-26.3812647862724,
-26.2761190663133,-26.1708614610085,-26.0655407602333,-25.9600387646782,
-25.9111027168866,-25.8055861967743,-25.7002283306547,-25.5949941064194,
-25.4898256734777,-25.3846869392368,-25.2795418551892,-25.1742848937338,
-25.0689648422825,-24.9634634977247,-24.9145218431602,-24.8090048011679,
-24.7036464050276,-24.5984116413407,-24.4932426634084,-24.3881033794713,
-24.2829577418491,-24.1777002247361,-24.0723796156286,-23.9668777161668,
-23.9179409694338,-23.8127945908852,-23.7039574758217,-23.5990948008806,
-23.494295154551,-23.3895219001086,-23.2847384419457,-23.1798422596674,
-23.0748784618845,-22.9697413145944,-22.9420976703771),.UNSPECIFIED.);
#859=B_SPLINE_CURVE_WITH_KNOTS('',3,(#10800,#10801,#10802,#10803,#10804,
#10805,#10806,#10807,#10808,#10809),.UNSPECIFIED.,.F.,.F.,(4,1,1,1,1,1,
1,4),(19.9637512898265,20.9281983482546,21.924779221981,22.9213600957074,
23.9179409694338,24.9145218431602,25.9111027168866,26.2469251046285),
 .UNSPECIFIED.);
#860=B_SPLINE_CURVE_WITH_KNOTS('',3,(#10814,#10815,#10816,#10817,#10818,
#10819,#10820,#10821,#10822,#10823,#10824,#10825,#10826,#10827,#10828,#10829,
#10830,#10831,#10832,#10833,#10834,#10835,#10836,#10837,#10838,#10839,#10840,
#10841,#10842,#10843,#10844,#10845,#10846,#10847,#10848,#10849,#10850,#10851,
#10852,#10853,#10854,#10855,#10856,#10857,#10858,#10859,#10860,#10861,#10862,
#10863,#10864,#10865,#10866,#10867,#10868,#10869,#10870,#10871,#10872,#10873,
#10874,#10875,#10876,#10877,#10878,#10879,#10880,#10881,#10882,#10883,#10884,
#10885,#10886,#10887,#10888,#10889,#10890,#10891,#10892,#10893,#10894,#10895,
#10896,#10897,#10898,#10899,#10900,#10901,#10902,#10903,#10904,#10905,#10906,
#10907,#10908,#10909,#10910,#10911,#10912,#10913,#10914,#10915,#10916,#10917,
#10918,#10919,#10920,#10921,#10922,#10923,#10924,#10925,#10926,#10927,#10928,
#10929,#10930,#10931,#10932,#10933,#10934,#10935,#10936,#10937,#10938,#10939,
#10940,#10941,#10942,#10943,#10944,#10945,#10946,#10947,#10948,#10949,#10950,
#10951,#10952,#10953,#10954,#10955,#10956,#10957,#10958,#10959,#10960,#10961,
#10962,#10963,#10964,#10965,#10966,#10967,#10968,#10969,#10970,#10971,#10972,
#10973,#10974,#10975,#10976,#10977,#10978,#10979,#10980,#10981,#10982,#10983,
#10984,#10985,#10986,#10987,#10988,#10989,#10990,#10991,#10992,#10993,#10994,
#10995,#10996,#10997,#10998,#10999,#11000,#11001,#11002,#11003),
 .UNSPECIFIED.,.F.,.F.,(4,3,3,3,3,3,3,3,3,3,3,3,3,3,3,3,3,3,3,3,3,3,3,3,
3,3,3,3,3,3,3,3,3,3,3,3,3,3,3,3,3,3,3,3,3,3,3,3,3,3,3,3,3,3,3,3,3,3,3,3,
3,3,3,4),(-35.5084682847362,-35.4023595064501,-35.2962353664596,-35.1899767723764,
-35.0836517048972,-34.9771072128199,-34.8803305804243,-34.7749501203421,
-34.6697303251661,-34.5646364761803,-34.4596097707505,-34.3546139040871,
-34.2496126168137,-34.1444998826443,-34.0393245183888,-33.9339670573156,
-33.8837497066979,-33.7782042662089,-33.6728173464077,-33.5675540178139,
-33.4623564669826,-33.3571886468187,-33.2520145543263,-33.1467289026185,
-33.0413803014021,-32.9358509241569,-32.8871688329715,-32.7816310902557,
-32.6762515117445,-32.5709949564141,-32.4658038211253,-32.3606420477126,
-32.2554736217241,-32.1501930189172,-32.0448491206365,-31.9393238610625,
-31.8905879592451,-31.7850905501633,-31.6797520943827,-31.5745376278472,
-31.4693891567628,-31.3642705581269,-31.2591457532205,-31.1539091496212,
-31.048609530701,-30.9431285201143,-30.8940070855187,-30.7884848231672,
-30.6831211656921,-30.5778811063684,-30.472706814698,-30.3675622071504,
-30.2624112442604,-30.1571484360913,-30.0518225478093,-29.9463154429612,
-29.8974262117923,-29.792124966494,-29.6869771514363,-29.58194618625,-29.4769877321303,
-29.3720711679708,-29.2671322858916,-29.2252829775567),.UNSPECIFIED.);
#861=B_SPLINE_CURVE_WITH_KNOTS('',3,(#11004,#11005,#11006,#11007,#11008,
#11009,#11010,#11011,#11012,#11013,#11014,#11015,#11016,#11017,#11018,#11019,
#11020,#11021,#11022,#11023,#11024,#11025,#11026,#11027,#11028,#11029,#11030,
#11031,#11032,#11033,#11034,#11035,#11036,#11037,#11038,#11039,#11040,#11041,
#11042,#11043,#11044,#11045,#11046,#11047,#11048,#11049,#11050,#11051,#11052,
#11053,#11054,#11055,#11056,#11057,#11058,#11059,#11060,#11061,#11062,#11063,
#11064,#11065,#11066,#11067,#11068,#11069,#11070,#11071,#11072,#11073,#11074,
#11075,#11076,#11077,#11078,#11079,#11080,#11081,#11082,#11083,#11084,#11085,
#11086,#11087,#11088,#11089,#11090,#11091,#11092,#11093,#11094,#11095,#11096,
#11097,#11098,#11099,#11100,#11101,#11102,#11103,#11104,#11105,#11106,#11107,
#11108,#11109,#11110,#11111,#11112,#11113,#11114,#11115,#11116,#11117,#11118,
#11119,#11120,#11121,#11122,#11123,#11124,#11125,#11126,#11127,#11128,#11129,
#11130,#11131,#11132,#11133,#11134,#11135,#11136,#11137,#11138,#11139,#11140,
#11141,#11142,#11143,#11144,#11145,#11146,#11147,#11148,#11149,#11150,#11151,
#11152,#11153,#11154,#11155,#11156,#11157,#11158,#11159,#11160,#11161,#11162,
#11163,#11164,#11165,#11166,#11167,#11168,#11169,#11170,#11171,#11172,#11173,
#11174,#11175,#11176,#11177,#11178,#11179,#11180,#11181,#11182,#11183,#11184,
#11185,#11186,#11187,#11188,#11189,#11190,#11191,#11192,#11193),
 .UNSPECIFIED.,.F.,.F.,(4,3,3,3,3,3,3,3,3,3,3,3,3,3,3,3,3,3,3,3,3,3,3,3,
3,3,3,3,3,3,3,3,3,3,3,3,3,3,3,3,3,3,3,3,3,3,3,3,3,3,3,3,3,3,3,3,3,3,3,3,
3,3,3,4),(26.2469322667479,26.3520739127528,26.4572007025229,26.5623485411171,
26.6676237508216,26.7729747238682,26.8785103872484,26.9076835906131,27.0132014116089,
27.118560591826,27.2237961432062,27.3289659106069,27.4341059845772,27.5392524115874,
27.6445107116996,27.7498321012928,27.8553347691868,27.9042644643395,28.0097784777039,
28.1151338402059,28.2203655774865,28.3255315352489,28.4306678097396,28.5358104531349,
28.6410650192122,28.7463826976556,28.8518817282743,28.9008453380659,29.0063647936612,
29.1117255831178,29.2169626990725,29.3221340024981,29.4272755818894,29.5324234816313,
29.6376831956907,29.7430059677339,29.8485099556615,29.8974262117923,30.0029483903628,
30.108311972099,30.2135519678941,30.3187262036494,30.4238707629554,30.5290216853458,
30.6342844649438,30.7396103314271,30.8451174250958,30.8940070855187,30.9995034308466,
31.1048410912431,31.2100551614913,31.3152034841296,31.4203221815889,31.5254473322794,
31.6306846511212,31.7359851973193,31.8414674509992,31.8905879592451,31.9966053193322,
32.1024616306615,32.209375616478,32.3150131087613,32.4225653413444,32.5301175739275),
 .UNSPECIFIED.);
#862=B_SPLINE_CURVE_WITH_KNOTS('',3,(#11196,#11197,#11198,#11199,#11200,
#11201,#11202,#11203,#11204,#11205,#11206,#11207,#11208,#11209,#11210,#11211,
#11212,#11213,#11214,#11215,#11216,#11217,#11218,#11219,#11220,#11221,#11222,
#11223,#11224,#11225,#11226,#11227,#11228,#11229,#11230,#11231,#11232,#11233,
#11234,#11235,#11236,#11237,#11238,#11239,#11240,#11241,#11242,#11243,#11244,
#11245,#11246,#11247,#11248,#11249,#11250,#11251,#11252,#11253,#11254,#11255,
#11256,#11257,#11258,#11259,#11260,#11261,#11262,#11263,#11264,#11265,#11266,
#11267,#11268,#11269,#11270,#11271,#11272,#11273,#11274,#11275,#11276,#11277,
#11278,#11279,#11280,#11281,#11282,#11283,#11284,#11285,#11286,#11287,#11288,
#11289,#11290,#11291,#11292,#11293,#11294,#11295,#11296,#11297,#11298,#11299,
#11300,#11301,#11302,#11303,#11304,#11305,#11306,#11307,#11308,#11309,#11310,
#11311,#11312,#11313,#11314,#11315,#11316,#11317,#11318,#11319,#11320,#11321,
#11322),.UNSPECIFIED.,.F.,.F.,(4,3,3,3,3,3,3,3,3,3,3,3,3,3,3,3,3,3,3,3,
3,3,3,3,3,3,3,3,3,3,3,3,3,3,3,3,3,3,3,3,3,3,4),(32.5301175743904,32.6499243852402,
32.7707627025493,32.8871688329715,32.9927129802535,33.0980988488266,33.2033614876022,
33.3085585732965,33.4137261529852,33.5189002298822,33.6241862045267,33.7295353225628,
33.835065508577,33.8837497066979,33.9891233821121,34.0943380597534,34.1994292723218,
34.3044548813995,34.4094511884809,34.5144544512916,34.6195714611784,34.7247524196896,
34.8301174455498,34.8803305804243,34.9860472709756,35.0916046934768,35.1970366054675,
35.3024014441108,35.4077350088512,35.5130730534988,35.6185188580415,35.724025664367,
35.8297086352625,35.8769114541507,35.9814256971422,36.085764885428,36.1900065327749,
36.2941881420584,36.3983471341029,36.502590073869,36.6068728780942,36.7113371001606,
36.8011443739907),.UNSPECIFIED.);
#863=B_SPLINE_CURVE_WITH_KNOTS('',3,(#11325,#11326,#11327,#11328,#11329,
#11330,#11331),.UNSPECIFIED.,.F.,.F.,(4,1,1,1,4),(-38.86665407533,-37.8700732016036,
-36.8734923278771,-35.8769114541507,-35.5084758780373),.UNSPECIFIED.);
#864=B_SPLINE_CURVE_WITH_KNOTS('',3,(#11334,#11335,#11336,#11337,#11338,
#11339,#11340,#11341,#11342,#11343,#11344,#11345,#11346,#11347,#11348,#11349,
#11350,#11351,#11352,#11353,#11354,#11355,#11356,#11357,#11358,#11359,#11360,
#11361,#11362,#11363,#11364,#11365,#11366,#11367,#11368,#11369,#11370),
 .UNSPECIFIED.,.F.,.F.,(4,3,3,3,3,3,3,3,3,3,3,3,4),(47.1238898038469,47.2495729833432,
47.3762357179408,47.4923329732614,47.6078590787388,47.7183089200037,47.8286551120703,
47.9389421371105,48.0492143835049,48.1595854549815,48.2700151013785,48.3806268044217,
48.4165418170808),.UNSPECIFIED.);
#865=B_SPLINE_CURVE_WITH_KNOTS('',3,(#11373,#11374,#11375,#11376,#11377,
#11378),.UNSPECIFIED.,.F.,.F.,(4,2,4),(9.70317678907225E-6,0.00416850045813341,
0.00832730327467254),.UNSPECIFIED.);
#866=B_SPLINE_CURVE_WITH_KNOTS('',3,(#11547,#11548,#11549,#11550,#11551,
#11552,#11553,#11554,#11555,#11556,#11557,#11558,#11559,#11560,#11561,#11562,
#11563,#11564,#11565,#11566,#11567,#11568,#11569,#11570,#11571,#11572,#11573,
#11574,#11575,#11576,#11577,#11578,#11579,#11580,#11581,#11582,#11583,#11584,
#11585,#11586,#11587,#11588,#11589,#11590,#11591,#11592,#11593,#11594,#11595,
#11596,#11597,#11598,#11599,#11600,#11601,#11602,#11603,#11604,#11605,#11606,
#11607,#11608,#11609,#11610,#11611,#11612,#11613,#11614,#11615,#11616,#11617,
#11618,#11619,#11620,#11621,#11622,#11623,#11624,#11625,#11626,#11627,#11628,
#11629,#11630,#11631,#11632,#11633,#11634),.UNSPECIFIED.,.F.,.F.,(4,3,3,
3,3,3,3,3,3,3,3,3,3,3,3,3,3,3,3,3,3,3,3,3,3,3,3,3,3,4),(0.,0.0141071418350746,
0.0355442789019995,0.0572656760904613,0.06697208668337,0.0731473068625853,
0.0768712321996411,0.0979621356483863,0.118760026435482,0.139128689171148,
0.144047130561891,0.148652874160775,0.168817015624542,0.188376963144646,
0.19974270647635,0.210158636009444,0.214504663212601,0.217541294027054,
0.237154834633298,0.25693437910066,0.270710750298301,0.279046676838732,
0.283673142787779,0.30272570932202,0.318739227454765,0.32422732905593,0.328196248012664,
0.346653672874964,0.365111097737263,0.366397579005847),.UNSPECIFIED.);
#867=B_SPLINE_CURVE_WITH_KNOTS('',3,(#11635,#11636,#11637,#11638,#11639,
#11640,#11641,#11642,#11643,#11644,#11645,#11646,#11647,#11648,#11649,#11650,
#11651,#11652,#11653,#11654,#11655,#11656,#11657,#11658,#11659,#11660,#11661,
#11662,#11663,#11664,#11665,#11666,#11667,#11668,#11669,#11670,#11671,#11672,
#11673,#11674,#11675,#11676,#11677,#11678,#11679,#11680,#11681,#11682,#11683,
#11684,#11685,#11686,#11687,#11688,#11689,#11690,#11691,#11692,#11693,#11694,
#11695,#11696,#11697,#11698,#11699,#11700,#11701,#11702,#11703,#11704,#11705,
#11706,#11707,#11708,#11709,#11710,#11711,#11712,#11713,#11714,#11715,#11716,
#11717,#11718,#11719,#11720,#11721,#11722),.UNSPECIFIED.,.F.,.F.,(4,3,3,
3,3,3,3,3,3,3,3,3,3,3,3,3,3,3,3,3,3,3,3,3,3,3,3,3,3,4),(0.,0.0113475426890351,
0.0291670472690302,0.0475729928382081,0.0560296921941146,0.0601609064744176,
0.0640260637775195,0.0829599659512082,0.102409502742518,0.121425659695721,
0.125492936123647,0.128447152834782,0.148489790009647,0.168489720572082,
0.178766369133891,0.190382802806189,0.193958991929988,0.213661586205272,
0.234044797116619,0.250281897850443,0.259921705842752,0.263839735831979,
0.267527540815499,0.288775631126542,0.307651155122482,0.313183531167478,
0.32004907337882,0.341698300745877,0.360810180211172,0.364629307890663),
 .UNSPECIFIED.);
#868=B_SPLINE_CURVE_WITH_KNOTS('',3,(#11891,#11892,#11893,#11894,#11895,
#11896,#11897,#11898,#11899,#11900,#11901,#11902,#11903,#11904,#11905,#11906,
#11907,#11908,#11909,#11910,#11911,#11912,#11913,#11914,#11915,#11916,#11917,
#11918,#11919,#11920,#11921,#11922,#11923,#11924,#11925,#11926,#11927,#11928,
#11929,#11930,#11931,#11932,#11933,#11934,#11935,#11936,#11937,#11938,#11939,
#11940,#11941,#11942,#11943,#11944,#11945,#11946,#11947,#11948,#11949,#11950,
#11951,#11952,#11953,#11954,#11955,#11956,#11957,#11958,#11959,#11960,#11961,
#11962,#11963,#11964,#11965,#11966,#11967,#11968,#11969,#11970,#11971,#11972,
#11973,#11974,#11975,#11976,#11977,#11978),.UNSPECIFIED.,.F.,.F.,(4,3,3,
3,3,3,3,3,3,3,3,3,3,3,3,3,3,3,3,3,3,3,3,3,3,3,3,3,3,4),(0.,0.0113475426890348,
0.0291670043807534,0.0475729266099651,0.0560296567510807,0.0601608189473537,
0.0640260370044265,0.0829599116369005,0.102409445900677,0.121425612301813,
0.125492777386276,0.128446963922241,0.148489595599423,0.168489527822768,
0.178766369133891,0.19038280280619,0.193958992762406,0.213737700534491,
0.233952427821611,0.254598689423448,0.25992170946175,0.263839753817461,
0.267527548191952,0.288775627561601,0.307651148863046,0.313183536175324,
0.317664301192065,0.339328429314369,0.360810221497805,0.364629307890676),
 .UNSPECIFIED.);
#869=B_SPLINE_CURVE_WITH_KNOTS('',3,(#11979,#11980,#11981,#11982,#11983,
#11984,#11985,#11986,#11987,#11988,#11989,#11990,#11991,#11992,#11993,#11994,
#11995,#11996,#11997,#11998,#11999,#12000,#12001,#12002,#12003,#12004,#12005,
#12006,#12007,#12008,#12009,#12010,#12011,#12012,#12013,#12014,#12015,#12016,
#12017,#12018,#12019,#12020,#12021,#12022,#12023,#12024,#12025,#12026,#12027,
#12028,#12029,#12030,#12031,#12032,#12033,#12034,#12035,#12036,#12037,#12038,
#12039,#12040,#12041,#12042,#12043,#12044,#12045,#12046,#12047,#12048,#12049,
#12050,#12051,#12052,#12053,#12054,#12055,#12056,#12057,#12058,#12059,#12060,
#12061,#12062,#12063,#12064,#12065,#12066),.UNSPECIFIED.,.F.,.F.,(4,3,3,
3,3,3,3,3,3,3,3,3,3,3,3,3,3,3,3,3,3,3,3,3,3,3,3,3,3,4),(0.,0.0141071418350769,
0.0355442756622905,0.0572656706841107,0.0669721763873351,0.0731472545815266,
0.0768712310065397,0.097962134032381,0.118760002271128,0.139128677510718,
0.144047115685023,0.148652871054896,0.168816990652203,0.188376892480646,
0.199742706476349,0.210158636009442,0.214504668206205,0.217541304167668,
0.237154819513473,0.256934375573258,0.270710752081222,0.2790466832613,0.284344214540952,
0.303389571149022,0.318739247434016,0.324227244433163,0.328196234496932,
0.346653692953416,0.3651111514099,0.366397579005838),.UNSPECIFIED.);
#1065=VERTEX_POINT('',#8077);
#1066=VERTEX_POINT('',#8078);
#1067=VERTEX_POINT('',#8080);
#1068=VERTEX_POINT('',#8229);
#1069=VERTEX_POINT('',#8344);
#1070=VERTEX_POINT('',#8345);
#1071=VERTEX_POINT('',#8368);
#1072=VERTEX_POINT('',#8369);
#1073=VERTEX_POINT('',#8682);
#1074=VERTEX_POINT('',#8683);
#1075=VERTEX_POINT('',#8998);
#1076=VERTEX_POINT('',#8999);
#1077=VERTEX_POINT('',#9346);
#1078=VERTEX_POINT('',#9347);
#1079=VERTEX_POINT('',#9532);
#1080=VERTEX_POINT('',#9533);
#1081=VERTEX_POINT('',#9535);
#1082=VERTEX_POINT('',#9597);
#1083=VERTEX_POINT('',#9634);
#1084=VERTEX_POINT('',#9635);
#1085=VERTEX_POINT('',#10018);
#1086=VERTEX_POINT('',#10019);
#1087=VERTEX_POINT('',#10402);
#1088=VERTEX_POINT('',#10403);
#1089=VERTEX_POINT('',#10607);
#1090=VERTEX_POINT('',#10608);
#1091=VERTEX_POINT('',#10811);
#1092=VERTEX_POINT('',#10812);
#1093=VERTEX_POINT('',#11195);
#1094=VERTEX_POINT('',#11323);
#1095=VERTEX_POINT('',#11333);
#1096=VERTEX_POINT('',#11371);
#1097=VERTEX_POINT('',#12068);
#1098=VERTEX_POINT('',#12069);
#1099=VERTEX_POINT('',#12071);
#1100=VERTEX_POINT('',#12073);
#1101=VERTEX_POINT('',#12075);
#1102=VERTEX_POINT('',#12077);
#1103=VERTEX_POINT('',#12081);
#1104=VERTEX_POINT('',#12083);
#1105=VERTEX_POINT('',#12087);
#1106=VERTEX_POINT('',#12091);
#1107=VERTEX_POINT('',#12095);
#1108=VERTEX_POINT('',#12099);
#1405=EDGE_CURVE('',#1065,#1066,#626,.T.);
#1406=EDGE_CURVE('',#1067,#1065,#838,.T.);
#1407=EDGE_CURVE('',#1068,#1067,#241,.T.);
#1408=EDGE_CURVE('',#1068,#1066,#839,.T.);
#1409=EDGE_CURVE('',#1069,#1070,#627,.T.);
#1410=EDGE_CURVE('',#1065,#1069,#840,.T.);
#1411=EDGE_CURVE('',#1066,#1070,#841,.T.);
#1412=EDGE_CURVE('',#1071,#1072,#628,.T.);
#1413=EDGE_CURVE('',#1069,#1071,#842,.T.);
#1414=EDGE_CURVE('',#1070,#1072,#843,.T.);
#1415=EDGE_CURVE('',#1073,#1074,#629,.T.);
#1416=EDGE_CURVE('',#1071,#1073,#844,.T.);
#1417=EDGE_CURVE('',#1072,#1074,#845,.T.);
#1418=EDGE_CURVE('',#1075,#1076,#630,.T.);
#1419=EDGE_CURVE('',#1073,#1075,#846,.T.);
#1420=EDGE_CURVE('',#1074,#1076,#847,.T.);
#1421=EDGE_CURVE('',#1077,#1078,#631,.T.);
#1422=EDGE_CURVE('',#1075,#1077,#848,.T.);
#1423=EDGE_CURVE('',#1076,#1078,#849,.T.);
#1424=EDGE_CURVE('',#1079,#1080,#632,.T.);
#1425=EDGE_CURVE('',#1079,#1081,#850,.T.);
#1426=EDGE_CURVE('',#1081,#1082,#242,.F.);
#1427=EDGE_CURVE('',#1082,#1080,#851,.T.);
#1428=EDGE_CURVE('',#1083,#1084,#633,.T.);
#1429=EDGE_CURVE('',#1083,#1079,#852,.T.);
#1430=EDGE_CURVE('',#1080,#1084,#853,.T.);
#1431=EDGE_CURVE('',#1085,#1086,#634,.T.);
#1432=EDGE_CURVE('',#1085,#1083,#854,.T.);
#1433=EDGE_CURVE('',#1084,#1086,#855,.T.);
#1434=EDGE_CURVE('',#1087,#1088,#635,.T.);
#1435=EDGE_CURVE('',#1087,#1085,#856,.T.);
#1436=EDGE_CURVE('',#1086,#1088,#857,.T.);
#1437=EDGE_CURVE('',#1089,#1090,#636,.T.);
#1438=EDGE_CURVE('',#1089,#1087,#858,.T.);
#1439=EDGE_CURVE('',#1088,#1090,#859,.T.);
#1440=EDGE_CURVE('',#1091,#1092,#637,.T.);
#1441=EDGE_CURVE('',#1091,#1089,#860,.T.);
#1442=EDGE_CURVE('',#1090,#1092,#861,.T.);
#1443=EDGE_CURVE('',#1092,#1093,#862,.T.);
#1444=EDGE_CURVE('',#1094,#1093,#243,.F.);
#1445=EDGE_CURVE('',#1094,#1091,#863,.T.);
#1446=EDGE_CURVE('',#1078,#1095,#864,.T.);
#1447=EDGE_CURVE('',#1096,#1095,#244,.T.);
#1448=EDGE_CURVE('',#1077,#1096,#865,.T.);
#1449=EDGE_CURVE('',#1093,#1096,#866,.T.);
#1450=EDGE_CURVE('',#1067,#1082,#867,.T.);
#1451=EDGE_CURVE('',#1095,#1094,#868,.T.);
#1452=EDGE_CURVE('',#1081,#1068,#869,.T.);
#1453=EDGE_CURVE('',#1097,#1098,#638,.T.);
#1454=EDGE_CURVE('',#1098,#1099,#639,.T.);
#1455=EDGE_CURVE('',#1099,#1100,#640,.T.);
#1456=EDGE_CURVE('',#1100,#1101,#641,.T.);
#1457=EDGE_CURVE('',#1101,#1102,#642,.T.);
#1458=EDGE_CURVE('',#1102,#1097,#643,.T.);
#1459=EDGE_CURVE('',#1097,#1103,#644,.T.);
#1460=EDGE_CURVE('',#1103,#1104,#645,.T.);
#1461=EDGE_CURVE('',#1098,#1104,#646,.T.);
#1462=EDGE_CURVE('',#1102,#1105,#647,.T.);
#1463=EDGE_CURVE('',#1105,#1103,#648,.T.);
#1464=EDGE_CURVE('',#1101,#1106,#649,.T.);
#1465=EDGE_CURVE('',#1106,#1105,#650,.T.);
#1466=EDGE_CURVE('',#1100,#1107,#651,.T.);
#1467=EDGE_CURVE('',#1107,#1106,#652,.T.);
#1468=EDGE_CURVE('',#1099,#1108,#653,.T.);
#1469=EDGE_CURVE('',#1108,#1107,#654,.T.);
#1470=EDGE_CURVE('',#1104,#1108,#655,.T.);
#2063=ORIENTED_EDGE('',*,*,#1405,.F.);
#2064=ORIENTED_EDGE('',*,*,#1406,.F.);
#2065=ORIENTED_EDGE('',*,*,#1407,.F.);
#2066=ORIENTED_EDGE('',*,*,#1408,.T.);
#2067=ORIENTED_EDGE('',*,*,#1409,.F.);
#2068=ORIENTED_EDGE('',*,*,#1410,.F.);
#2069=ORIENTED_EDGE('',*,*,#1405,.T.);
#2070=ORIENTED_EDGE('',*,*,#1411,.T.);
#2071=ORIENTED_EDGE('',*,*,#1412,.F.);
#2072=ORIENTED_EDGE('',*,*,#1413,.F.);
#2073=ORIENTED_EDGE('',*,*,#1409,.T.);
#2074=ORIENTED_EDGE('',*,*,#1414,.T.);
#2075=ORIENTED_EDGE('',*,*,#1415,.F.);
#2076=ORIENTED_EDGE('',*,*,#1416,.F.);
#2077=ORIENTED_EDGE('',*,*,#1412,.T.);
#2078=ORIENTED_EDGE('',*,*,#1417,.T.);
#2079=ORIENTED_EDGE('',*,*,#1418,.F.);
#2080=ORIENTED_EDGE('',*,*,#1419,.F.);
#2081=ORIENTED_EDGE('',*,*,#1415,.T.);
#2082=ORIENTED_EDGE('',*,*,#1420,.T.);
#2083=ORIENTED_EDGE('',*,*,#1421,.F.);
#2084=ORIENTED_EDGE('',*,*,#1422,.F.);
#2085=ORIENTED_EDGE('',*,*,#1418,.T.);
#2086=ORIENTED_EDGE('',*,*,#1423,.T.);
#2087=ORIENTED_EDGE('',*,*,#1424,.F.);
#2088=ORIENTED_EDGE('',*,*,#1425,.T.);
#2089=ORIENTED_EDGE('',*,*,#1426,.T.);
#2090=ORIENTED_EDGE('',*,*,#1427,.T.);
#2091=ORIENTED_EDGE('',*,*,#1428,.F.);
#2092=ORIENTED_EDGE('',*,*,#1429,.T.);
#2093=ORIENTED_EDGE('',*,*,#1424,.T.);
#2094=ORIENTED_EDGE('',*,*,#1430,.T.);
#2095=ORIENTED_EDGE('',*,*,#1431,.F.);
#2096=ORIENTED_EDGE('',*,*,#1432,.T.);
#2097=ORIENTED_EDGE('',*,*,#1428,.T.);
#2098=ORIENTED_EDGE('',*,*,#1433,.T.);
#2099=ORIENTED_EDGE('',*,*,#1434,.F.);
#2100=ORIENTED_EDGE('',*,*,#1435,.T.);
#2101=ORIENTED_EDGE('',*,*,#1431,.T.);
#2102=ORIENTED_EDGE('',*,*,#1436,.T.);
#2103=ORIENTED_EDGE('',*,*,#1437,.F.);
#2104=ORIENTED_EDGE('',*,*,#1438,.T.);
#2105=ORIENTED_EDGE('',*,*,#1434,.T.);
#2106=ORIENTED_EDGE('',*,*,#1439,.T.);
#2107=ORIENTED_EDGE('',*,*,#1440,.F.);
#2108=ORIENTED_EDGE('',*,*,#1441,.T.);
#2109=ORIENTED_EDGE('',*,*,#1437,.T.);
#2110=ORIENTED_EDGE('',*,*,#1442,.T.);
#2111=ORIENTED_EDGE('',*,*,#1440,.T.);
#2112=ORIENTED_EDGE('',*,*,#1443,.T.);
#2113=ORIENTED_EDGE('',*,*,#1444,.F.);
#2114=ORIENTED_EDGE('',*,*,#1445,.T.);
#2115=ORIENTED_EDGE('',*,*,#1421,.T.);
#2116=ORIENTED_EDGE('',*,*,#1446,.T.);
#2117=ORIENTED_EDGE('',*,*,#1447,.F.);
#2118=ORIENTED_EDGE('',*,*,#1448,.F.);
#2119=ORIENTED_EDGE('',*,*,#1449,.F.);
#2120=ORIENTED_EDGE('',*,*,#1443,.F.);
#2121=ORIENTED_EDGE('',*,*,#1442,.F.);
#2122=ORIENTED_EDGE('',*,*,#1439,.F.);
#2123=ORIENTED_EDGE('',*,*,#1436,.F.);
#2124=ORIENTED_EDGE('',*,*,#1433,.F.);
#2125=ORIENTED_EDGE('',*,*,#1430,.F.);
#2126=ORIENTED_EDGE('',*,*,#1427,.F.);
#2127=ORIENTED_EDGE('',*,*,#1450,.F.);
#2128=ORIENTED_EDGE('',*,*,#1406,.T.);
#2129=ORIENTED_EDGE('',*,*,#1410,.T.);
#2130=ORIENTED_EDGE('',*,*,#1413,.T.);
#2131=ORIENTED_EDGE('',*,*,#1416,.T.);
#2132=ORIENTED_EDGE('',*,*,#1419,.T.);
#2133=ORIENTED_EDGE('',*,*,#1422,.T.);
#2134=ORIENTED_EDGE('',*,*,#1448,.T.);
#2135=ORIENTED_EDGE('',*,*,#1451,.F.);
#2136=ORIENTED_EDGE('',*,*,#1446,.F.);
#2137=ORIENTED_EDGE('',*,*,#1423,.F.);
#2138=ORIENTED_EDGE('',*,*,#1420,.F.);
#2139=ORIENTED_EDGE('',*,*,#1417,.F.);
#2140=ORIENTED_EDGE('',*,*,#1414,.F.);
#2141=ORIENTED_EDGE('',*,*,#1411,.F.);
#2142=ORIENTED_EDGE('',*,*,#1408,.F.);
#2143=ORIENTED_EDGE('',*,*,#1452,.F.);
#2144=ORIENTED_EDGE('',*,*,#1425,.F.);
#2145=ORIENTED_EDGE('',*,*,#1429,.F.);
#2146=ORIENTED_EDGE('',*,*,#1432,.F.);
#2147=ORIENTED_EDGE('',*,*,#1435,.F.);
#2148=ORIENTED_EDGE('',*,*,#1438,.F.);
#2149=ORIENTED_EDGE('',*,*,#1441,.F.);
#2150=ORIENTED_EDGE('',*,*,#1445,.F.);
#2151=ORIENTED_EDGE('',*,*,#1449,.T.);
#2152=ORIENTED_EDGE('',*,*,#1447,.T.);
#2153=ORIENTED_EDGE('',*,*,#1451,.T.);
#2154=ORIENTED_EDGE('',*,*,#1444,.T.);
#2155=ORIENTED_EDGE('',*,*,#1453,.T.);
#2156=ORIENTED_EDGE('',*,*,#1454,.T.);
#2157=ORIENTED_EDGE('',*,*,#1455,.T.);
#2158=ORIENTED_EDGE('',*,*,#1456,.T.);
#2159=ORIENTED_EDGE('',*,*,#1457,.T.);
#2160=ORIENTED_EDGE('',*,*,#1458,.T.);
#2161=ORIENTED_EDGE('',*,*,#1453,.F.);
#2162=ORIENTED_EDGE('',*,*,#1459,.T.);
#2163=ORIENTED_EDGE('',*,*,#1460,.T.);
#2164=ORIENTED_EDGE('',*,*,#1461,.F.);
#2165=ORIENTED_EDGE('',*,*,#1458,.F.);
#2166=ORIENTED_EDGE('',*,*,#1462,.T.);
#2167=ORIENTED_EDGE('',*,*,#1463,.T.);
#2168=ORIENTED_EDGE('',*,*,#1459,.F.);
#2169=ORIENTED_EDGE('',*,*,#1457,.F.);
#2170=ORIENTED_EDGE('',*,*,#1464,.T.);
#2171=ORIENTED_EDGE('',*,*,#1465,.T.);
#2172=ORIENTED_EDGE('',*,*,#1462,.F.);
#2173=ORIENTED_EDGE('',*,*,#1456,.F.);
#2174=ORIENTED_EDGE('',*,*,#1466,.T.);
#2175=ORIENTED_EDGE('',*,*,#1467,.T.);
#2176=ORIENTED_EDGE('',*,*,#1464,.F.);
#2177=ORIENTED_EDGE('',*,*,#1455,.F.);
#2178=ORIENTED_EDGE('',*,*,#1468,.T.);
#2179=ORIENTED_EDGE('',*,*,#1469,.T.);
#2180=ORIENTED_EDGE('',*,*,#1466,.F.);
#2181=ORIENTED_EDGE('',*,*,#1454,.F.);
#2182=ORIENTED_EDGE('',*,*,#1461,.T.);
#2183=ORIENTED_EDGE('',*,*,#1470,.T.);
#2184=ORIENTED_EDGE('',*,*,#1468,.F.);
#2185=ORIENTED_EDGE('',*,*,#1470,.F.);
#2186=ORIENTED_EDGE('',*,*,#1460,.F.);
#2187=ORIENTED_EDGE('',*,*,#1463,.F.);
#2188=ORIENTED_EDGE('',*,*,#1465,.F.);
#2189=ORIENTED_EDGE('',*,*,#1467,.F.);
#2190=ORIENTED_EDGE('',*,*,#1469,.F.);
#2191=ORIENTED_EDGE('',*,*,#1450,.T.);
#2192=ORIENTED_EDGE('',*,*,#1426,.F.);
#2193=ORIENTED_EDGE('',*,*,#1452,.T.);
#2194=ORIENTED_EDGE('',*,*,#1407,.T.);
#2260=CYLINDRICAL_SURFACE('',#2696,1.5555);
#2261=CYLINDRICAL_SURFACE('',#2698,1.5555);
#2262=CYLINDRICAL_SURFACE('',#2699,1.5555);
#2263=CYLINDRICAL_SURFACE('',#2700,1.5555);
#2264=CYLINDRICAL_SURFACE('',#2701,1.5555);
#2265=CYLINDRICAL_SURFACE('',#2702,1.5555);
#2266=CYLINDRICAL_SURFACE('',#2703,1.954);
#2267=CYLINDRICAL_SURFACE('',#2705,1.954);
#2268=CYLINDRICAL_SURFACE('',#2706,1.954);
#2269=CYLINDRICAL_SURFACE('',#2707,1.954);
#2270=CYLINDRICAL_SURFACE('',#2708,1.954);
#2271=CYLINDRICAL_SURFACE('',#2709,1.954);
#2272=CYLINDRICAL_SURFACE('',#2710,1.954);
#2273=CYLINDRICAL_SURFACE('',#2712,1.5555);
#2381=ADVANCED_FACE('',(#352),#2260,.T.);
#2382=ADVANCED_FACE('',(#353),#2261,.T.);
#2383=ADVANCED_FACE('',(#354),#2262,.T.);
#2384=ADVANCED_FACE('',(#355),#2263,.T.);
#2385=ADVANCED_FACE('',(#356),#2264,.T.);
#2386=ADVANCED_FACE('',(#357),#2265,.T.);
#2387=ADVANCED_FACE('',(#358),#2266,.T.);
#2388=ADVANCED_FACE('',(#359),#2267,.T.);
#2389=ADVANCED_FACE('',(#360),#2268,.T.);
#2390=ADVANCED_FACE('',(#361),#2269,.T.);
#2391=ADVANCED_FACE('',(#362),#2270,.T.);
#2392=ADVANCED_FACE('',(#363),#2271,.T.);
#2393=ADVANCED_FACE('',(#364),#2272,.T.);
#2394=ADVANCED_FACE('',(#365),#2273,.T.);
#2395=ADVANCED_FACE('',(#366),#25,.F.);
#2396=ADVANCED_FACE('',(#367),#26,.F.);
#2397=ADVANCED_FACE('',(#368,#57),#88,.T.);
#2398=ADVANCED_FACE('',(#369),#89,.F.);
#2399=ADVANCED_FACE('',(#370),#90,.F.);
#2400=ADVANCED_FACE('',(#371),#91,.F.);
#2401=ADVANCED_FACE('',(#372),#92,.F.);
#2402=ADVANCED_FACE('',(#373),#93,.F.);
#2403=ADVANCED_FACE('',(#374),#94,.F.);
#2404=ADVANCED_FACE('',(#375),#95,.F.);
#2405=ADVANCED_FACE('',(#376),#96,.F.);
#2408=CLOSED_SHELL('',(#2381,#2382,#2383,#2384,#2385,#2386,#2387,#2388,
#2389,#2390,#2391,#2392,#2393,#2394,#2395,#2396,#2397,#2398,#2399,#2400,
#2401,#2402,#2403,#2404,#2405));
#2695=AXIS2_PLACEMENT_3D('',#8075,#3338,#3339);
#2696=AXIS2_PLACEMENT_3D('',#8076,#3340,#3341);
#2697=AXIS2_PLACEMENT_3D('',#8230,#3343,#3344);
#2698=AXIS2_PLACEMENT_3D('',#8343,#3345,#3346);
#2699=AXIS2_PLACEMENT_3D('',#8367,#3348,#3349);
#2700=AXIS2_PLACEMENT_3D('',#8681,#3351,#3352);
#2701=AXIS2_PLACEMENT_3D('',#8997,#3354,#3355);
#2702=AXIS2_PLACEMENT_3D('',#9345,#3357,#3358);
#2703=AXIS2_PLACEMENT_3D('',#9531,#3360,#3361);
#2704=AXIS2_PLACEMENT_3D('',#9598,#3363,#3364);
#2705=AXIS2_PLACEMENT_3D('',#9633,#3365,#3366);
#2706=AXIS2_PLACEMENT_3D('',#10017,#3368,#3369);
#2707=AXIS2_PLACEMENT_3D('',#10401,#3371,#3372);
#2708=AXIS2_PLACEMENT_3D('',#10606,#3374,#3375);
#2709=AXIS2_PLACEMENT_3D('',#10810,#3377,#3378);
#2710=AXIS2_PLACEMENT_3D('',#11194,#3380,#3381);
#2711=AXIS2_PLACEMENT_3D('',#11324,#3382,#3383);
#2712=AXIS2_PLACEMENT_3D('',#11332,#3384,#3385);
#2713=AXIS2_PLACEMENT_3D('',#11372,#3386,#3387);
#2714=AXIS2_PLACEMENT_3D('',#12067,#3388,#3389);
#2715=AXIS2_PLACEMENT_3D('',#12080,#3396,#3397);
#2716=AXIS2_PLACEMENT_3D('',#12086,#3401,#3402);
#2717=AXIS2_PLACEMENT_3D('',#12090,#3405,#3406);
#2718=AXIS2_PLACEMENT_3D('',#12094,#3409,#3410);
#2719=AXIS2_PLACEMENT_3D('',#12098,#3413,#3414);
#2720=AXIS2_PLACEMENT_3D('',#12102,#3417,#3418);
#2721=AXIS2_PLACEMENT_3D('',#12104,#3420,#3421);
#2722=AXIS2_PLACEMENT_3D('',#12105,#3422,#3423);
#3338=DIRECTION('axis',(0.,0.,1.));
#3339=DIRECTION('refdir',(1.,0.,0.));
#3340=DIRECTION('center_axis',(-2.22044604925031E-16,1.,0.));
#3341=DIRECTION('ref_axis',(-1.,-2.22044604925031E-16,4.63931189975154E-15));
#3342=DIRECTION('',(2.22044604925031E-16,-1.,0.));
#3343=DIRECTION('center_axis',(2.22044604925031E-16,-1.,0.));
#3344=DIRECTION('ref_axis',(-1.,-2.22044604925031E-16,4.63931189975154E-15));
#3345=DIRECTION('center_axis',(-2.22044604925031E-16,1.,0.));
#3346=DIRECTION('ref_axis',(-1.,-2.22044604925031E-16,4.63931189975154E-15));
#3347=DIRECTION('',(2.22044604925031E-16,-1.,0.));
#3348=DIRECTION('center_axis',(-2.22044604925031E-16,1.,0.));
#3349=DIRECTION('ref_axis',(-1.,-2.22044604925031E-16,4.63931189975154E-15));
#3350=DIRECTION('',(2.22044604925031E-16,-1.,0.));
#3351=DIRECTION('center_axis',(-2.22044604925031E-16,1.,0.));
#3352=DIRECTION('ref_axis',(-1.,-2.22044604925031E-16,4.63931189975154E-15));
#3353=DIRECTION('',(2.22044604925031E-16,-1.,0.));
#3354=DIRECTION('center_axis',(-2.22044604925031E-16,1.,0.));
#3355=DIRECTION('ref_axis',(-1.,-2.22044604925031E-16,4.63931189975154E-15));
#3356=DIRECTION('',(2.22044604925031E-16,-1.,0.));
#3357=DIRECTION('center_axis',(-2.22044604925031E-16,1.,0.));
#3358=DIRECTION('ref_axis',(-1.,-2.22044604925031E-16,4.63931189975154E-15));
#3359=DIRECTION('',(2.22044604925031E-16,-1.,0.));
#3360=DIRECTION('center_axis',(-2.22044604925031E-16,1.,0.));
#3361=DIRECTION('ref_axis',(-1.,-2.22044604925031E-16,0.));
#3362=DIRECTION('',(2.22044604925031E-16,-1.,0.));
#3363=DIRECTION('center_axis',(2.22044604925031E-16,-1.,0.));
#3364=DIRECTION('ref_axis',(-1.,-2.22044604925031E-16,0.));
#3365=DIRECTION('center_axis',(-2.22044604925031E-16,1.,0.));
#3366=DIRECTION('ref_axis',(-1.,-2.22044604925031E-16,0.));
#3367=DIRECTION('',(2.22044604925031E-16,-1.,0.));
#3368=DIRECTION('center_axis',(-2.22044604925031E-16,1.,0.));
#3369=DIRECTION('ref_axis',(-1.,-2.22044604925031E-16,0.));
#3370=DIRECTION('',(2.22044604925031E-16,-1.,0.));
#3371=DIRECTION('center_axis',(-2.22044604925031E-16,1.,0.));
#3372=DIRECTION('ref_axis',(-1.,-2.22044604925031E-16,0.));
#3373=DIRECTION('',(2.22044604925031E-16,-1.,0.));
#3374=DIRECTION('center_axis',(-2.22044604925031E-16,1.,0.));
#3375=DIRECTION('ref_axis',(-1.,-2.22044604925031E-16,0.));
#3376=DIRECTION('',(2.22044604925031E-16,-1.,0.));
#3377=DIRECTION('center_axis',(-2.22044604925031E-16,1.,0.));
#3378=DIRECTION('ref_axis',(-1.,-2.22044604925031E-16,0.));
#3379=DIRECTION('',(2.22044604925031E-16,-1.,0.));
#3380=DIRECTION('center_axis',(-2.22044604925031E-16,1.,0.));
#3381=DIRECTION('ref_axis',(-1.,-2.22044604925031E-16,0.));
#3382=DIRECTION('center_axis',(2.22044604925031E-16,-1.,0.));
#3383=DIRECTION('ref_axis',(-1.,-2.22044604925031E-16,0.));
#3384=DIRECTION('center_axis',(-2.22044604925031E-16,1.,0.));
#3385=DIRECTION('ref_axis',(-1.,-2.22044604925031E-16,4.63931189975154E-15));
#3386=DIRECTION('center_axis',(-2.22044604925031E-16,1.,0.));
#3387=DIRECTION('ref_axis',(-1.,-2.22044604925031E-16,4.63931189975154E-15));
#3388=DIRECTION('center_axis',(-2.22044604925031E-16,1.,0.));
#3389=DIRECTION('ref_axis',(-1.,-2.22044604925031E-16,0.));
#3390=DIRECTION('',(-0.5,-1.11022302462516E-16,0.866025403784439));
#3391=DIRECTION('',(-1.,-2.22044604925031E-16,0.));
#3392=DIRECTION('',(-0.499999999999999,-1.11022302462515E-16,-0.866025403784439));
#3393=DIRECTION('',(0.5,1.11022302462516E-16,-0.866025403784438));
#3394=DIRECTION('',(1.,2.22044604925031E-16,4.80740671595891E-16));
#3395=DIRECTION('',(0.499999999999999,1.11022302462515E-16,0.866025403784439));
#3396=DIRECTION('center_axis',(0.866025403784439,1.92296268638356E-16,0.5));
#3397=DIRECTION('ref_axis',(-0.5,-1.11022302462516E-16,0.866025403784439));
#3398=DIRECTION('',(2.22044604925031E-16,-1.,0.));
#3399=DIRECTION('',(-0.5,-1.11022302462516E-16,0.866025403784439));
#3400=DIRECTION('',(2.22044604925031E-16,-1.,0.));
#3401=DIRECTION('center_axis',(0.866025403784439,1.92296268638356E-16,-0.499999999999999));
#3402=DIRECTION('ref_axis',(0.499999999999999,1.11022302462515E-16,0.866025403784439));
#3403=DIRECTION('',(2.22044604925031E-16,-1.,0.));
#3404=DIRECTION('',(0.499999999999999,1.11022302462515E-16,0.866025403784439));
#3405=DIRECTION('center_axis',(4.80740671595891E-16,1.06745872495904E-31,
-1.));
#3406=DIRECTION('ref_axis',(1.,2.22044604925031E-16,4.80740671595891E-16));
#3407=DIRECTION('',(2.22044604925031E-16,-1.,0.));
#3408=DIRECTION('',(1.,2.22044604925031E-16,4.80740671595891E-16));
#3409=DIRECTION('center_axis',(-0.866025403784438,-1.92296268638356E-16,
-0.5));
#3410=DIRECTION('ref_axis',(0.5,1.11022302462516E-16,-0.866025403784438));
#3411=DIRECTION('',(2.22044604925031E-16,-1.,0.));
#3412=DIRECTION('',(0.5,1.11022302462516E-16,-0.866025403784438));
#3413=DIRECTION('center_axis',(-0.866025403784439,-1.92296268638356E-16,
0.499999999999999));
#3414=DIRECTION('ref_axis',(-0.499999999999999,-1.11022302462515E-16,-0.866025403784439));
#3415=DIRECTION('',(2.22044604925031E-16,-1.,0.));
#3416=DIRECTION('',(-0.499999999999999,-1.11022302462515E-16,-0.866025403784439));
#3417=DIRECTION('center_axis',(0.,0.,1.));
#3418=DIRECTION('ref_axis',(-1.,-2.22044604925031E-16,0.));
#3419=DIRECTION('',(-1.,-2.22044604925031E-16,0.));
#3420=DIRECTION('center_axis',(2.22044604925031E-16,-1.,0.));
#3421=DIRECTION('ref_axis',(0.,0.,1.));
#3422=DIRECTION('center_axis',(-2.22044604925031E-16,1.,0.));
#3423=DIRECTION('ref_axis',(-1.,-2.22044604925031E-16,0.));
#8075=CARTESIAN_POINT('',(0.,0.,0.));
#8076=CARTESIAN_POINT('Origin',(-2.67773308947627E-16,1.2059437743963,3.64739446828387));
#8077=CARTESIAN_POINT('',(1.55537930835193,3.0940562256037,3.64803845831604));
#8078=CARTESIAN_POINT('',(1.55549966270667,2.95594377439629,3.64841883122548));
#8079=CARTESIAN_POINT('',(1.5555,1.2059437743963,3.64739446828386));
#8080=CARTESIAN_POINT('',(0.903577229903434,2.50004392260581,2.38124738377906));
#8081=CARTESIAN_POINT('Ctrl Pts',(0.903577229903434,2.50004392260581,2.38124738377906));
#8082=CARTESIAN_POINT('Ctrl Pts',(0.85508552397506,2.50433411497395,2.34664160862681));
#8083=CARTESIAN_POINT('Ctrl Pts',(0.804491254712248,2.50862430734209,2.31474615079293));
#8084=CARTESIAN_POINT('Ctrl Pts',(0.752136324784236,2.51291449971023,2.28582508006303));
#8085=CARTESIAN_POINT('Ctrl Pts',(0.702087969422062,2.51701568125145,2.25817817026229));
#8086=CARTESIAN_POINT('Ctrl Pts',(0.650431357336846,2.52111686279267,2.2332493669833));
#8087=CARTESIAN_POINT('Ctrl Pts',(0.597496772224334,2.52521804433389,2.21122670051386));
#8088=CARTESIAN_POINT('Ctrl Pts',(0.544609525470966,2.52931555826907,2.18922372848223));
#8089=CARTESIAN_POINT('Ctrl Pts',(0.490447057473847,2.53341307220424,2.17012195018667));
#8090=CARTESIAN_POINT('Ctrl Pts',(0.435362908197919,2.53751058613941,2.15406282790205));
#8091=CARTESIAN_POINT('Ctrl Pts',(0.380305862575478,2.5416060839302,2.13801160736216));
#8092=CARTESIAN_POINT('Ctrl Pts',(0.324328543987183,2.54570158172099,2.12500022449484));
#8093=CARTESIAN_POINT('Ctrl Pts',(0.267800829156942,2.54979707951179,2.11512067881188));
#8094=CARTESIAN_POINT('Ctrl Pts',(0.211278192468849,2.55389220938536,2.10524202065352));
#8095=CARTESIAN_POINT('Ctrl Pts',(0.154205781558203,2.55798733925892,2.09849473034023));
#8096=CARTESIAN_POINT('Ctrl Pts',(0.0969625372345533,2.56208246913249,2.09491950347025));
#8097=CARTESIAN_POINT('Ctrl Pts',(0.0396642560698652,2.56618153629184,2.09134083917819));
#8098=CARTESIAN_POINT('Ctrl Pts',(-0.0178046547620221,2.57028060345119,
2.09094035559527));
#8099=CARTESIAN_POINT('Ctrl Pts',(-0.0750629135761472,2.57437967061054,
2.09370665890727));
#8100=CARTESIAN_POINT('Ctrl Pts',(-0.132353730100078,2.578481068547,2.0964745351714));
#8101=CARTESIAN_POINT('Ctrl Pts',(-0.189433127822198,2.58258246648346,2.10241272382604));
#8102=CARTESIAN_POINT('Ctrl Pts',(-0.245925895792534,2.58668386441992,2.11145804258825));
#8103=CARTESIAN_POINT('Ctrl Pts',(-0.302514885660697,2.5907922481053,2.12051876788423));
#8104=CARTESIAN_POINT('Ctrl Pts',(-0.358514735044354,2.59490063179069,2.13269706306549));
#8105=CARTESIAN_POINT('Ctrl Pts',(-0.413562868294952,2.59900901547607,2.14787921195346));
#8106=CARTESIAN_POINT('Ctrl Pts',(-0.43142604312879,2.60034219013111,2.15280583460031));
#8107=CARTESIAN_POINT('Ctrl Pts',(-0.449189147593431,2.60167536478614,2.15804838267405));
#8108=CARTESIAN_POINT('Ctrl Pts',(-0.46684025607362,2.60300853944117,2.16360188665087));
#8109=CARTESIAN_POINT('Ctrl Pts',(-0.521858625278674,2.60716403457439,2.18091211578018));
#8110=CARTESIAN_POINT('Ctrl Pts',(-0.576023644694715,2.61131952970761,2.20132138484263));
#8111=CARTESIAN_POINT('Ctrl Pts',(-0.628963033455794,2.61547502484083,2.22472593607193));
#8112=CARTESIAN_POINT('Ctrl Pts',(-0.681811493753012,2.61962338251369,2.24809028774584));
#8113=CARTESIAN_POINT('Ctrl Pts',(-0.73343803157307,2.62377174018655,2.27443950101458));
#8114=CARTESIAN_POINT('Ctrl Pts',(-0.783487045040432,2.6279200978594,2.30362056607643));
#8115=CARTESIAN_POINT('Ctrl Pts',(-0.833488047437585,2.63206447609135,2.33277363829554));
#8116=CARTESIAN_POINT('Ctrl Pts',(-0.881914078343796,2.6362088543233,2.36475291915533));
#8117=CARTESIAN_POINT('Ctrl Pts',(-0.928432591928929,2.64035323255525,2.39935874273587));
#8118=CARTESIAN_POINT('Ctrl Pts',(-0.974924175980665,2.64449521160968,2.43394453303052));
#8119=CARTESIAN_POINT('Ctrl Pts',(-1.0195100167281,2.64863719066411,2.47115354250067));
#8120=CARTESIAN_POINT('Ctrl Pts',(-1.06188696852167,2.65277916971855,2.51074310745072));
#8121=CARTESIAN_POINT('Ctrl Pts',(-1.10425550673426,2.6569203264185,2.55032481223158));
#8122=CARTESIAN_POINT('Ctrl Pts',(-1.14441564814527,2.66106148311845,2.59228577999225));
#8123=CARTESIAN_POINT('Ctrl Pts',(-1.18209939933821,2.6652026398184,2.63634488488836));
#8124=CARTESIAN_POINT('Ctrl Pts',(-1.2198180628967,2.66934763312091,2.68044480863946));
#8125=CARTESIAN_POINT('Ctrl Pts',(-1.25505541323189,2.67349262642343,2.72664635923883));
#8126=CARTESIAN_POINT('Ctrl Pts',(-1.28758315415599,2.67763761972594,2.7746345521937));
#8127=CARTESIAN_POINT('Ctrl Pts',(-1.32012488618734,2.68178439590806,2.82264338623632));
#8128=CARTESIAN_POINT('Ctrl Pts',(-1.3499544173738,2.68593117209018,2.87243994937997));
#8129=CARTESIAN_POINT('Ctrl Pts',(-1.37688806469825,2.6900779482723,2.92368215852846));
#8130=CARTESIAN_POINT('Ctrl Pts',(-1.40387406427022,2.69423278474608,2.97502396966493));
#8131=CARTESIAN_POINT('Ctrl Pts',(-1.42795271460863,2.69838762121987,3.02781656903583));
#8132=CARTESIAN_POINT('Ctrl Pts',(-1.44898778761461,2.70254245769366,3.08169610224088));
#8133=CARTESIAN_POINT('Ctrl Pts',(-1.46838439412369,2.70637366513319,3.13137884421063));
#8134=CARTESIAN_POINT('Ctrl Pts',(-1.48519355951164,2.71020487257272,3.18198527015832));
#8135=CARTESIAN_POINT('Ctrl Pts',(-1.49934664266485,2.71403608001225,3.23322071835562));
#8136=CARTESIAN_POINT('Ctrl Pts',(-1.51465181137774,2.71817915439409,3.28862682105783));
#8137=CARTESIAN_POINT('Ctrl Pts',(-1.52691450781882,2.72232222877592,3.34500138694105));
#8138=CARTESIAN_POINT('Ctrl Pts',(-1.5360179517072,2.72646530315776,3.40197828700557));
#8139=CARTESIAN_POINT('Ctrl Pts',(-1.54510497073757,2.73060090241158,3.45885238668986));
#8140=CARTESIAN_POINT('Ctrl Pts',(-1.55104396849636,2.73473650166541,3.51632615235849));
#8141=CARTESIAN_POINT('Ctrl Pts',(-1.55376848069946,2.73887210091923,3.57402036941438));
#8142=CARTESIAN_POINT('Ctrl Pts',(-1.55649024188075,2.74300352433428,3.63165633088644));
#8143=CARTESIAN_POINT('Ctrl Pts',(-1.55600392310557,2.74713494774932,3.68951178383784));
#8144=CARTESIAN_POINT('Ctrl Pts',(-1.55229470988028,2.75126637116436,3.74720119990903));
#8145=CARTESIAN_POINT('Ctrl Pts',(-1.54858780655053,2.75539522175441,3.80485469016077));
#8146=CARTESIAN_POINT('Ctrl Pts',(-1.54166202030053,2.75952407234446,3.86234182841598));
#8147=CARTESIAN_POINT('Ctrl Pts',(-1.53155460991275,2.76365292293451,3.91927813247688));
#8148=CARTESIAN_POINT('Ctrl Pts',(-1.52144958264269,2.76778080002723,3.97620101213824));
#8149=CARTESIAN_POINT('Ctrl Pts',(-1.50816451151996,2.77190867711994,4.03257280145901));
#8150=CARTESIAN_POINT('Ctrl Pts',(-1.49178807918711,2.77603655421266,4.08801741003253));
#8151=CARTESIAN_POINT('Ctrl Pts',(-1.47539694624562,2.78016813677092,4.14351178948869));
#8152=CARTESIAN_POINT('Ctrl Pts',(-1.45590905346099,2.78429971932918,4.19807682245725));
#8153=CARTESIAN_POINT('Ctrl Pts',(-1.4334631269432,2.78843130188743,4.25135118336719));
#8154=CARTESIAN_POINT('Ctrl Pts',(-1.41100802357335,2.79256457361285,4.30464732510796));
#8155=CARTESIAN_POINT('Ctrl Pts',(-1.38559270429132,2.79669784533826,4.35665127207841));
#8156=CARTESIAN_POINT('Ctrl Pts',(-1.35740294273004,2.80083111706367,4.40702431305554));
#8157=CARTESIAN_POINT('Ctrl Pts',(-1.32915808863627,2.80497246662991,4.45749580035656));
#8158=CARTESIAN_POINT('Ctrl Pts',(-1.29812823699444,2.80911381619615,4.50632956924819));
#8159=CARTESIAN_POINT('Ctrl Pts',(-1.26454328228958,2.81325516576239,4.55321483525312));
#8160=CARTESIAN_POINT('Ctrl Pts',(-1.23262241414806,2.81719131736937,4.59777700325588));
#8161=CARTESIAN_POINT('Ctrl Pts',(-1.19839396464653,2.82112746897635,4.64057893014162));
#8162=CARTESIAN_POINT('Ctrl Pts',(-1.16208710892346,2.82506362058333,4.68138373383449));
#8163=CARTESIAN_POINT('Ctrl Pts',(-1.12381204372855,2.82921315257595,4.72440058259503));
#8164=CARTESIAN_POINT('Ctrl Pts',(-1.0830653595052,2.83336268456856,4.7653790955833));
#8165=CARTESIAN_POINT('Ctrl Pts',(-1.04009256905409,2.83751221656118,4.80402219482274));
#8166=CARTESIAN_POINT('Ctrl Pts',(-0.997195985606611,2.84165438986481,4.84259676523792));
#8167=CARTESIAN_POINT('Ctrl Pts',(-0.952081515568061,2.84579656316844,4.87884379743944));
#8168=CARTESIAN_POINT('Ctrl Pts',(-0.905032885213852,2.84993873647208,4.91250147035187));
#8169=CARTESIAN_POINT('Ctrl Pts',(-0.858030931578233,2.85407680034561,4.94612575164982));
#8170=CARTESIAN_POINT('Ctrl Pts',(-0.80909904069553,2.85821486421915,4.97716546230243));
#8171=CARTESIAN_POINT('Ctrl Pts',(-0.758554187283879,2.86235292809268,5.00539881104353));
#8172=CARTESIAN_POINT('Ctrl Pts',(-0.708040087859642,2.8664884741636,5.03361498121959));
#8173=CARTESIAN_POINT('Ctrl Pts',(-0.655915424773617,2.87062402023451,5.05902792115146));
#8174=CARTESIAN_POINT('Ctrl Pts',(-0.602524480517743,2.87475956630543,5.08146019215319));
#8175=CARTESIAN_POINT('Ctrl Pts',(-0.549145539849393,2.87889418260464,5.10388741983283));
#8176=CARTESIAN_POINT('Ctrl Pts',(-0.49450136273391,2.88302879890385,5.12333510754783));
#8177=CARTESIAN_POINT('Ctrl Pts',(-0.438957034282652,2.88716341520306,5.13967358830592));
#8178=CARTESIAN_POINT('Ctrl Pts',(-0.383362726489432,2.89130175187135,5.15602677059232));
#8179=CARTESIAN_POINT('Ctrl Pts',(-0.326867148839283,2.89544008853964,5.16926500675));
#8180=CARTESIAN_POINT('Ctrl Pts',(-0.269850104507525,2.89957842520793,5.17930868621426));
#8181=CARTESIAN_POINT('Ctrl Pts',(-0.212809518986636,2.90371847051207,5.18935651251147));
#8182=CARTESIAN_POINT('Ctrl Pts',(-0.155247555237378,2.90785851581621,5.19620708965532));
#8183=CARTESIAN_POINT('Ctrl Pts',(-0.0975505429432606,2.91199856112035,
5.19983259638157));
#8184=CARTESIAN_POINT('Ctrl Pts',(-0.0397417314675407,2.91614662856738,
5.20346512823214));
#8185=CARTESIAN_POINT('Ctrl Pts',(0.0182021292546374,2.92029469601441,5.20386009675022));
#8186=CARTESIAN_POINT('Ctrl Pts',(0.0758942242731154,2.92444276346144,5.2010418918398));
#8187=CARTESIAN_POINT('Ctrl Pts',(0.129896919511928,2.92832556269243,5.19840391065973));
#8188=CARTESIAN_POINT('Ctrl Pts',(0.18367870036531,2.93220836192342,5.19295113580138));
#8189=CARTESIAN_POINT('Ctrl Pts',(0.23692976137395,2.93609116115441,5.18474431076452));
#8190=CARTESIAN_POINT('Ctrl Pts',(0.293834898607228,2.94024039722414,5.17597433517856));
#8191=CARTESIAN_POINT('Ctrl Pts',(0.350371063130971,2.94438963329388,5.16402229316462));
#8192=CARTESIAN_POINT('Ctrl Pts',(0.406155507456965,2.94853886936361,5.14893299718094));
#8193=CARTESIAN_POINT('Ctrl Pts',(0.461841333946411,2.95268077025793,5.13387037662162));
#8194=CARTESIAN_POINT('Ctrl Pts',(0.516777579703641,2.95682267115225,5.11568164538636));
#8195=CARTESIAN_POINT('Ctrl Pts',(0.570590348551129,2.96096457204657,5.09446285095979));
#8196=CARTESIAN_POINT('Ctrl Pts',(0.624349914882789,2.9651023780104,5.07326503470012));
#8197=CARTESIAN_POINT('Ctrl Pts',(0.676987723304679,2.96924018397423,5.04904328073132));
#8198=CARTESIAN_POINT('Ctrl Pts',(0.728145436661754,2.97337798993807,5.02194329356025));
#8199=CARTESIAN_POINT('Ctrl Pts',(0.779272206164133,2.97751329306003,4.99485969840536));
#8200=CARTESIAN_POINT('Ctrl Pts',(0.828920196343082,2.98164859618201,4.964901564363));
#8201=CARTESIAN_POINT('Ctrl Pts',(0.876753485845882,2.98578389930398,4.93226161124344));
#8202=CARTESIAN_POINT('Ctrl Pts',(0.924576199211511,2.98991828809341,4.89962887495186));
#8203=CARTESIAN_POINT('Ctrl Pts',(0.970584578814995,2.99405267688284,4.86431579004715));
#8204=CARTESIAN_POINT('Ctrl Pts',(1.01447152341757,2.99818706567227,4.82655848493924));
#8205=CARTESIAN_POINT('Ctrl Pts',(1.05839823980066,3.00232520117965,4.78876696293005));
#8206=CARTESIAN_POINT('Ctrl Pts',(1.10019928310736,3.00646333668704,4.74852713370935));
#8207=CARTESIAN_POINT('Ctrl Pts',(1.13960159336571,3.01060147219443,4.70611466663579));
#8208=CARTESIAN_POINT('Ctrl Pts',(1.17902030680071,3.01474133040709,4.6636845432577));
#8209=CARTESIAN_POINT('Ctrl Pts',(1.21603796238847,3.01888118861976,4.61908037948246));
#8210=CARTESIAN_POINT('Ctrl Pts',(1.25042144777114,3.02302104683242,4.57261144443267));
#8211=CARTESIAN_POINT('Ctrl Pts',(1.28487178165961,3.0271689537735,4.52605216429891));
#8212=CARTESIAN_POINT('Ctrl Pts',(1.31667742338708,3.03131686071457,4.4776213038563));
#8213=CARTESIAN_POINT('Ctrl Pts',(1.34564884130234,3.03546476765565,4.42765688946131));
#8214=CARTESIAN_POINT('Ctrl Pts',(1.37278148105619,3.0393494123456,4.38086365137207));
#8215=CARTESIAN_POINT('Ctrl Pts',(1.3974285397566,3.04323405703554,4.33272591740904));
#8216=CARTESIAN_POINT('Ctrl Pts',(1.41947265623264,3.04711870172549,4.28353724173009));
#8217=CARTESIAN_POINT('Ctrl Pts',(1.4452163205397,3.05165528585027,4.22609348998056));
#8218=CARTESIAN_POINT('Ctrl Pts',(1.46750340567379,3.05619186997506,4.1670086888806));
#8219=CARTESIAN_POINT('Ctrl Pts',(1.48614312745063,3.06072845409985,4.1066970425541));
#8220=CARTESIAN_POINT('Ctrl Pts',(1.50472689290404,3.06525141942863,4.04656645139723));
#8221=CARTESIAN_POINT('Ctrl Pts',(1.5196849767674,3.06977438475741,3.9852166812314));
#8222=CARTESIAN_POINT('Ctrl Pts',(1.53087461175194,3.07429735008618,3.92308119827525));
#8223=CARTESIAN_POINT('Ctrl Pts',(1.54201174785395,3.07879909482771,3.86123723898596));
#8224=CARTESIAN_POINT('Ctrl Pts',(1.54941557119274,3.08330083956923,3.79861525544648));
#8225=CARTESIAN_POINT('Ctrl Pts',(1.55299366908018,3.08780258431076,3.73566062146206));
#8226=CARTESIAN_POINT('Ctrl Pts',(1.55465051858957,3.0898871314084,3.70650927968446));
#8227=CARTESIAN_POINT('Ctrl Pts',(1.55548775667918,3.09197167850605,3.67728683394469));
#8228=CARTESIAN_POINT('Ctrl Pts',(1.55549986667069,3.0940562256037,3.64803850823206));
#8229=CARTESIAN_POINT('',(-0.903606778650208,2.5,2.38126847156104));
#8230=CARTESIAN_POINT('Origin',(-5.55111512312578E-16,2.5,3.64739446828387));
#8231=CARTESIAN_POINT('Ctrl Pts',(-0.903606778650211,2.5,2.38126847156104));
#8232=CARTESIAN_POINT('Ctrl Pts',(-0.951845303079983,2.50424458524762,2.41569526461295));
#8233=CARTESIAN_POINT('Ctrl Pts',(-0.998152286150682,2.50848917049524,2.45290980505554));
#8234=CARTESIAN_POINT('Ctrl Pts',(-1.04220403534506,2.51273375574287,2.49266896033383));
#8235=CARTESIAN_POINT('Ctrl Pts',(-1.0862342553778,2.5169762665584,2.53240868434557));
#8236=CARTESIAN_POINT('Ctrl Pts',(-1.12801106716941,2.52121877737394,2.57469023195131));
#8237=CARTESIAN_POINT('Ctrl Pts',(-1.16724434287758,2.52546128818948,2.61923062238172));
#8238=CARTESIAN_POINT('Ctrl Pts',(-1.20646784811623,2.52970274247018,2.66375992068386));
#8239=CARTESIAN_POINT('Ctrl Pts',(-1.24314875403147,2.53394419675088,2.71054658023795));
#8240=CARTESIAN_POINT('Ctrl Pts',(-1.27703555050147,2.53818565103158,2.75927260009494));
#8241=CARTESIAN_POINT('Ctrl Pts',(-1.3109241886902,2.54242733583174,2.80800126816989));
#8242=CARTESIAN_POINT('Ctrl Pts',(-1.34201813870958,2.54666902063189,2.85866910663535));
#8243=CARTESIAN_POINT('Ctrl Pts',(-1.37010880618711,2.55091070543205,2.91092850898329));
#8244=CARTESIAN_POINT('Ctrl Pts',(-1.39820952338904,2.55515390773844,2.96320660766839));
#8245=CARTESIAN_POINT('Ctrl Pts',(-1.42330459453232,2.55939711004483,3.01707697287849));
#8246=CARTESIAN_POINT('Ctrl Pts',(-1.44523186702567,2.56364031235123,3.07216833837189));
#8247=CARTESIAN_POINT('Ctrl Pts',(-1.46719221439394,2.56788991506085,3.12734280312097));
#8248=CARTESIAN_POINT('Ctrl Pts',(-1.48597504305491,2.57213951777047,3.18374149258924));
#8249=CARTESIAN_POINT('Ctrl Pts',(-1.50146706506275,2.57638912048008,3.24097485442173));
#8250=CARTESIAN_POINT('Ctrl Pts',(-1.51697108246425,2.58064201363542,3.29825253175453));
#8251=CARTESIAN_POINT('Ctrl Pts',(-1.52917911615242,2.58489490679075,3.35636569303991));
#8252=CARTESIAN_POINT('Ctrl Pts',(-1.53802901468286,2.58914779994608,3.41491436162167));
#8253=CARTESIAN_POINT('Ctrl Pts',(-1.5468976907274,2.59340971679371,3.47358725744129));
#8254=CARTESIAN_POINT('Ctrl Pts',(-1.55239394856734,2.59767163364134,3.53269702190671));
#8255=CARTESIAN_POINT('Ctrl Pts',(-1.55450758299866,2.60193355048897,3.59183887090913));
#8256=CARTESIAN_POINT('Ctrl Pts',(-1.55601092615331,2.60496488051634,3.63390408925213));
#8257=CARTESIAN_POINT('Ctrl Pts',(-1.55580413569243,2.60799621054371,3.67598547779196));
#8258=CARTESIAN_POINT('Ctrl Pts',(-1.55389953165917,2.61102754057108,3.71793874877079));
#8259=CARTESIAN_POINT('Ctrl Pts',(-1.55131896143399,2.61513472499091,3.77478172507797));
#8260=CARTESIAN_POINT('Ctrl Pts',(-1.5456085090895,2.61924190941074,3.83162701942664));
#8261=CARTESIAN_POINT('Ctrl Pts',(-1.53676371753943,2.62334909383056,3.88809662127467));
#8262=CARTESIAN_POINT('Ctrl Pts',(-1.52790694169175,2.62746184330188,3.94464273691164));
#8263=CARTESIAN_POINT('Ctrl Pts',(-1.51590728810265,2.6315745927732,4.00081160376278));
#8264=CARTESIAN_POINT('Ctrl Pts',(-1.50081279014695,2.63568734224451,4.05622355106947));
#8265=CARTESIAN_POINT('Ctrl Pts',(-1.48578618297733,2.63978159373098,4.1113862710967));
#8266=CARTESIAN_POINT('Ctrl Pts',(-1.46769260897502,2.64387584521744,4.16579833998209));
#8267=CARTESIAN_POINT('Ctrl Pts',(-1.44663091606904,2.64797009670391,4.21909302755551));
#8268=CARTESIAN_POINT('Ctrl Pts',(-1.42558455612138,2.65206136756637,4.27234891648024));
#8269=CARTESIAN_POINT('Ctrl Pts',(-1.40157455173156,2.65615263842883,4.32448854122648));
#8270=CARTESIAN_POINT('Ctrl Pts',(-1.37474917137091,2.66024390929129,4.3751615778835));
#8271=CARTESIAN_POINT('Ctrl Pts',(-1.34793248907838,2.66433385356855,4.42581818392449));
#8272=CARTESIAN_POINT('Ctrl Pts',(-1.31830248987025,2.66842379784581,4.47500867441785));
#8273=CARTESIAN_POINT('Ctrl Pts',(-1.28605401101194,2.67251374212307,4.52240608578394));
#8274=CARTESIAN_POINT('Ctrl Pts',(-1.25350196148784,2.67664218704132,4.57024967210882));
#8275=CARTESIAN_POINT('Ctrl Pts',(-1.2182821514702,2.68077063195958,4.61626576508545));
#8276=CARTESIAN_POINT('Ctrl Pts',(-1.18063904171929,2.68489907687784,4.66014898106975));
#8277=CARTESIAN_POINT('Ctrl Pts',(-1.14330212489149,2.68899394060087,4.70367524646556));
#8278=CARTESIAN_POINT('Ctrl Pts',(-1.10358160406713,2.6930888043239,4.7451028578062));
#8279=CARTESIAN_POINT('Ctrl Pts',(-1.06175385752749,2.69718366804694,4.78417017000585));
#8280=CARTESIAN_POINT('Ctrl Pts',(-1.01941157894819,2.70132890356281,4.82371805755304));
#8281=CARTESIAN_POINT('Ctrl Pts',(-0.974910298315904,2.70547413907868,4.86084680903068));
#8282=CARTESIAN_POINT('Ctrl Pts',(-0.92856965375026,2.70961937459455,4.89532821978438));
#8283=CARTESIAN_POINT('Ctrl Pts',(-0.882229009184617,2.71376461011042,4.92980963053807));
#8284=CARTESIAN_POINT('Ctrl Pts',(-0.834049506379406,2.71790984562629,4.96164345442314));
#8285=CARTESIAN_POINT('Ctrl Pts',(-0.78437668455737,2.72205508114216,4.99064927163385));
#8286=CARTESIAN_POINT('Ctrl Pts',(-0.734596789904455,2.72620925196883,5.01971761267242));
#8287=CARTESIAN_POINT('Ctrl Pts',(-0.683096214577692,2.7303634227955,5.04607495812685));
#8288=CARTESIAN_POINT('Ctrl Pts',(-0.630201320826871,2.73451759362217,5.06951490805965));
#8289=CARTESIAN_POINT('Ctrl Pts',(-0.57740037556843,2.73866438607905,5.09291322546801));
#8290=CARTESIAN_POINT('Ctrl Pts',(-0.523210498602592,2.74281117853593,5.11340422484301));
#8291=CARTESIAN_POINT('Ctrl Pts',(-0.467983399567077,2.74695797099281,5.1308269027849));
#8292=CARTESIAN_POINT('Ctrl Pts',(-0.412811236673254,2.75110063850411,5.14823224983814));
#8293=CARTESIAN_POINT('Ctrl Pts',(-0.356604388684699,2.75524330601541,5.16257516809759));
#8294=CARTESIAN_POINT('Ctrl Pts',(-0.299733729231309,2.7593859735267,5.1737430331802));
#8295=CARTESIAN_POINT('Ctrl Pts',(-0.242897963352596,2.76352609926199,5.18490404610499));
#8296=CARTESIAN_POINT('Ctrl Pts',(-0.185399701714465,2.76766622499727,5.19289376819827));
#8297=CARTESIAN_POINT('Ctrl Pts',(-0.127622009920969,2.77180635073256,5.19765021253504));
#8298=CARTESIAN_POINT('Ctrl Pts',(-0.0698577464276305,2.77594551424783,
5.20240555141119));
#8299=CARTESIAN_POINT('Ctrl Pts',(-0.0118146987146111,2.78008467776311,
5.20392906193616));
#8300=CARTESIAN_POINT('Ctrl Pts',(0.0461191024158557,2.78422384127839,5.20221062410177));
#8301=CARTESIAN_POINT('Ctrl Pts',(0.104103724821396,2.78836663579255,5.20049067880196));
#8302=CARTESIAN_POINT('Ctrl Pts',(0.161978389084628,2.79250943030672,5.19552311584121));
#8303=CARTESIAN_POINT('Ctrl Pts',(0.219356586646835,2.79665222482088,5.18734996695734));
#8304=CARTESIAN_POINT('Ctrl Pts',(0.276757871024163,2.80079668623877,5.17917352950768));
#8305=CARTESIAN_POINT('Ctrl Pts',(0.3336617800461,2.80494114765666,5.16778903477395));
#8306=CARTESIAN_POINT('Ctrl Pts',(0.389691619463284,2.80908560907455,5.15328978062138));
#8307=CARTESIAN_POINT('Ctrl Pts',(0.445828152477652,2.81323796249251,5.13876291658097));
#8308=CARTESIAN_POINT('Ctrl Pts',(0.501086793044856,2.81739031591048,5.12110959723251));
#8309=CARTESIAN_POINT('Ctrl Pts',(0.555106538707356,2.82154266932844,5.10047291788126));
#8310=CARTESIAN_POINT('Ctrl Pts',(0.605149267896905,2.82538932012337,5.08135554249414));
#8311=CARTESIAN_POINT('Ctrl Pts',(0.65412871360423,2.8292359709183,5.05967858632402));
#8312=CARTESIAN_POINT('Ctrl Pts',(0.701776811900781,2.83308262171323,5.03559098040972));
#8313=CARTESIAN_POINT('Ctrl Pts',(0.753250629317281,2.83723812440404,5.00956935366784));
#8314=CARTESIAN_POINT('Ctrl Pts',(0.803378780995946,2.84139362709485,4.98062856210418));
#8315=CARTESIAN_POINT('Ctrl Pts',(0.85181079741487,2.84554912978566,4.94893148865918));
#8316=CARTESIAN_POINT('Ctrl Pts',(0.900159631423033,2.84969749536434,4.91728885521438));
#8317=CARTESIAN_POINT('Ctrl Pts',(0.946817682329863,2.85384586094302,4.88289961882828));
#8318=CARTESIAN_POINT('Ctrl Pts',(0.991458942442062,2.8579942265217,4.84597254894932));
#8319=CARTESIAN_POINT('Ctrl Pts',(1.03605738133996,2.86213861286568,4.8090809006057));
#8320=CARTESIAN_POINT('Ctrl Pts',(1.07864246529873,2.86628299920966,4.76965657176451));
#8321=CARTESIAN_POINT('Ctrl Pts',(1.11891851883289,2.87042738555364,4.72795062055585));
#8322=CARTESIAN_POINT('Ctrl Pts',(1.15917125850317,2.87456937291235,4.68626881090983));
#8323=CARTESIAN_POINT('Ctrl Pts',(1.19711725811528,2.87871136027106,4.64230836973605));
#8324=CARTESIAN_POINT('Ctrl Pts',(1.23249683959235,2.88285334762977,4.59635800309164));
#8325=CARTESIAN_POINT('Ctrl Pts',(1.26786939829556,2.88699451281254,4.55041675750013));
#8326=CARTESIAN_POINT('Ctrl Pts',(1.30067623431273,2.89113567799531,4.50248678159935));
#8327=CARTESIAN_POINT('Ctrl Pts',(1.33069860539264,2.89527684317808,4.45288901923136));
#8328=CARTESIAN_POINT('Ctrl Pts',(1.36074879240209,2.89942184517836,4.40324530420158));
#8329=CARTESIAN_POINT('Ctrl Pts',(1.38800908947886,2.90356684717864,4.35193115929334));
#8330=CARTESIAN_POINT('Ctrl Pts',(1.4123054265734,2.90771184917893,4.29929448521234));
#8331=CARTESIAN_POINT('Ctrl Pts',(1.43661221496204,2.91185863419015,4.24663516897915));
#8332=CARTESIAN_POINT('Ctrl Pts',(1.45795230958076,2.91600541920138,4.19265267234776));
#8333=CARTESIAN_POINT('Ctrl Pts',(1.47620006451295,2.92015220421261,4.13771438377982));
#8334=CARTESIAN_POINT('Ctrl Pts',(1.49448328890889,2.92430704962585,4.08266930773903));
#8335=CARTESIAN_POINT('Ctrl Pts',(1.50966202478598,2.92846189503909,4.02666522918658));
#8336=CARTESIAN_POINT('Ctrl Pts',(1.52166098851939,2.93261674045233,3.97008330604899));
#8337=CARTESIAN_POINT('Ctrl Pts',(1.53272511068826,2.93644788106299,3.91790969138913));
#8338=CARTESIAN_POINT('Ctrl Pts',(1.54108617161882,2.94027902167365,3.86524520012911));
#8339=CARTESIAN_POINT('Ctrl Pts',(1.54672433177784,2.94411016228431,3.81239171518941));
#8340=CARTESIAN_POINT('Ctrl Pts',(1.55252937411617,2.94805469965497,3.75797383610294));
#8341=CARTESIAN_POINT('Ctrl Pts',(1.5554635597827,2.95199923702563,3.7032412811352));
#8342=CARTESIAN_POINT('Ctrl Pts',(1.55549966270667,2.95594377439629,3.64841883122548));
#8343=CARTESIAN_POINT('Origin',(-2.67773308947627E-16,1.2059437743963,3.64739446828387));
#8344=CARTESIAN_POINT('',(1.55549937976474,3.7940562256037,3.64600538531537));
#8345=CARTESIAN_POINT('',(1.55328922867418,3.65594309057409,3.64812360962188));
#8346=CARTESIAN_POINT('',(1.5555,1.2059437743963,3.64739446828386));
#8347=CARTESIAN_POINT('Ctrl Pts',(1.55320831614475,3.0940562256037,3.64803755943733));
#8348=CARTESIAN_POINT('Ctrl Pts',(1.55211225787393,3.11541956450132,3.34872916974666));
#8349=CARTESIAN_POINT('Ctrl Pts',(1.32451511527677,3.1737920835893,2.5293530162389));
#8350=CARTESIAN_POINT('Ctrl Pts',(-0.00194386449727044,3.26917378286764,
1.80949553386703));
#8351=CARTESIAN_POINT('Ctrl Pts',(-1.54419526187211,3.38020132343872,2.6507072563878));
#8352=CARTESIAN_POINT('Ctrl Pts',(-1.67560476579265,3.4912288640098,4.40256135417452));
#8353=CARTESIAN_POINT('Ctrl Pts',(-0.276097817182277,3.60225640458088,5.46444788548381));
#8354=CARTESIAN_POINT('Ctrl Pts',(1.22562677556159,3.70319885844551,4.92053574953289));
#8355=CARTESIAN_POINT('Ctrl Pts',(1.55162911722742,3.76713213211979,4.02218696309102));
#8356=CARTESIAN_POINT('Ctrl Pts',(1.5548981372976,3.7940562256037,3.64600592223341));
#8357=CARTESIAN_POINT('Ctrl Pts',(1.55731930826876,2.95594474730389,3.64840649193144));
#8358=CARTESIAN_POINT('Ctrl Pts',(1.55406984475527,2.98900906582105,3.18832795677562));
#8359=CARTESIAN_POINT('Ctrl Pts',(1.09493216072152,3.05908256452858,2.20731900520876));
#8360=CARTESIAN_POINT('Ctrl Pts',(-0.571437519320521,3.16616524342647,1.90065774706199));
#8361=CARTESIAN_POINT('Ctrl Pts',(-1.77703909951801,3.27719278399755,3.17828914298809));
#8362=CARTESIAN_POINT('Ctrl Pts',(-1.35908642417454,3.38822032456863,4.88467959896744));
#8363=CARTESIAN_POINT('Ctrl Pts',(0.300609421841398,3.4992478651397,5.4605432395681));
#8364=CARTESIAN_POINT('Ctrl Pts',(1.41386361340157,3.58848878714153,4.59192891748905));
#8365=CARTESIAN_POINT('Ctrl Pts',(1.55417851871196,3.64072052895299,3.86136782353057));
#8366=CARTESIAN_POINT('Ctrl Pts',(1.55328922867418,3.65594309057409,3.64812360962188));
#8367=CARTESIAN_POINT('Origin',(-2.67773308947627E-16,1.2059437743963,3.64739446828387));
#8368=CARTESIAN_POINT('',(1.55549997006787,4.49405622566528,3.64769962209175));
#8369=CARTESIAN_POINT('',(1.5555,4.35539415465377,3.64739446822635));
#8370=CARTESIAN_POINT('',(1.5555,1.2059437743963,3.64739446828386));
#8371=CARTESIAN_POINT('Ctrl Pts',(1.55549937976474,3.7940562256037,3.64600538531537));
#8372=CARTESIAN_POINT('Ctrl Pts',(1.55543459285259,3.79924672256036,3.57345680185905));
#8373=CARTESIAN_POINT('Ctrl Pts',(1.55029041969615,3.80443721951702,3.50113325274295));
#8374=CARTESIAN_POINT('Ctrl Pts',(1.54018379952597,3.80962771647368,3.4296466469911));
#8375=CARTESIAN_POINT('Ctrl Pts',(1.53065335188231,3.81452230622346,3.36223545097616));
#8376=CARTESIAN_POINT('Ctrl Pts',(1.5167106747383,3.81941689597325,3.29556811307819));
#8377=CARTESIAN_POINT('Ctrl Pts',(1.49849211920356,3.82431148572304,3.23013960769527));
#8378=CARTESIAN_POINT('Ctrl Pts',(1.48305092809396,3.82845990987145,3.17468548271226));
#8379=CARTESIAN_POINT('Ctrl Pts',(1.46449498927747,3.83260833401987,3.11997351657152));
#8380=CARTESIAN_POINT('Ctrl Pts',(1.44291390367819,3.83675675816828,3.06637836130218));
#8381=CARTESIAN_POINT('Ctrl Pts',(1.42137112324434,3.84089781910633,3.01287833430057));
#8382=CARTESIAN_POINT('Ctrl Pts',(1.39681404658784,3.84503888004438,2.96049166264535));
#8383=CARTESIAN_POINT('Ctrl Pts',(1.3693821080243,3.84917994098242,2.9095781685026));
#8384=CARTESIAN_POINT('Ctrl Pts',(1.34197740488627,3.85331689052468,2.85871522312709));
#8385=CARTESIAN_POINT('Ctrl Pts',(1.31170374076445,3.85745384006693,2.80932301343158));
#8386=CARTESIAN_POINT('Ctrl Pts',(1.27874802547175,3.86159078960918,2.76174005636458));
#8387=CARTESIAN_POINT('Ctrl Pts',(1.24581236754328,3.86572522133919,2.71418605903015));
#8388=CARTESIAN_POINT('Ctrl Pts',(1.21019819009312,3.86985965306919,2.66843955871361));
#8389=CARTESIAN_POINT('Ctrl Pts',(1.17213644518852,3.87399408479919,2.62481126684703));
#8390=CARTESIAN_POINT('Ctrl Pts',(1.13408324191106,3.87812758870062,2.58119276582432));
#8391=CARTESIAN_POINT('Ctrl Pts',(1.09358390378644,3.88226109260205,2.53969192169267));
#8392=CARTESIAN_POINT('Ctrl Pts',(1.05090908617986,3.88639459650348,2.50058570367461));
#8393=CARTESIAN_POINT('Ctrl Pts',(1.00819573351749,3.89053183292944,2.46144417302074));
#8394=CARTESIAN_POINT('Ctrl Pts',(0.963303359719073,3.8946690693554,2.42470194310747));
#8395=CARTESIAN_POINT('Ctrl Pts',(0.916537863760172,3.89880630578136,2.39059751002293));
#8396=CARTESIAN_POINT('Ctrl Pts',(0.869752999509781,3.90294525567575,2.35647895232393));
#8397=CARTESIAN_POINT('Ctrl Pts',(0.821093903997002,3.90708420557015,2.32500065384963));
#8398=CARTESIAN_POINT('Ctrl Pts',(0.770895120881294,3.91122315546454,2.29635747300898));
#8399=CARTESIAN_POINT('Ctrl Pts',(0.720598766603014,3.91537015021835,2.26765861853878));
#8400=CARTESIAN_POINT('Ctrl Pts',(0.668757211424777,3.91951714497215,2.24180612807529));
#8401=CARTESIAN_POINT('Ctrl Pts',(0.615728403904911,3.92366413972596,2.21894818556103));
#8402=CARTESIAN_POINT('Ctrl Pts',(0.565965033127361,3.92755576858201,2.19749780185924));
#8403=CARTESIAN_POINT('Ctrl Pts',(0.515156658330857,3.93144739743807,2.17868417709866));
#8404=CARTESIAN_POINT('Ctrl Pts',(0.46361041530187,3.93533902629412,2.16258955422155));
#8405=CARTESIAN_POINT('Ctrl Pts',(0.408662882562632,3.93948744510044,2.14543292426175));
#8406=CARTESIAN_POINT('Ctrl Pts',(0.352646623653704,3.94363586390677,2.13129460873933));
#8407=CARTESIAN_POINT('Ctrl Pts',(0.29592487144026,3.94778428271309,2.12030287952337));
#8408=CARTESIAN_POINT('Ctrl Pts',(0.239303797818613,3.95192533826022,2.10933066013875));
#8409=CARTESIAN_POINT('Ctrl Pts',(0.181980223358933,3.95606639380735,2.10149403971228));
#8410=CARTESIAN_POINT('Ctrl Pts',(0.12433199791367,3.96020744935448,2.0968713938684));
#8411=CARTESIAN_POINT('Ctrl Pts',(0.0667410081572819,3.96434439347988,2.09225333759024));
#8412=CARTESIAN_POINT('Ctrl Pts',(0.00882652245797441,3.96848133760527,
2.09084297499291));
#8413=CARTESIAN_POINT('Ctrl Pts',(-0.0490257099392019,3.97261828173067,
2.09266724791209));
#8414=CARTESIAN_POINT('Ctrl Pts',(-0.10684273228549,3.97675270802733,2.09449041054149));
#8415=CARTESIAN_POINT('Ctrl Pts',(-0.164597057061184,3.98088713432399,2.09954428982219));
#8416=CARTESIAN_POINT('Ctrl Pts',(-0.221902358276799,3.98502156062065,2.10780374559449));
#8417=CARTESIAN_POINT('Ctrl Pts',(-0.279194799207534,3.98915505908169,2.11606134780436));
#8418=CARTESIAN_POINT('Ctrl Pts',(-0.336037901517815,3.99328855754272,2.12752302405911));
#8419=CARTESIAN_POINT('Ctrl Pts',(-0.392052103871645,3.99742205600376,2.14211197059454));
#8420=CARTESIAN_POINT('Ctrl Pts',(-0.44811688716568,4.00155928702242,2.15671409097877));
#8421=CARTESIAN_POINT('Ctrl Pts',(-0.503350769331993,4.00569651804109,2.17444899447387));
#8422=CARTESIAN_POINT('Ctrl Pts',(-0.557387348271533,4.00983374905976,2.19518938841848));
#8423=CARTESIAN_POINT('Ctrl Pts',(-0.611446307026563,4.01397269355601,2.21593837221462));
#8424=CARTESIAN_POINT('Ctrl Pts',(-0.664306497514911,4.01811163805226,2.23969511520848));
#8425=CARTESIAN_POINT('Ctrl Pts',(-0.715622597532242,4.02225058254852,2.26628457117169));
#8426=CARTESIAN_POINT('Ctrl Pts',(-0.767038441642636,4.02639757199099,2.29292570957315));
#8427=CARTESIAN_POINT('Ctrl Pts',(-0.816903747256544,4.03054456143347,2.32241029888276));
#8428=CARTESIAN_POINT('Ctrl Pts',(-0.864899667938166,4.03469155087595,2.35451828921626));
#8429=CARTESIAN_POINT('Ctrl Pts',(-0.909940626698667,4.03858322287236,2.38464948886732));
#8430=CARTESIAN_POINT('Ctrl Pts',(-0.953335299435889,4.04247489486877,2.41709037054295));
#8431=CARTESIAN_POINT('Ctrl Pts',(-0.994847796632108,4.04636656686519,2.4516277219925));
#8432=CARTESIAN_POINT('Ctrl Pts',(-1.03909898735835,4.0505149831588,2.48844359743718));
#8433=CARTESIAN_POINT('Ctrl Pts',(-1.08139645579429,4.05466339945241,2.5277962696892));
#8434=CARTESIAN_POINT('Ctrl Pts',(-1.12143520301905,4.05881181574602,2.56945043660615));
#8435=CARTESIAN_POINT('Ctrl Pts',(-1.16140288229428,4.06295286868638,2.61103066823696));
#8436=CARTESIAN_POINT('Ctrl Pts',(-1.19911944019534,4.06709392162673,2.65490391383242));
#8437=CARTESIAN_POINT('Ctrl Pts',(-1.23431383195748,4.07123497456708,2.70079549604777));
#8438=CARTESIAN_POINT('Ctrl Pts',(-1.26947328068964,4.0753719160303,2.74664151444306));
#8439=CARTESIAN_POINT('Ctrl Pts',(-1.30211520951443,4.07950885749352,2.79450148797204));
#8440=CARTESIAN_POINT('Ctrl Pts',(-1.33200746762014,4.08364579895674,2.84406616914074));
#8441=CARTESIAN_POINT('Ctrl Pts',(-1.36188153230805,4.08778022254043,2.89360068360376));
#8442=CARTESIAN_POINT('Ctrl Pts',(-1.38900897537655,4.09191464612413,2.94483740401328));
#8443=CARTESIAN_POINT('Ctrl Pts',(-1.41320106171709,4.09604906970783,2.99743830886872));
#8444=CARTESIAN_POINT('Ctrl Pts',(-1.43738771866766,4.10018256540968,3.05002740858999));
#8445=CARTESIAN_POINT('Ctrl Pts',(-1.45864010930288,4.10431606111152,3.103979612102));
#8446=CARTESIAN_POINT('Ctrl Pts',(-1.47681655061521,4.10844955681337,3.15893451513622));
#8447=CARTESIAN_POINT('Ctrl Pts',(-1.49500940507868,4.11258678502195,3.2139390419177));
#8448=CARTESIAN_POINT('Ctrl Pts',(-1.51012059463379,4.11672401323054,3.26994758241586));
#8449=CARTESIAN_POINT('Ctrl Pts',(-1.52205797546509,4.12086124143913,3.32658335668842));
#8450=CARTESIAN_POINT('Ctrl Pts',(-1.53400030019751,4.12500018309285,3.3832425868322));
#8451=CARTESIAN_POINT('Ctrl Pts',(-1.5427661155984,4.12913912474657,3.44052905299625));
#8452=CARTESIAN_POINT('Ctrl Pts',(-1.54831482273191,4.1332780664003,3.49805773566704));
#8453=CARTESIAN_POINT('Ctrl Pts',(-1.55387431497743,4.13742505298202,3.55569823777111));
#8454=CARTESIAN_POINT('Ctrl Pts',(-1.55620418080109,4.14157203956375,3.61358137509542));
#8455=CARTESIAN_POINT('Ctrl Pts',(-1.55531598818641,4.14571902614547,3.67131991272537));
#8456=CARTESIAN_POINT('Ctrl Pts',(-1.55448247363523,4.14961071990907,3.72550400577358));
#8457=CARTESIAN_POINT('Ctrl Pts',(-1.55081545093387,4.15350241367267,3.77956041061299));
#8458=CARTESIAN_POINT('Ctrl Pts',(-1.5443658084111,4.15739410743627,3.83317525257204));
#8459=CARTESIAN_POINT('Ctrl Pts',(-1.53749069896047,4.16154252658953,3.89032693273814));
#8460=CARTESIAN_POINT('Ctrl Pts',(-1.52742442723014,4.16569094574279,3.94721615662609));
#8461=CARTESIAN_POINT('Ctrl Pts',(-1.51419888969869,4.16983936489604,4.00345903045659));
#8462=CARTESIAN_POINT('Ctrl Pts',(-1.50099682699795,4.17398042076163,4.05960207530557));
#8463=CARTESIAN_POINT('Ctrl Pts',(-1.48464674700967,4.17812147662723,4.115100544536));
#8464=CARTESIAN_POINT('Ctrl Pts',(-1.46523204945129,4.18226253249282,4.16957766531415));
#8465=CARTESIAN_POINT('Ctrl Pts',(-1.44583662773766,4.18639947691915,4.22400069858879));
#8466=CARTESIAN_POINT('Ctrl Pts',(-1.42338279090196,4.19053642134547,4.27740390454189));
#8467=CARTESIAN_POINT('Ctrl Pts',(-1.39800409065944,4.19467336577179,4.32942438881484));
#8468=CARTESIAN_POINT('Ctrl Pts',(-1.37264083652224,4.19880779235131,4.38141321213309));
#8469=CARTESIAN_POINT('Ctrl Pts',(-1.34435647560062,4.20294221893083,4.43202051497412));
#8470=CARTESIAN_POINT('Ctrl Pts',(-1.31333230115958,4.20707664551035,4.48090422631367));
#8471=CARTESIAN_POINT('Ctrl Pts',(-1.28231508921055,4.21121014423562,4.529776967097));
#8472=CARTESIAN_POINT('Ctrl Pts',(-1.24855956333046,4.21534364296089,4.57692644490255));
#8473=CARTESIAN_POINT('Ctrl Pts',(-1.21229136733349,4.21947714168616,4.62203793678336));
#8474=CARTESIAN_POINT('Ctrl Pts',(-1.1759904213609,4.22361437293737,4.66719016408588));
#8475=CARTESIAN_POINT('Ctrl Pts',(-1.13717259725465,4.22775160418858,4.71030032036805));
#8476=CARTESIAN_POINT('Ctrl Pts',(-1.09610419663964,4.2318888354398,4.75108638186709));
#8477=CARTESIAN_POINT('Ctrl Pts',(-1.0550187872851,4.23602778015166,4.7918893351731));
#8478=CARTESIAN_POINT('Ctrl Pts',(-1.01168133261275,4.24016672486353,4.83036592741652));
#8479=CARTESIAN_POINT('Ctrl Pts',(-0.96639305027996,4.2443056695754,4.86627293735722));
#8480=CARTESIAN_POINT('Ctrl Pts',(-0.921016740592843,4.24845265920163,4.9022497401654));
#8481=CARTESIAN_POINT('Ctrl Pts',(-0.873682452134067,4.25259964882785,4.93564667763783));
#8482=CARTESIAN_POINT('Ctrl Pts',(-0.824721598466733,4.25674663845408,4.96626312551342));
#8483=CARTESIAN_POINT('Ctrl Pts',(-0.778775142055082,4.26063830830517,4.99499459529852));
#8484=CARTESIAN_POINT('Ctrl Pts',(-0.731396819639847,4.26452997815626,5.02127767127383));
#8485=CARTESIAN_POINT('Ctrl Pts',(-0.682877801894672,4.26842164800735,5.04498459334898));
#8486=CARTESIAN_POINT('Ctrl Pts',(-0.631157796762294,4.27257006638072,5.07025555282798));
#8487=CARTESIAN_POINT('Ctrl Pts',(-0.577924791530158,4.27671848475409,5.09270459408808));
#8488=CARTESIAN_POINT('Ctrl Pts',(-0.523518435833301,4.28086690312746,5.11214997598564));
#8489=CARTESIAN_POINT('Ctrl Pts',(-0.469208649529518,4.2850079582022,5.13156084300522));
#8490=CARTESIAN_POINT('Ctrl Pts',(-0.413730132841114,4.28914901327694,5.14797845897071));
#8491=CARTESIAN_POINT('Ctrl Pts',(-0.357444531875422,4.29329006835168,5.16126819374196));
#8492=CARTESIAN_POINT('Ctrl Pts',(-0.301214814053124,4.29742701198103,5.17454473380371));
#8493=CARTESIAN_POINT('Ctrl Pts',(-0.24418010380913,4.30156395561038,5.18469942661238));
#8494=CARTESIAN_POINT('Ctrl Pts',(-0.186717636011615,4.30570089923973,5.19164728903643));
#8495=CARTESIAN_POINT('Ctrl Pts',(-0.129290141367093,4.30983532501754,5.19859092281064));
#8496=CARTESIAN_POINT('Ctrl Pts',(-0.0714359211261828,4.31396975079536,
5.20233153280199));
#8497=CARTESIAN_POINT('Ctrl Pts',(-0.013540658583629,4.31810417657318,5.20283553131555));
#8498=CARTESIAN_POINT('Ctrl Pts',(0.044341610967578,4.32223767449342,5.20333941672058));
#8499=CARTESIAN_POINT('Ctrl Pts',(0.102264384113867,4.32637117241365,5.20060812818138));
#8500=CARTESIAN_POINT('Ctrl Pts',(0.159840849344005,4.33050467033389,5.19466017037934));
#8501=CARTESIAN_POINT('Ctrl Pts',(0.21746930582411,4.33464190078135,5.1887068416022));
#8502=CARTESIAN_POINT('Ctrl Pts',(0.274750310160414,4.3387791312288,5.17953109150457));
#8503=CARTESIAN_POINT('Ctrl Pts',(0.331302421324793,4.34291636167625,5.167203323247));
#8504=CARTESIAN_POINT('Ctrl Pts',(0.387877953901925,4.34705530558374,5.15487044936662));
#8505=CARTESIAN_POINT('Ctrl Pts',(0.443723488319045,4.35119424949122,5.13938309309894));
#8506=CARTESIAN_POINT('Ctrl Pts',(0.498471197309759,4.3553331933987,5.12086205036791));
#8507=CARTESIAN_POINT('Ctrl Pts',(0.553325320197712,4.35948018223007,5.10230500802385));
#8508=CARTESIAN_POINT('Ctrl Pts',(0.607076868142722,4.36362717106143,5.0807026894981));
#8509=CARTESIAN_POINT('Ctrl Pts',(0.659377377398335,4.3677741598928,5.05622438142999));
#8510=CARTESIAN_POINT('Ctrl Pts',(0.708457964997536,4.37166583612134,5.0332530994957));
#8511=CARTESIAN_POINT('Ctrl Pts',(0.756260586977096,4.37555751234989,5.00774967826566));
#8512=CARTESIAN_POINT('Ctrl Pts',(0.80251981524134,4.37944918857843,4.97988919478188));
#8513=CARTESIAN_POINT('Ctrl Pts',(0.851830855280501,4.38359760630016,4.95019070070559));
#8514=CARTESIAN_POINT('Ctrl Pts',(0.899594386513453,4.3877460240219,4.91768906526787));
#8515=CARTESIAN_POINT('Ctrl Pts',(0.945473326109702,4.39189444174363,4.88257074704535));
#8516=CARTESIAN_POINT('Ctrl Pts',(0.99127083205346,4.39603549615641,4.84751476271606));
#8517=CARTESIAN_POINT('Ctrl Pts',(1.03518997586039,4.40017655056918,4.80985162826572));
#8518=CARTESIAN_POINT('Ctrl Pts',(1.07692128200614,4.40431760498195,4.76981186050578));
#8519=CARTESIAN_POINT('Ctrl Pts',(1.11861115517062,4.40845454794349,4.72981184628105));
#8520=CARTESIAN_POINT('Ctrl Pts',(1.15811712064237,4.41259149090503,4.68744023260774));
#8521=CARTESIAN_POINT('Ctrl Pts',(1.19516291999959,4.41672843386657,4.64296759199607));
#8522=CARTESIAN_POINT('Ctrl Pts',(1.23218617227358,4.42086285897187,4.59852201864564));
#8523=CARTESIAN_POINT('Ctrl Pts',(1.26675189399722,4.42499728407717,4.55197835246778));
#8524=CARTESIAN_POINT('Ctrl Pts',(1.29862239032697,4.42913170918246,4.50364217621742));
#8525=CARTESIAN_POINT('Ctrl Pts',(1.33048573417583,4.43326520642657,4.45531684772963));
#8526=CARTESIAN_POINT('Ctrl Pts',(1.35965476700255,4.43739870367068,4.40520024231475));
#8527=CARTESIAN_POINT('Ctrl Pts',(1.38593491887229,4.44153220091479,4.35362718534706));
#8528=CARTESIAN_POINT('Ctrl Pts',(1.41223880158493,4.4456694306858,4.30200755817238));
#8529=CARTESIAN_POINT('Ctrl Pts',(1.4356483522893,4.4498066604568,4.248929315779));
#8530=CARTESIAN_POINT('Ctrl Pts',(1.4560154931007,4.45394389022781,4.19475096440931));
#8531=CARTESIAN_POINT('Ctrl Pts',(1.47639106908664,4.45808283345754,4.14055017474775));
#8532=CARTESIAN_POINT('Ctrl Pts',(1.49372156596716,4.46222177668727,4.08524886536955));
#8533=CARTESIAN_POINT('Ctrl Pts',(1.50790861123547,4.46636071991701,4.02922148430278));
#8534=CARTESIAN_POINT('Ctrl Pts',(1.52212323209167,4.47050770807722,3.97308520191503));
#8535=CARTESIAN_POINT('Ctrl Pts',(1.53318209055855,4.47465469623742,3.91622054035924));
#8536=CARTESIAN_POINT('Ctrl Pts',(1.54103804564486,4.47880168439763,3.85901202869666));
#8537=CARTESIAN_POINT('Ctrl Pts',(1.54841035406551,4.48269336598159,3.80532552112007));
#8538=CARTESIAN_POINT('Ctrl Pts',(1.55296246258241,4.48658504756555,3.75133661842237));
#8539=CARTESIAN_POINT('Ctrl Pts',(1.55469719497037,4.49047672914951,3.6973632780683));
#8540=CARTESIAN_POINT('Ctrl Pts',(1.55522905318279,4.49166989463424,3.68081538600244));
#8541=CARTESIAN_POINT('Ctrl Pts',(1.55549672149285,4.49286306011897,3.66425895728588));
#8542=CARTESIAN_POINT('Ctrl Pts',(1.5554999700677,4.4940562256037,3.64769962294641));
#8543=CARTESIAN_POINT('Ctrl Pts',(1.55549987088463,3.65467159675291,3.64802824892935));
#8544=CARTESIAN_POINT('Ctrl Pts',(1.55550680899066,3.6558397976945,3.63099992358026));
#8545=CARTESIAN_POINT('Ctrl Pts',(1.55523412898573,3.65701542995216,3.61397308773208));
#8546=CARTESIAN_POINT('Ctrl Pts',(1.55413408026995,3.65937408981715,3.58006687167519));
#8547=CARTESIAN_POINT('Ctrl Pts',(1.55331107084226,3.66055682043176,3.56318981869217));
#8548=CARTESIAN_POINT('Ctrl Pts',(1.55069027106267,3.66340087943599,3.52293785225933));
#8549=CARTESIAN_POINT('Ctrl Pts',(1.5486386943779,3.66506974526968,3.49958428363513));
#8550=CARTESIAN_POINT('Ctrl Pts',(1.54262409405456,3.66900197693008,3.44523866763588));
#8551=CARTESIAN_POINT('Ctrl Pts',(1.53825361546319,3.67127758602551,3.41430303623448));
#8552=CARTESIAN_POINT('Ctrl Pts',(1.51028537399236,3.68343974554108,3.25182285702067));
#8553=CARTESIAN_POINT('Ctrl Pts',(1.47074125747952,3.69383819776969,3.12361475845923));
#8554=CARTESIAN_POINT('Ctrl Pts',(1.39151303190329,3.70859912506545,2.94985225609737));
#8555=CARTESIAN_POINT('Ctrl Pts',(1.36483055976558,3.71299964536092,2.89898780474795));
#8556=CARTESIAN_POINT('Ctrl Pts',(1.32549190967572,3.71871027510865,2.83313138202807));
#8557=CARTESIAN_POINT('Ctrl Pts',(1.31528024997209,3.72013282285924,2.81673741705178));
#8558=CARTESIAN_POINT('Ctrl Pts',(1.2966262245711,3.7226228050478,2.78799690110064));
#8559=CARTESIAN_POINT('Ctrl Pts',(1.28830732785269,3.72369706600524,2.77557567591207));
#8560=CARTESIAN_POINT('Ctrl Pts',(1.26719687946834,3.72633755331549,2.74501720118994));
#8561=CARTESIAN_POINT('Ctrl Pts',(1.25419411705297,3.72789032617511,2.72703045520652));
#8562=CARTESIAN_POINT('Ctrl Pts',(1.19592062594428,3.73456811992015,2.64995036594936));
#8563=CARTESIAN_POINT('Ctrl Pts',(1.14682172558588,3.73949171494677,2.59386547306114));
#8564=CARTESIAN_POINT('Ctrl Pts',(1.0425410697477,3.7491572560565,2.49071611753265));
#8565=CARTESIAN_POINT('Ctrl Pts',(0.987719652740954,3.75388941824133,2.44356475363856));
#8566=CARTESIAN_POINT('Ctrl Pts',(0.901121842986846,3.76113182859896,2.37899336284216));
#8567=CARTESIAN_POINT('Ctrl Pts',(0.871692903772833,3.76355595621517,2.35859147991404));
#8568=CARTESIAN_POINT('Ctrl Pts',(0.814750259645494,3.76820638574019,2.32195845638407));
#8569=CARTESIAN_POINT('Ctrl Pts',(0.787389467575394,3.77042440273263,2.30552406392175));
#8570=CARTESIAN_POINT('Ctrl Pts',(0.736979070458522,3.77449557003692,2.27731757093331));
#8571=CARTESIAN_POINT('Ctrl Pts',(0.714103896334424,3.77633744759335,2.26525687274253));
#8572=CARTESIAN_POINT('Ctrl Pts',(0.662031327540791,3.78052407799057,2.23943995787138));
#8573=CARTESIAN_POINT('Ctrl Pts',(0.632685878936297,3.78287931487906,2.22601145424455));
#8574=CARTESIAN_POINT('Ctrl Pts',(0.485608225534339,3.79467579654246,2.16416571683604));
#8575=CARTESIAN_POINT('Ctrl Pts',(0.362675252472724,3.80456766130157,2.12942285856927));
#8576=CARTESIAN_POINT('Ctrl Pts',(0.177330195496293,3.81907447215376,2.10085992851241));
#8577=CARTESIAN_POINT('Ctrl Pts',(0.117254235714492,3.82370504365851,2.09514835401264));
#8578=CARTESIAN_POINT('Ctrl Pts',(0.037506588442317,3.82964856040533,2.09222446656055));
#8579=CARTESIAN_POINT('Ctrl Pts',(0.0180072309046056,3.83108561643035,2.09187644622304));
#8580=CARTESIAN_POINT('Ctrl Pts',(-0.0164270910425457,3.8335889385491,2.09190953556467));
#8581=CARTESIAN_POINT('Ctrl Pts',(-0.0313576239195812,3.83466241648109,
2.09213887509024));
#8582=CARTESIAN_POINT('Ctrl Pts',(-0.0682069141322419,3.83728434998413,
2.0932358269107));
#8583=CARTESIAN_POINT('Ctrl Pts',(-0.0901145359935279,3.83881988654501,
2.09435204504922));
#8584=CARTESIAN_POINT('Ctrl Pts',(-0.215852175537578,3.84753727450119,2.10342844313732));
#8585=CARTESIAN_POINT('Ctrl Pts',(-0.318709908064491,3.85430539505901,2.12133652219782));
#8586=CARTESIAN_POINT('Ctrl Pts',(-0.490423267156545,3.86606195438738,2.16936768880608));
#8587=CARTESIAN_POINT('Ctrl Pts',(-0.560303712190142,3.87098351014319,2.19441950024454));
#8588=CARTESIAN_POINT('Ctrl Pts',(-0.658944774022162,3.87836259443022,2.23795954717942));
#8589=CARTESIAN_POINT('Ctrl Pts',(-0.689310208044195,3.88069634274766,2.25255893699465));
#8590=CARTESIAN_POINT('Ctrl Pts',(-0.74214737817428,3.88488549146296,2.28010932246865));
#8591=CARTESIAN_POINT('Ctrl Pts',(-0.764814597393762,3.88672620365825,2.29265837394572));
#8592=CARTESIAN_POINT('Ctrl Pts',(-0.813669412320802,3.89079627301213,2.32132236129594));
#8593=CARTESIAN_POINT('Ctrl Pts',(-0.839713288787418,3.89303318337717,2.33765919423326));
#8594=CARTESIAN_POINT('Ctrl Pts',(-0.975481178202155,3.90507091660595,2.42853824264552));
#8595=CARTESIAN_POINT('Ctrl Pts',(-1.07579959823294,3.91537836815593,2.51610516441592));
#8596=CARTESIAN_POINT('Ctrl Pts',(-1.20329253551976,3.93023958039282,2.6598648928988));
#8597=CARTESIAN_POINT('Ctrl Pts',(-1.24022315403323,3.93481226237697,2.70666307428755));
#8598=CARTESIAN_POINT('Ctrl Pts',(-1.28553665769892,3.94069738495624,2.77140690163983));
#8599=CARTESIAN_POINT('Ctrl Pts',(-1.29639246572693,3.94213095783939,2.78755414106259));
#8600=CARTESIAN_POINT('Ctrl Pts',(-1.31504202698694,3.94463099181762,2.81645055925579));
#8601=CARTESIAN_POINT('Ctrl Pts',(-1.32295931239141,3.94570457421527,2.82911456180254));
#8602=CARTESIAN_POINT('Ctrl Pts',(-1.34208104326949,3.94833055590119,2.86070376855965));
#8603=CARTESIAN_POINT('Ctrl Pts',(-1.35306867879817,3.94986991580466,2.87975583757072));
#8604=CARTESIAN_POINT('Ctrl Pts',(-1.40379912232057,3.95716047724157,2.97219618430925));
#8605=CARTESIAN_POINT('Ctrl Pts',(-1.43800116895929,3.96265200893646,3.04847820183888));
#8606=CARTESIAN_POINT('Ctrl Pts',(-1.48831473982958,3.97255653176303,3.19024780674943));
#8607=CARTESIAN_POINT('Ctrl Pts',(-1.50661116414808,3.97695707524957,3.25472924498367));
#8608=CARTESIAN_POINT('Ctrl Pts',(-1.53066914784216,3.98463974755485,3.36653822113338));
#8609=CARTESIAN_POINT('Ctrl Pts',(-1.53851744739748,3.98786841186561,3.41331832020172));
#8610=CARTESIAN_POINT('Ctrl Pts',(-1.54754519080994,3.99308676380265,3.48786243751191));
#8611=CARTESIAN_POINT('Ctrl Pts',(-1.55013900021884,3.9950318376677,3.51542669523067));
#8612=CARTESIAN_POINT('Ctrl Pts',(-1.5537959718898,3.99890865359388,3.5698165285004));
#8613=CARTESIAN_POINT('Ctrl Pts',(-1.55490289421904,4.0008383074917,3.59662950069242));
#8614=CARTESIAN_POINT('Ctrl Pts',(-1.55595583761273,4.0058148796882,3.66504128398195));
#8615=CARTESIAN_POINT('Ctrl Pts',(-1.55492777078369,4.00889081730036,3.70663136778312));
#8616=CARTESIAN_POINT('Ctrl Pts',(-1.5451581658646,4.02021507583114,3.85717591500449));
#8617=CARTESIAN_POINT('Ctrl Pts',(-1.52661002056277,4.02872846159367,3.96516491297883));
#8618=CARTESIAN_POINT('Ctrl Pts',(-1.48123288127581,4.0416298553189,4.12578027454459));
#8619=CARTESIAN_POINT('Ctrl Pts',(-1.46248512658164,4.04605113103239,4.18035078001403));
#8620=CARTESIAN_POINT('Ctrl Pts',(-1.43346189450557,4.05178295040139,4.25166337019466));
#8621=CARTESIAN_POINT('Ctrl Pts',(-1.42584152590385,4.05320695329046,4.269431403307));
#8622=CARTESIAN_POINT('Ctrl Pts',(-1.41174427596951,4.05569830103502,4.30067986094912));
#8623=CARTESIAN_POINT('Ctrl Pts',(-1.40540142053742,4.05677251003103,4.31421572277038));
#8624=CARTESIAN_POINT('Ctrl Pts',(-1.38916956655271,4.05941129017011,4.34759409175537));
#8625=CARTESIAN_POINT('Ctrl Pts',(-1.37904990282173,4.06096245831637,4.3673202275207));
#8626=CARTESIAN_POINT('Ctrl Pts',(-1.33258346637689,4.06771803553351,4.45331867323996));
#8627=CARTESIAN_POINT('Ctrl Pts',(-1.29185274846998,4.07271401779846,4.51711374837089));
#8628=CARTESIAN_POINT('Ctrl Pts',(-1.20385374876466,4.0824082992758,4.63503528730362));
#8629=CARTESIAN_POINT('Ctrl Pts',(-1.15716490630667,4.0870973463686,4.68934792617555));
#8630=CARTESIAN_POINT('Ctrl Pts',(-1.08186035945384,4.0942852276056,4.76562036350572));
#8631=CARTESIAN_POINT('Ctrl Pts',(-1.05595219040463,4.09669956078723,4.7901173942015));
#8632=CARTESIAN_POINT('Ctrl Pts',(-1.00536851711708,4.10133405586616,4.83475578174981));
#8633=CARTESIAN_POINT('Ctrl Pts',(-0.980871428792829,4.10354607254253,4.85507146753244));
#8634=CARTESIAN_POINT('Ctrl Pts',(-0.935369985281544,4.10761129536025,4.89050822931024));
#8635=CARTESIAN_POINT('Ctrl Pts',(-0.914578126148144,4.1094534041472,4.90588385487769));
#8636=CARTESIAN_POINT('Ctrl Pts',(-0.866924244355616,4.11364728350535,4.93931928796561));
#8637=CARTESIAN_POINT('Ctrl Pts',(-0.839863119069813,4.11600971701675,4.95707268674787));
#8638=CARTESIAN_POINT('Ctrl Pts',(-0.704269964341053,4.12776720776442,5.04009727419382));
#8639=CARTESIAN_POINT('Ctrl Pts',(-0.588614722709753,4.13760696901563,5.0927796949871));
#8640=CARTESIAN_POINT('Ctrl Pts',(-0.410052301755297,4.15209204024159,5.14909841878631));
#8641=CARTESIAN_POINT('Ctrl Pts',(-0.351195803165076,4.15675058905869,5.16394339408206));
#8642=CARTESIAN_POINT('Ctrl Pts',(-0.272443798948656,4.16272218540384,5.17897392928248));
#8643=CARTESIAN_POINT('Ctrl Pts',(-0.253201732900101,4.16416081350884,5.1822723952049));
#8644=CARTESIAN_POINT('Ctrl Pts',(-0.219141589904982,4.16666552363155,5.1874529435621));
#8645=CARTESIAN_POINT('Ctrl Pts',(-0.20435098522404,4.16773886117158,5.189485209551));
#8646=CARTESIAN_POINT('Ctrl Pts',(-0.167793747187085,4.17035850698453,5.19397300024505));
#8647=CARTESIAN_POINT('Ctrl Pts',(-0.146000645682202,4.17189195897003,5.19618232992627));
#8648=CARTESIAN_POINT('Ctrl Pts',(-0.0201587373251121,4.18062243716555,
5.20625972862682));
#8649=CARTESIAN_POINT('Ctrl Pts',(0.084436912459217,4.18740359634424,5.20410360241846));
#8650=CARTESIAN_POINT('Ctrl Pts',(0.261661543953308,4.19917557832372,5.18252119934605));
#8651=CARTESIAN_POINT('Ctrl Pts',(0.334540989733795,4.20409875308634,5.16830259511418));
#8652=CARTESIAN_POINT('Ctrl Pts',(0.438580618066137,4.21147563304065,5.14016296928541));
#8653=CARTESIAN_POINT('Ctrl Pts',(0.470741964500938,4.21380525218522,5.13033494943017));
#8654=CARTESIAN_POINT('Ctrl Pts',(0.527071454822894,4.21799003989888,5.1111044438017));
#8655=CARTESIAN_POINT('Ctrl Pts',(0.55137089440572,4.21983064183916,5.10212509645768));
#8656=CARTESIAN_POINT('Ctrl Pts',(0.604033807235616,4.22390400242875,5.08115563162026));
#8657=CARTESIAN_POINT('Ctrl Pts',(0.632287646929645,4.22614440236699,5.06892181386107));
#8658=CARTESIAN_POINT('Ctrl Pts',(0.77945934922997,4.23812145992238,4.99994128604665));
#8659=CARTESIAN_POINT('Ctrl Pts',(0.891152971316397,4.24835666459975,4.9291013957991));
#8660=CARTESIAN_POINT('Ctrl Pts',(1.0389128326723,4.26320164283447,4.8066462636505));
#8661=CARTESIAN_POINT('Ctrl Pts',(1.08300182460194,4.26782534952738,4.76556847845488));
#8662=CARTESIAN_POINT('Ctrl Pts',(1.13806943313459,4.27376189484348,4.70794065377763));
#8663=CARTESIAN_POINT('Ctrl Pts',(1.15127156698475,4.27519850063877,4.69359431729372));
#8664=CARTESIAN_POINT('Ctrl Pts',(1.17410413686256,4.27770133638679,4.66782706550215));
#8665=CARTESIAN_POINT('Ctrl Pts',(1.18384496852464,4.27877476820537,4.6565100888032));
#8666=CARTESIAN_POINT('Ctrl Pts',(1.20518276318679,4.28114087800315,4.63098531790373));
#8667=CARTESIAN_POINT('Ctrl Pts',(1.21669392899843,4.28242797244065,4.6167099041841));
#8668=CARTESIAN_POINT('Ctrl Pts',(1.29072584311944,4.29080267171439,4.52150271466707));
#8669=CARTESIAN_POINT('Ctrl Pts',(1.345395616747,4.29746748967359,4.43476660068687));
#8670=CARTESIAN_POINT('Ctrl Pts',(1.42707242919979,4.30949517736764,4.27148493600972));
#8671=CARTESIAN_POINT('Ctrl Pts',(1.45737082104823,4.31481006451829,4.19702433963266));
#8672=CARTESIAN_POINT('Ctrl Pts',(1.49195467811449,4.32259461685936,4.08872067062043));
#8673=CARTESIAN_POINT('Ctrl Pts',(1.50109295279395,4.32491140714319,4.05656098880325));
#8674=CARTESIAN_POINT('Ctrl Pts',(1.51545879030476,4.32908270041734,3.9990125973105));
#8675=CARTESIAN_POINT('Ctrl Pts',(1.52110124708772,4.33092301439652,3.97374014819926));
#8676=CARTESIAN_POINT('Ctrl Pts',(1.53209368873156,4.33500692163563,3.91799691542918));
#8677=CARTESIAN_POINT('Ctrl Pts',(1.53717057127463,4.33725843599311,3.88748431756648));
#8678=CARTESIAN_POINT('Ctrl Pts',(1.55076865302059,4.34470269924416,3.78741568145517));
#8679=CARTESIAN_POINT('Ctrl Pts',(1.55550000000259,4.35000710688228,3.71744083094467));
#8680=CARTESIAN_POINT('Ctrl Pts',(1.5555,4.35539415465377,3.64739446822635));
#8681=CARTESIAN_POINT('Origin',(-2.67773308947627E-16,1.2059437743963,3.64739446828387));
#8682=CARTESIAN_POINT('',(1.55549955406273,5.19405622556279,3.64857230980728));
#8683=CARTESIAN_POINT('',(1.5554999873946,5.05594377443822,3.64759249708933));
#8684=CARTESIAN_POINT('',(1.5555,1.2059437743963,3.64739446828386));
#8685=CARTESIAN_POINT('Ctrl Pts',(1.55549997006787,4.49405622566528,3.64769962209176));
#8686=CARTESIAN_POINT('Ctrl Pts',(1.5555112048523,4.49818264884198,3.59043110243972));
#8687=CARTESIAN_POINT('Ctrl Pts',(1.55235548796176,4.50230907201867,3.53303695693616));
#8688=CARTESIAN_POINT('Ctrl Pts',(1.54601728863953,4.50643549519536,3.47589871548611));
#8689=CARTESIAN_POINT('Ctrl Pts',(1.53969015520276,4.51055471403468,3.41886023190156));
#8690=CARTESIAN_POINT('Ctrl Pts',(1.53019162173891,4.514673932874,3.36207728507753));
#8691=CARTESIAN_POINT('Ctrl Pts',(1.51755815074409,4.51879315171333,3.30593069405566));
#8692=CARTESIAN_POINT('Ctrl Pts',(1.50493690032262,4.52290838596156,3.24983841459505));
#8693=CARTESIAN_POINT('Ctrl Pts',(1.48918683358188,4.52702362020979,3.19438178319573));
#8694=CARTESIAN_POINT('Ctrl Pts',(1.47039588386746,4.53113885445802,3.13993393316253));
#8695=CARTESIAN_POINT('Ctrl Pts',(1.45161569328146,4.53525173244781,3.08551725831847));
#8696=CARTESIAN_POINT('Ctrl Pts',(1.429798241767,4.53936461043761,3.03210871724348));
#8697=CARTESIAN_POINT('Ctrl Pts',(1.40508135769004,4.5434774884274,2.98006649174466));
#8698=CARTESIAN_POINT('Ctrl Pts',(1.38036886934147,4.54758963497004,2.92803352159889));
#8699=CARTESIAN_POINT('Ctrl Pts',(1.35275819858074,4.55170178151267,2.87736686006049));
#8700=CARTESIAN_POINT('Ctrl Pts',(1.32243444548008,4.55581392805531,2.8284027788219));
#8701=CARTESIAN_POINT('Ctrl Pts',(1.29208256946628,4.55992988829277,2.77939328722135));
#8702=CARTESIAN_POINT('Ctrl Pts',(1.25901286363791,4.56404584853022,2.73208997848173));
#8703=CARTESIAN_POINT('Ctrl Pts',(1.22345458874833,4.56816180876768,2.68680136021435));
#8704=CARTESIAN_POINT('Ctrl Pts',(1.18787941608737,4.5722797249649,2.64149122018531));
#8705=CARTESIAN_POINT('Ctrl Pts',(1.14981366757703,4.57639764116212,2.5981980734549));
#8706=CARTESIAN_POINT('Ctrl Pts',(1.10952573337371,4.58051555735934,2.55719590977192));
#8707=CARTESIAN_POINT('Ctrl Pts',(1.06916306124129,4.58464111268065,2.5161176831966));
#8708=CARTESIAN_POINT('Ctrl Pts',(1.02657036213311,4.58876666800197,2.47733928112318));
#8709=CARTESIAN_POINT('Ctrl Pts',(0.982050677732466,4.59289222332328,2.44109570082814));
#8710=CARTESIAN_POINT('Ctrl Pts',(0.951072578398685,4.59576290545572,2.41587635694225));
#8711=CARTESIAN_POINT('Ctrl Pts',(0.919162176237059,4.59863358758815,2.39188346783218));
#8712=CARTESIAN_POINT('Ctrl Pts',(0.886429325065603,4.60150426972059,2.36918349130717));
#8713=CARTESIAN_POINT('Ctrl Pts',(0.839127122506271,4.60565268890353,2.33637978343418));
#8714=CARTESIAN_POINT('Ctrl Pts',(0.789902466076941,4.60980110808647,2.30613665572483));
#8715=CARTESIAN_POINT('Ctrl Pts',(0.739063605726963,4.61394952726941,2.27868513585063));
#8716=CARTESIAN_POINT('Ctrl Pts',(0.688314982571474,4.61809058315376,2.25128234146162));
#8717=CARTESIAN_POINT('Ctrl Pts',(0.635958296846781,4.62223163903811,2.22666156523239));
#8718=CARTESIAN_POINT('Ctrl Pts',(0.582330668195567,4.62637269492246,2.20501059327732));
#8719=CARTESIAN_POINT('Ctrl Pts',(0.528756283717064,4.6305096393609,2.18338111748234));
#8720=CARTESIAN_POINT('Ctrl Pts',(0.473913936833557,4.63464658379933,2.16471579788028));
#8721=CARTESIAN_POINT('Ctrl Pts',(0.418163666519987,4.63878352823777,2.14915570293218));
#8722=CARTESIAN_POINT('Ctrl Pts',(0.362447327290461,4.64291795482277,2.13360507826801));
#8723=CARTESIAN_POINT('Ctrl Pts',(0.305824660527443,4.64705238140778,2.12115607155644));
#8724=CARTESIAN_POINT('Ctrl Pts',(0.248671830850362,4.65118680799278,2.11190022520071));
#8725=CARTESIAN_POINT('Ctrl Pts',(0.191531827588873,4.65532030671693,2.10264645607078));
#8726=CARTESIAN_POINT('Ctrl Pts',(0.133862411373075,4.65945380544108,2.09658450778817));
#8727=CARTESIAN_POINT('Ctrl Pts',(0.0760487419179381,4.66358730416522,2.09375460047258));
#8728=CARTESIAN_POINT('Ctrl Pts',(0.0181828671915226,4.66772453540495,2.09092213777379));
#8729=CARTESIAN_POINT('Ctrl Pts',(-0.0398269998096223,4.67186176664468,
2.09132757497707));
#8730=CARTESIAN_POINT('Ctrl Pts',(-0.0975931575225837,4.67599899788441,
2.09495901854537));
#8731=CARTESIAN_POINT('Ctrl Pts',(-0.155383239378268,4.68013794257913,2.09859196609416));
#8732=CARTESIAN_POINT('Ctrl Pts',(-0.212928892430087,4.68427688727384,2.10545352302032));
#8733=CARTESIAN_POINT('Ctrl Pts',(-0.269848249449828,4.68841583196855,2.11547992358209));
#8734=CARTESIAN_POINT('Ctrl Pts',(-0.326878241148675,4.69256282156823,2.12552581255109));
#8735=CARTESIAN_POINT('Ctrl Pts',(-0.383278995100198,4.69670981116791,2.13874871992923));
#8736=CARTESIAN_POINT('Ctrl Pts',(-0.438680449723717,4.70085680076759,2.15503401818135));
#8737=CARTESIAN_POINT('Ctrl Pts',(-0.490670975608389,4.70474847060895,2.17031667142701));
#8738=CARTESIAN_POINT('Ctrl Pts',(-0.541781273715216,4.7086401404503,2.18829563175241));
#8739=CARTESIAN_POINT('Ctrl Pts',(-0.591722488297608,4.71253181029166,2.20883798804304));
#8740=CARTESIAN_POINT('Ctrl Pts',(-0.644958489593133,4.71668022643349,2.23073559136017));
#8741=CARTESIAN_POINT('Ctrl Pts',(-0.69708881376828,4.72082864257532,2.25563816533533));
#8742=CARTESIAN_POINT('Ctrl Pts',(-0.747752051956195,4.72497705871715,2.28341238673173));
#8743=CARTESIAN_POINT('Ctrl Pts',(-0.798325364621596,4.7291181115616,2.31113730983097));
#8744=CARTESIAN_POINT('Ctrl Pts',(-0.84743630712596,4.73325916440605,2.34172351508062));
#8745=CARTESIAN_POINT('Ctrl Pts',(-0.894744095649219,4.7374002172505,2.37498995190519));
#8746=CARTESIAN_POINT('Ctrl Pts',(-0.942004914647774,4.74153715865178,2.40822336015719));
#8747=CARTESIAN_POINT('Ctrl Pts',(-0.987465702944342,4.74567410005306,2.44413142958445));
#8748=CARTESIAN_POINT('Ctrl Pts',(-1.03081245246944,4.74981104145434,2.48248849017493));
#8749=CARTESIAN_POINT('Ctrl Pts',(-1.07413282008242,4.75394546500998,2.52082220570235));
#8750=CARTESIAN_POINT('Ctrl Pts',(-1.11534131031366,4.75807988856562,2.5616016133837));
#8751=CARTESIAN_POINT('Ctrl Pts',(-1.15415673901441,4.76221431212126,2.60456060242238));
#8752=CARTESIAN_POINT('Ctrl Pts',(-1.19296345675003,4.76634780782886,2.6475099505974));
#8753=CARTESIAN_POINT('Ctrl Pts',(-1.22937783025491,4.77048130353646,2.6926375228735));
#8754=CARTESIAN_POINT('Ctrl Pts',(-1.26315688060045,4.77461479924406,2.73964177895062));
#8755=CARTESIAN_POINT('Ctrl Pts',(-1.29696643353523,4.77875202751135,2.78668848001956));
#8756=CARTESIAN_POINT('Ctrl Pts',(-1.32813560223634,4.78288925577863,2.83561482825171));
#8757=CARTESIAN_POINT('Ctrl Pts',(-1.35646378270186,4.78702648404592,2.88608884225832));
#8758=CARTESIAN_POINT('Ctrl Pts',(-1.38480369556457,4.79116542578737,2.93658376057894));
#8759=CARTESIAN_POINT('Ctrl Pts',(-1.41030004380524,4.79530436752882,2.98862715446294));
#8760=CARTESIAN_POINT('Ctrl Pts',(-1.4327989453742,4.79944330927028,3.04186376540037));
#8761=CARTESIAN_POINT('Ctrl Pts',(-1.45534157868286,4.80359029598771,3.09520385381669));
#8762=CARTESIAN_POINT('Ctrl Pts',(-1.474874945188,4.80773728270515,3.14974130245472));
#8763=CARTESIAN_POINT('Ctrl Pts',(-1.49129427990586,4.81188426942259,3.20510313814041));
#8764=CARTESIAN_POINT('Ctrl Pts',(-1.50670282295054,4.81577596323597,3.25705684045867));
#8765=CARTESIAN_POINT('Ctrl Pts',(-1.51936934366869,4.81966765704936,3.30973606651612));
#8766=CARTESIAN_POINT('Ctrl Pts',(-1.529248536561,4.82355935086274,3.36282608735225));
#8767=CARTESIAN_POINT('Ctrl Pts',(-1.53977943481766,4.82770776987243,3.41941832256457));
#8768=CARTESIAN_POINT('Ctrl Pts',(-1.54718672201664,4.83185618888211,3.47671443938883));
#8769=CARTESIAN_POINT('Ctrl Pts',(-1.55138603020248,4.8360046078918,3.53433857373343));
#8770=CARTESIAN_POINT('Ctrl Pts',(-1.55557788472731,4.84014566356742,3.59186042676303));
#8771=CARTESIAN_POINT('Ctrl Pts',(-1.55657302470185,4.84428671924304,3.64970862663675));
#8772=CARTESIAN_POINT('Ctrl Pts',(-1.55433835797629,4.84842777491866,3.70749870210799));
#8773=CARTESIAN_POINT('Ctrl Pts',(-1.55210590995044,4.85256471912704,3.7652314004221));
#8774=CARTESIAN_POINT('Ctrl Pts',(-1.54665002876785,4.85670166333542,3.82290557099127));
#8775=CARTESIAN_POINT('Ctrl Pts',(-1.53798962954333,4.8608386075438,3.88013498778397));
#8776=CARTESIAN_POINT('Ctrl Pts',(-1.52933450130965,4.86497303387807,3.93732957295701));
#8777=CARTESIAN_POINT('Ctrl Pts',(-1.51747879900516,4.86910746021233,3.99407942716118));
#8778=CARTESIAN_POINT('Ctrl Pts',(-1.50249322175679,4.87324188654659,4.05000391747117));
#8779=CARTESIAN_POINT('Ctrl Pts',(-1.48751100769123,4.87737538499991,4.10591585676088));
#8780=CARTESIAN_POINT('Ctrl Pts',(-1.46940044792973,4.88150888345323,4.16100229719957));
#8781=CARTESIAN_POINT('Ctrl Pts',(-1.44828274104248,4.88564238190655,4.21489543920681));
#8782=CARTESIAN_POINT('Ctrl Pts',(-1.42714596518474,4.88977961284657,4.26883724590764));
#8783=CARTESIAN_POINT('Ctrl Pts',(-1.40299680515486,4.89391684378659,4.32158311447313));
#8784=CARTESIAN_POINT('Ctrl Pts',(-1.37600503548616,4.89805407472661,4.3727842892193));
#8785=CARTESIAN_POINT('Ctrl Pts',(-1.34900208714668,4.90219301910532,4.42400666898771));
#8786=CARTESIAN_POINT('Ctrl Pts',(-1.31915444986938,4.90633196348404,4.47368263163852));
#8787=CARTESIAN_POINT('Ctrl Pts',(-1.28667682036272,4.91047090786275,4.52149000650683));
#8788=CARTESIAN_POINT('Ctrl Pts',(-1.25413606396406,4.9146178971234,4.56939030475151));
#8789=CARTESIAN_POINT('Ctrl Pts',(-1.21895541635321,4.91876488638404,4.61541434136025));
#8790=CARTESIAN_POINT('Ctrl Pts',(-1.18139112704005,4.92291187564469,4.65927156306913));
#8791=CARTESIAN_POINT('Ctrl Pts',(-1.1461395550944,4.9268035475744,4.70042863098323));
#8792=CARTESIAN_POINT('Ctrl Pts',(-1.10878944216815,4.93069521950411,4.73967755409274));
#8793=CARTESIAN_POINT('Ctrl Pts',(-1.06958042727821,4.93458689143382,4.77680934315642));
#8794=CARTESIAN_POINT('Ctrl Pts',(-1.02778460459304,4.93873531572807,4.81639089541027));
#8795=CARTESIAN_POINT('Ctrl Pts',(-0.983701114049857,4.94288374002232,4.85373212912806));
#8796=CARTESIAN_POINT('Ctrl Pts',(-0.937599712680937,4.94703216431657,4.88855804685868));
#8797=CARTESIAN_POINT('Ctrl Pts',(-0.891580139198416,4.95117322534676,4.92332215017249));
#8798=CARTESIAN_POINT('Ctrl Pts',(-0.843550176143913,4.95531428637694,4.95557948781596));
#8799=CARTESIAN_POINT('Ctrl Pts',(-0.79381465899519,4.95945534740713,4.9850934393399));
#8800=CARTESIAN_POINT('Ctrl Pts',(-0.74412852146618,4.96359229700889,5.01457808810825));
#8801=CARTESIAN_POINT('Ctrl Pts',(-0.692740630421603,4.96772924661066,5.04132448297697));
#8802=CARTESIAN_POINT('Ctrl Pts',(-0.63998554372013,4.97186619621242,5.06513871666905));
#8803=CARTESIAN_POINT('Ctrl Pts',(-0.58726256500489,4.97600062796938,5.08893845645854));
#8804=CARTESIAN_POINT('Ctrl Pts',(-0.533174513733451,4.98013505972634,5.1098093588572));
#8805=CARTESIAN_POINT('Ctrl Pts',(-0.478079379464037,4.9842694914833,5.1276040334912));
#8806=CARTESIAN_POINT('Ctrl Pts',(-0.422996609803048,4.9884029953792,5.14539471459317));
#8807=CARTESIAN_POINT('Ctrl Pts',(-0.366907701096103,4.9925364992751,5.16011037858373));
#8808=CARTESIAN_POINT('Ctrl Pts',(-0.310187297829203,4.996670003171,5.1716530061525));
#8809=CARTESIAN_POINT('Ctrl Pts',(-0.253415677140842,5.00080723954056,5.18320605648957));
#8810=CARTESIAN_POINT('Ctrl Pts',(-0.19601193360329,5.00494447591012,5.19158023947204));
#8811=CARTESIAN_POINT('Ctrl Pts',(-0.138361107359085,5.00908171227968,5.19672866527636));
#8812=CARTESIAN_POINT('Ctrl Pts',(-0.0806864049680436,5.01322066208979,
5.20187922330633));
#8813=CARTESIAN_POINT('Ctrl Pts',(-0.022764937357718,5.01735961189989,5.20380134227935));
#8814=CARTESIAN_POINT('Ctrl Pts',(0.0350161759650124,5.02149856170999,5.20250029022037));
#8815=CARTESIAN_POINT('Ctrl Pts',(0.0929095975521726,5.02564555633341,5.20119670932644));
#8816=CARTESIAN_POINT('Ctrl Pts',(0.150661598631048,5.02979255095683,5.19665747786724));
#8817=CARTESIAN_POINT('Ctrl Pts',(0.207889035770754,5.03393954558024,5.18893992619496));
#8818=CARTESIAN_POINT('Ctrl Pts',(0.261592491699019,5.03783117438846,5.18169760997704));
#8819=CARTESIAN_POINT('Ctrl Pts',(0.314833719845909,5.04172280319668,5.17165692314213));
#8820=CARTESIAN_POINT('Ctrl Pts',(0.367307093263549,5.0456144320049,5.15890554969819));
#8821=CARTESIAN_POINT('Ctrl Pts',(0.423242717723974,5.04976283477335,5.14531282657292));
#8822=CARTESIAN_POINT('Ctrl Pts',(0.478539950070272,5.05391123754181,5.12858247703888));
#8823=CARTESIAN_POINT('Ctrl Pts',(0.532821374524922,5.05805964031026,5.10879161924913));
#8824=CARTESIAN_POINT('Ctrl Pts',(0.587006451339249,5.0622006798081,5.08903588954357));
#8825=CARTESIAN_POINT('Ctrl Pts',(0.640178813855858,5.06634171930594,5.06623061086359));
#8826=CARTESIAN_POINT('Ctrl Pts',(0.691974214247196,5.07048275880377,5.04050319943768));
#8827=CARTESIAN_POINT('Ctrl Pts',(0.743718189736949,5.07461968688347,5.01480133139189));
#8828=CARTESIAN_POINT('Ctrl Pts',(0.794087447787117,5.07875661496317,4.98618330930379));
#8829=CARTESIAN_POINT('Ctrl Pts',(0.842737458631534,5.08289354304286,4.95482470574179));
#8830=CARTESIAN_POINT('Ctrl Pts',(0.891357860324589,5.08702795332395,4.92348518751241));
#8831=CARTESIAN_POINT('Ctrl Pts',(0.938260652246649,5.09116236360504,4.88940867573691));
#8832=CARTESIAN_POINT('Ctrl Pts',(0.983127633410276,5.09529677388613,4.8528156836377));
#8833=CARTESIAN_POINT('Ctrl Pts',(1.02798454623534,5.09943025638822,4.81623090315925));
#8834=CARTESIAN_POINT('Ctrl Pts',(1.07080615196489,5.10356373889032,4.7771310924156));
#8835=CARTESIAN_POINT('Ctrl Pts',(1.11130665585431,5.10769722139242,4.73577756565993));
#8836=CARTESIAN_POINT('Ctrl Pts',(1.1518437340318,5.11183443666732,4.6943866942874));
#8837=CARTESIAN_POINT('Ctrl Pts',(1.19005515556565,5.11597165194223,4.65073841184222));
#8838=CARTESIAN_POINT('Ctrl Pts',(1.2256924082796,5.12010886721714,4.60513053332776));
#8839=CARTESIAN_POINT('Ctrl Pts',(1.26134442137995,5.12424779606118,4.55950376475141));
#8840=CARTESIAN_POINT('Ctrl Pts',(1.29441984130309,5.12838672490521,4.5119162098285));
#8841=CARTESIAN_POINT('Ctrl Pts',(1.32471281917197,5.13252565374925,4.46269576027442));
#8842=CARTESIAN_POINT('Ctrl Pts',(1.35506468093426,5.13667262789824,4.41337963535565));
#8843=CARTESIAN_POINT('Ctrl Pts',(1.38262304284443,5.14081960204723,4.36242473206768));
#8844=CARTESIAN_POINT('Ctrl Pts',(1.40722792828634,5.14496657619622,4.3101838826916));
#8845=CARTESIAN_POINT('Ctrl Pts',(1.43031880371275,5.14885837498947,4.26115756440366));
#8846=CARTESIAN_POINT('Ctrl Pts',(1.45080881805183,5.15275017378272,4.21099922990207));
#8847=CARTESIAN_POINT('Ctrl Pts',(1.46860557248654,5.15664197257597,4.16001315938036));
#8848=CARTESIAN_POINT('Ctrl Pts',(1.490795582025,5.16149448951443,4.09644081559399));
#8849=CARTESIAN_POINT('Ctrl Pts',(1.50887543297797,5.16634700645289,4.03136398579588));
#8850=CARTESIAN_POINT('Ctrl Pts',(1.52267165228983,5.17119952339134,3.96528012274624));
#8851=CARTESIAN_POINT('Ctrl Pts',(1.53632980103551,5.17600347704257,3.89985761743379));
#8852=CARTESIAN_POINT('Ctrl Pts',(1.5457895385634,5.18080743069381,3.83344827699458));
#8853=CARTESIAN_POINT('Ctrl Pts',(1.5509290488956,5.18561138434504,3.76655543207561));
#8854=CARTESIAN_POINT('Ctrl Pts',(1.55394062032499,5.18842633141762,3.72735858888101));
#8855=CARTESIAN_POINT('Ctrl Pts',(1.55546970192271,5.19124127849021,3.68799611136951));
#8856=CARTESIAN_POINT('Ctrl Pts',(1.55549955406273,5.19405622556279,3.64857230980727));
#8857=CARTESIAN_POINT('Ctrl Pts',(1.5555,4.35539415465377,3.64739446822635));
#8858=CARTESIAN_POINT('Ctrl Pts',(1.55549999999998,4.35542999814836,3.64692840471078));
#8859=CARTESIAN_POINT('Ctrl Pts',(1.55549979055613,4.35546584504022,3.6464623380092));
#8860=CARTESIAN_POINT('Ctrl Pts',(1.55542473595912,4.36188857679378,3.56296395502293));
#8861=CARTESIAN_POINT('Ctrl Pts',(1.54870199287245,4.36837449542619,3.48007311827894));
#8862=CARTESIAN_POINT('Ctrl Pts',(1.52889270440882,4.37785809760788,3.35806064973547));
#8863=CARTESIAN_POINT('Ctrl Pts',(1.52082399216785,4.38093859904206,3.31827147924465));
#8864=CARTESIAN_POINT('Ctrl Pts',(1.50684734298435,4.38531873479868,3.26096210660124));
#8865=CARTESIAN_POINT('Ctrl Pts',(1.5021700412061,4.3866710431493,3.24316169155459));
#8866=CARTESIAN_POINT('Ctrl Pts',(1.49307977307113,4.38910145249918,3.21090706305395));
#8867=CARTESIAN_POINT('Ctrl Pts',(1.48877062776986,4.39018445434306,3.19642827795496));
#8868=CARTESIAN_POINT('Ctrl Pts',(1.47714668947669,4.39294051384069,3.15935583138254));
#8869=CARTESIAN_POINT('Ctrl Pts',(1.46952431871862,4.39459689997359,3.13686289014809));
#8870=CARTESIAN_POINT('Ctrl Pts',(1.45091238522665,4.39833868534909,3.0858172824324));
#8871=CARTESIAN_POINT('Ctrl Pts',(1.43958953000541,4.40040948261442,3.05739624327111));
#8872=CARTESIAN_POINT('Ctrl Pts',(1.3935987134821,4.40816645041638,2.95118001327726));
#8873=CARTESIAN_POINT('Ctrl Pts',(1.35340098778299,4.41370528325842,2.87594199554569));
#8874=CARTESIAN_POINT('Ctrl Pts',(1.27096408468862,4.42377475954,2.74811029532056));
#8875=CARTESIAN_POINT('Ctrl Pts',(1.23109277753004,4.428255456671,2.6942571150238));
#8876=CARTESIAN_POINT('Ctrl Pts',(1.1680043673741,4.43498426132566,2.61963291254187));
#8877=CARTESIAN_POINT('Ctrl Pts',(1.14743635971125,4.43712901503914,2.59671964265142));
#8878=CARTESIAN_POINT('Ctrl Pts',(1.10833588627034,4.44113146877616,2.55567895097275));
#8879=CARTESIAN_POINT('Ctrl Pts',(1.09000387279488,4.44298009405443,2.53737527190501));
#8880=CARTESIAN_POINT('Ctrl Pts',(1.04684672837064,4.4472756489092,2.49638511099435));
#8881=CARTESIAN_POINT('Ctrl Pts',(1.02172668075684,4.44973562529083,2.47402970038339));
#8882=CARTESIAN_POINT('Ctrl Pts',(0.938928703210333,4.45772661735186,2.40501999259121));
#8883=CARTESIAN_POINT('Ctrl Pts',(0.878637787054446,4.46337778056003,2.36167507033747));
#8884=CARTESIAN_POINT('Ctrl Pts',(0.726626581277196,4.47715923622267,2.26808858605383));
#8885=CARTESIAN_POINT('Ctrl Pts',(0.632476451274895,4.48533743175628,2.2224570852839));
#8886=CARTESIAN_POINT('Ctrl Pts',(0.51389604740648,4.49479424411113,2.17907206156493));
#8887=CARTESIAN_POINT('Ctrl Pts',(0.493171773749558,4.49641661501248,2.1719821285031));
#8888=CARTESIAN_POINT('Ctrl Pts',(0.458079326012494,4.49910532165137,2.16079887788345));
#8889=CARTESIAN_POINT('Ctrl Pts',(0.44379066473939,4.50018369446635,2.15647091884479));
#8890=CARTESIAN_POINT('Ctrl Pts',(0.410678268950601,4.50264447935619,2.14695964673775));
#8891=CARTESIAN_POINT('Ctrl Pts',(0.391815574230482,4.50401897428642,2.14192379497555));
#8892=CARTESIAN_POINT('Ctrl Pts',(0.313977050032271,4.50959855783355,2.12270516721571));
#8893=CARTESIAN_POINT('Ctrl Pts',(0.254285161224476,4.51366228573275,2.11162111071004));
#8894=CARTESIAN_POINT('Ctrl Pts',(0.0684829468289144,4.52606993601891,2.08825446455554));
#8895=CARTESIAN_POINT('Ctrl Pts',(-0.0585741758224798,4.5342576646857,2.08785139797022));
#8896=CARTESIAN_POINT('Ctrl Pts',(-0.216408854516841,4.54516460934817,2.1066820276763));
#8897=CARTESIAN_POINT('Ctrl Pts',(-0.248414344754627,4.54741203071616,2.11151762772879));
#8898=CARTESIAN_POINT('Ctrl Pts',(-0.305677513142983,4.55151215067336,2.12200596710727));
#8899=CARTESIAN_POINT('Ctrl Pts',(-0.330989559564697,4.5533527030844,2.12729756806451));
#8900=CARTESIAN_POINT('Ctrl Pts',(-0.387127098001552,4.55750396918868,2.14050193863259));
#8901=CARTESIAN_POINT('Ctrl Pts',(-0.417864477660436,4.55982431334066,2.14873457099195));
#8902=CARTESIAN_POINT('Ctrl Pts',(-0.482454373697825,4.56480659263543,2.16817565209562));
#8903=CARTESIAN_POINT('Ctrl Pts',(-0.516217209066973,4.56747461720144,2.17961724720742));
#8904=CARTESIAN_POINT('Ctrl Pts',(-0.616455924361088,4.57558649949667,2.21747265391306));
#8905=CARTESIAN_POINT('Ctrl Pts',(-0.681529451947081,4.5811157931353,2.24731936958475));
#8906=CARTESIAN_POINT('Ctrl Pts',(-0.810726560539948,4.5925232712912,2.31772414450078));
#8907=CARTESIAN_POINT('Ctrl Pts',(-0.87441706813729,4.59838835464249,2.35871396976759));
#8908=CARTESIAN_POINT('Ctrl Pts',(-0.952591794174984,4.60571793002098,2.41749999648646));
#8909=CARTESIAN_POINT('Ctrl Pts',(-0.97002144512225,4.60736081083441,2.43119955320827));
#8910=CARTESIAN_POINT('Ctrl Pts',(-0.998705307251497,4.61007133987632,2.45475395708422));
#8911=CARTESIAN_POINT('Ctrl Pts',(-1.01012003536558,4.61115155011968,2.46440619165219));
#8912=CARTESIAN_POINT('Ctrl Pts',(-1.03597528651205,4.6136011516674,2.48691648062338));
#8913=CARTESIAN_POINT('Ctrl Pts',(-1.05031825667497,4.61496302755117,2.49988167554502));
#8914=CARTESIAN_POINT('Ctrl Pts',(-1.10646622025366,4.62032447951741,2.5525712094774));
#8915=CARTESIAN_POINT('Ctrl Pts',(-1.14629392514209,4.62419688080577,2.59434309080453));
#8916=CARTESIAN_POINT('Ctrl Pts',(-1.25460414204208,4.63527457122279,2.72138768445489));
#8917=CARTESIAN_POINT('Ctrl Pts',(-1.31653308385251,4.64235106796483,2.8117747636599));
#8918=CARTESIAN_POINT('Ctrl Pts',(-1.38824632396734,4.65255069316582,2.94448532693523));
#8919=CARTESIAN_POINT('Ctrl Pts',(-1.40653715151324,4.65539975421856,2.98184066910839));
#8920=CARTESIAN_POINT('Ctrl Pts',(-1.43413299580547,4.66017171477297,3.04443282191966));
#8921=CARTESIAN_POINT('Ctrl Pts',(-1.44431966234323,4.66206380018973,3.06925888761211));
#8922=CARTESIAN_POINT('Ctrl Pts',(-1.46370230015254,4.66595323500559,3.12021109068446));
#8923=CARTESIAN_POINT('Ctrl Pts',(-1.47285268958301,4.66795131216819,3.14634406304927));
#8924=CARTESIAN_POINT('Ctrl Pts',(-1.4957746290852,4.67343547084167,3.21787363350106));
#8925=CARTESIAN_POINT('Ctrl Pts',(-1.50817388211601,4.67696409985088,3.26367508107682));
#8926=CARTESIAN_POINT('Ctrl Pts',(-1.53299545183572,4.68561167185927,3.37537493216633));
#8927=CARTESIAN_POINT('Ctrl Pts',(-1.54328759819419,4.69077900636863,3.44164798915467));
#8928=CARTESIAN_POINT('Ctrl Pts',(-1.55672745150483,4.70243354335533,3.591422803953));
#8929=CARTESIAN_POINT('Ctrl Pts',(-1.5574904033563,4.70891850701704,3.6749445312974));
#8930=CARTESIAN_POINT('Ctrl Pts',(-1.54998777875069,4.7168131069242,3.78006612871679));
#8931=CARTESIAN_POINT('Ctrl Pts',(-1.5479570642334,4.7184425982157,3.80196789962133));
#8932=CARTESIAN_POINT('Ctrl Pts',(-1.54376846267121,4.72113885910744,3.83865930334746));
#8933=CARTESIAN_POINT('Ctrl Pts',(-1.54186089649022,4.72221784814295,3.85347296396247));
#8934=CARTESIAN_POINT('Ctrl Pts',(-1.53697778997546,4.72467463794818,3.88751518709492));
#8935=CARTESIAN_POINT('Ctrl Pts',(-1.5338544371308,4.72604466352001,3.90671926351459));
#8936=CARTESIAN_POINT('Ctrl Pts',(-1.51971159811976,4.73154357133582,3.9844442386269));
#8937=CARTESIAN_POINT('Ctrl Pts',(-1.5056953768279,4.73553644040192,4.04237414377839));
#8938=CARTESIAN_POINT('Ctrl Pts',(-1.44985041264986,4.74827744764488,4.22627853082451));
#8939=CARTESIAN_POINT('Ctrl Pts',(-1.39524132686724,4.75684396019484,4.34773184749127));
#8940=CARTESIAN_POINT('Ctrl Pts',(-1.30981470610301,4.76809456482178,4.48698395210403));
#8941=CARTESIAN_POINT('Ctrl Pts',(-1.2929695035071,4.77023620124597,4.51270059951141));
#8942=CARTESIAN_POINT('Ctrl Pts',(-1.26054325591555,4.7742358831103,4.55914120380146));
#8943=CARTESIAN_POINT('Ctrl Pts',(-1.24518448300833,4.77608494904194,4.58000739144719));
#8944=CARTESIAN_POINT('Ctrl Pts',(-1.20867120393973,4.78038602871796,4.62710313544392));
#8945=CARTESIAN_POINT('Ctrl Pts',(-1.18717188668116,4.78285121678727,4.65304735908694));
#8946=CARTESIAN_POINT('Ctrl Pts',(-1.11570732639708,4.7908467590375,4.73379938693622));
#8947=CARTESIAN_POINT('Ctrl Pts',(-1.06266489891863,4.79649695392724,4.78573496557076));
#8948=CARTESIAN_POINT('Ctrl Pts',(-0.926709698403657,4.81026035894515,4.90104268528015));
#8949=CARTESIAN_POINT('Ctrl Pts',(-0.840724536636249,4.81842067398266,4.96025739752718));
#8950=CARTESIAN_POINT('Ctrl Pts',(-0.730244834359119,4.82786399248016,5.02100422202298));
#8951=CARTESIAN_POINT('Ctrl Pts',(-0.710803484380253,4.82948889400623,5.03116461320231));
#8952=CARTESIAN_POINT('Ctrl Pts',(-0.677776337640811,4.8321802833817,5.04754532419139));
#8953=CARTESIAN_POINT('Ctrl Pts',(-0.664305236812612,4.8332588731138,5.05398673398091));
#8954=CARTESIAN_POINT('Ctrl Pts',(-0.63303328058106,4.8357182275306,5.06839032584697));
#8955=CARTESIAN_POINT('Ctrl Pts',(-0.61517199606121,4.83709112577514,5.07621351721705));
#8956=CARTESIAN_POINT('Ctrl Pts',(-0.541533940049074,4.84264138873306,5.1068297425127));
#8957=CARTESIAN_POINT('Ctrl Pts',(-0.484597085563224,4.84667935041719,5.12671108817259));
#8958=CARTESIAN_POINT('Ctrl Pts',(-0.300022473846509,4.8593987841055,5.179355346805));
#8959=CARTESIAN_POINT('Ctrl Pts',(-0.169339690549315,4.86790736886002,5.19924479353335));
#8960=CARTESIAN_POINT('Ctrl Pts',(-0.00693726053703426,4.87909349000794,
5.20318365165234));
#8961=CARTESIAN_POINT('Ctrl Pts',(0.0238543599284254,4.88123833983494,5.20301616049979));
#8962=CARTESIAN_POINT('Ctrl Pts',(0.0805057286813397,4.88524087923301,5.20102570800575));
#8963=CARTESIAN_POINT('Ctrl Pts',(0.106364194731054,4.88708949112897,5.19946975994246));
#8964=CARTESIAN_POINT('Ctrl Pts',(0.165667618915032,4.89138487683024,5.19441247539608));
#8965=CARTESIAN_POINT('Ctrl Pts',(0.199060825190142,4.89384469353514,5.19047092059296));
#8966=CARTESIAN_POINT('Ctrl Pts',(0.305636727207883,4.90183554276984,5.17437440333785));
#8967=CARTESIAN_POINT('Ctrl Pts',(0.378079556000965,4.90748673212127,5.15806804776789));
#8968=CARTESIAN_POINT('Ctrl Pts',(0.548996000259684,4.92126877416249,5.10652976367326));
#8969=CARTESIAN_POINT('Ctrl Pts',(0.645635091687667,4.92944755621753,5.06641872758857));
#8970=CARTESIAN_POINT('Ctrl Pts',(0.756812690538516,4.93890481289353,5.00654653594583));
#8971=CARTESIAN_POINT('Ctrl Pts',(0.775873061328148,4.94052710273782,4.99575677770474));
#8972=CARTESIAN_POINT('Ctrl Pts',(0.807533810189901,4.94321572188394,4.97694035353649));
#8973=CARTESIAN_POINT('Ctrl Pts',(0.820256839427936,4.94429408624312,4.96912889660789));
#8974=CARTESIAN_POINT('Ctrl Pts',(0.849354163985706,4.94675490993549,4.95068216686474));
#8975=CARTESIAN_POINT('Ctrl Pts',(0.865644040164713,4.94812945060267,4.93991983166864));
#8976=CARTESIAN_POINT('Ctrl Pts',(0.931705492617353,4.95370991074706,4.89446519351761));
#8977=CARTESIAN_POINT('Ctrl Pts',(0.979634465981861,4.95777441024533,4.85717896516727));
#8978=CARTESIAN_POINT('Ctrl Pts',(1.12045677245441,4.9701812864885,4.73375460362749));
#8979=CARTESIAN_POINT('Ctrl Pts',(1.2050998194748,4.97836762238755,4.63902655933112));
#8980=CARTESIAN_POINT('Ctrl Pts',(1.29580110506019,4.98927315414945,4.50851427377775));
#8981=CARTESIAN_POINT('Ctrl Pts',(1.31343668563415,4.99152078286865,4.4813678702151));
#8982=CARTESIAN_POINT('Ctrl Pts',(1.34361465959424,4.9956211066508,4.43158096879652));
#8983=CARTESIAN_POINT('Ctrl Pts',(1.35646337366098,4.99746164930446,4.40913969473083));
#8984=CARTESIAN_POINT('Ctrl Pts',(1.38385985427357,5.00161266991114,4.35839671230256));
#8985=CARTESIAN_POINT('Ctrl Pts',(1.39811010021698,5.00393277247568,4.32994861158317));
#8986=CARTESIAN_POINT('Ctrl Pts',(1.45176048803832,5.01336249309508,4.21410442814453));
#8987=CARTESIAN_POINT('Ctrl Pts',(1.48391078081463,5.0207068912447,4.12360010393777));
#8988=CARTESIAN_POINT('Ctrl Pts',(1.5287126263025,5.03479064832996,3.94740938413806));
#8989=CARTESIAN_POINT('Ctrl Pts',(1.54295667978206,5.04148626376499,3.86247127854805));
#8990=CARTESIAN_POINT('Ctrl Pts',(1.55196051596764,5.04960547706827,3.75460553906682));
#8991=CARTESIAN_POINT('Ctrl Pts',(1.5533358305926,5.05125710375816,3.73238618335164));
#8992=CARTESIAN_POINT('Ctrl Pts',(1.55469402656414,5.05371899289713,3.69874495057206));
#8993=CARTESIAN_POINT('Ctrl Pts',(1.55502884006779,5.05454679470241,3.6873410315443));
#8994=CARTESIAN_POINT('Ctrl Pts',(1.55541087755945,5.05604459048751,3.66652198520036));
#8995=CARTESIAN_POINT('Ctrl Pts',(1.55549815372627,5.05671690269938,3.6571086182568));
#8996=CARTESIAN_POINT('Ctrl Pts',(1.55549997101641,5.05738485701522,3.64769474805265));
#8997=CARTESIAN_POINT('Origin',(-2.67773308947627E-16,1.2059437743963,3.64739446828387));
#8998=CARTESIAN_POINT('',(1.55549964733824,5.89405622564623,3.64634702825329));
#8999=CARTESIAN_POINT('',(1.5554995134887,5.7559437743963,3.64862472695888));
#9000=CARTESIAN_POINT('',(1.5555,1.2059437743963,3.64739446828386));
#9001=CARTESIAN_POINT('Ctrl Pts',(1.55549955406316,5.1940562256037,3.64857230923438));
#9002=CARTESIAN_POINT('Ctrl Pts',(1.55554339101516,5.19818989105023,3.59067963768888));
#9003=CARTESIAN_POINT('Ctrl Pts',(1.55235092862268,5.20232355649676,3.53275114493701));
#9004=CARTESIAN_POINT('Ctrl Pts',(1.54593674727678,5.20645722194329,3.47517419241811));
#9005=CARTESIAN_POINT('Ctrl Pts',(1.53952345737511,5.21059031289216,3.4176052419557));
#9006=CARTESIAN_POINT('Ctrl Pts',(1.52988939577038,5.21472340384103,3.36038825123378));
#9007=CARTESIAN_POINT('Ctrl Pts',(1.51710097035125,5.2188564947899,3.30390517331344));
#9008=CARTESIAN_POINT('Ctrl Pts',(1.50429938807024,5.2229938379047,3.24736398502915));
#9009=CARTESIAN_POINT('Ctrl Pts',(1.48833707342149,5.22713118101949,3.19155872648236));
#9010=CARTESIAN_POINT('Ctrl Pts',(1.46933126780937,5.23126852413429,3.13685957678506));
#9011=CARTESIAN_POINT('Ctrl Pts',(1.4503162406771,5.23540787466691,3.08213388733872));
#9012=CARTESIAN_POINT('Ctrl Pts',(1.42825497839268,5.23954722519952,3.02851585791755));
#9013=CARTESIAN_POINT('Ctrl Pts',(1.40331301745104,5.24368657573214,2.97635585162128));
#9014=CARTESIAN_POINT('Ctrl Pts',(1.37832001504554,5.24783439707068,2.92408910459671));
#9015=CARTESIAN_POINT('Ctrl Pts',(1.35043478546577,5.25198221840923,2.87328680009967));
#9016=CARTESIAN_POINT('Ctrl Pts',(1.31986857258952,5.25613003974777,2.82427406330627));
#9017=CARTESIAN_POINT('Ctrl Pts',(1.29152292864674,5.25997653088087,2.77882199531761));
#9018=CARTESIAN_POINT('Ctrl Pts',(1.26087236047473,5.26382302201396,2.73490888339637));
#9019=CARTESIAN_POINT('Ctrl Pts',(1.22811608950117,5.26766951314705,2.69276830024302));
#9020=CARTESIAN_POINT('Ctrl Pts',(1.1927883306997,5.27181796799075,2.64731952621754));
#9021=CARTESIAN_POINT('Ctrl Pts',(1.15486031021853,5.27596642283445,2.60373928251711));
#9022=CARTESIAN_POINT('Ctrl Pts',(1.11455708914475,5.28011487767815,2.56234020925477));
#9023=CARTESIAN_POINT('Ctrl Pts',(1.07432540113556,5.28425596954489,2.52101461405456));
#9024=CARTESIAN_POINT('Ctrl Pts',(1.03172724032223,5.28839706141163,2.48186287528167));
#9025=CARTESIAN_POINT('Ctrl Pts',(0.987028147397972,5.29253815327837,2.44516500339619));
#9026=CARTESIAN_POINT('Ctrl Pts',(0.942373431723652,5.29667513386998,2.4085035651501));
#9027=CARTESIAN_POINT('Ctrl Pts',(0.89562231697053,5.30081211446159,2.37429149565244));
#9028=CARTESIAN_POINT('Ctrl Pts',(0.847076184934661,5.30494909505321,2.34277107936409));
#9029=CARTESIAN_POINT('Ctrl Pts',(0.798559597826388,5.3090835578996,2.31126984623983));
#9030=CARTESIAN_POINT('Ctrl Pts',(0.748250594795294,5.31321802074599,2.28245730203282));
#9031=CARTESIAN_POINT('Ctrl Pts',(0.696480755874186,5.31735248359238,2.25653329379631));
#9032=CARTESIAN_POINT('Ctrl Pts',(0.644722534624885,5.32148601862378,2.23061510316761));
#9033=CARTESIAN_POINT('Ctrl Pts',(0.591504593667746,5.32561955365519,2.20758439462339));
#9034=CARTESIAN_POINT('Ctrl Pts',(0.537182444298231,5.32975308868659,2.18759473149194));
#9035=CARTESIAN_POINT('Ctrl Pts',(0.48281124580911,5.3338903560124,2.16758701908613));
#9036=CARTESIAN_POINT('Ctrl Pts',(0.427334335914796,5.33802762333821,2.15062602066201));
#9037=CARTESIAN_POINT('Ctrl Pts',(0.37112523597503,5.34216489066401,2.1368163308734));
#9038=CARTESIAN_POINT('Ctrl Pts',(0.314892857790601,5.34630387138358,2.12300092198704));
#9039=CARTESIAN_POINT('Ctrl Pts',(0.257928197727324,5.35044285210315,2.11233952072553));
#9040=CARTESIAN_POINT('Ctrl Pts',(0.20061472232642,5.35458183282272,2.10488547862258));
#9041=CARTESIAN_POINT('Ctrl Pts',(0.14318985516695,5.35872885786934,2.09741694919614));
#9042=CARTESIAN_POINT('Ctrl Pts',(0.0854153389819498,5.36287588291597,2.09316827547533));
#9043=CARTESIAN_POINT('Ctrl Pts',(0.0276785853041187,5.36702290796259,2.09214074431612));
#9044=CARTESIAN_POINT('Ctrl Pts',(-0.0264989894077483,5.37091428988111,
2.09117655525801));
#9045=CARTESIAN_POINT('Ctrl Pts',(-0.0806429526473259,5.37480567179962,
2.09304809442987));
#9046=CARTESIAN_POINT('Ctrl Pts',(-0.134437993166186,5.37869705371814,2.0977149285101));
#9047=CARTESIAN_POINT('Ctrl Pts',(-0.191784778467867,5.38284535886403,2.10268988399774));
#9048=CARTESIAN_POINT('Ctrl Pts',(-0.248975180305849,5.38699366400992,2.11086278502762));
#9049=CARTESIAN_POINT('Ctrl Pts',(-0.305624474969962,5.39114196915581,2.12221450175555));
#9050=CARTESIAN_POINT('Ctrl Pts',(-0.362173217818001,5.39528291111001,2.13354606932294));
#9051=CARTESIAN_POINT('Ctrl Pts',(-0.418182253502629,5.3994238530642,2.14804515179915));
#9052=CARTESIAN_POINT('Ctrl Pts',(-0.473272264851127,5.4035647950184,2.16564090803079));
#9053=CARTESIAN_POINT('Ctrl Pts',(-0.528307580459116,5.40770162566673,2.18321919443635));
#9054=CARTESIAN_POINT('Ctrl Pts',(-0.582425186030991,5.41183845631507,2.20388790541525));
#9055=CARTESIAN_POINT('Ctrl Pts',(-0.635257970069161,5.4159752869634,2.2275256146697));
#9056=CARTESIAN_POINT('Ctrl Pts',(-0.688058601996187,5.42010960008704,2.25114893887387));
#9057=CARTESIAN_POINT('Ctrl Pts',(-0.739575487986166,5.42424391321067,2.27773746746318));
#9058=CARTESIAN_POINT('Ctrl Pts',(-0.789460743674072,5.42837822633431,2.30712136768176));
#9059=CARTESIAN_POINT('Ctrl Pts',(-0.839334809894685,5.43251161211456,2.33649867697111));
#9060=CARTESIAN_POINT('Ctrl Pts',(-0.887577523941612,5.43664499789482,2.36866984892289));
#9061=CARTESIAN_POINT('Ctrl Pts',(-0.933866862659667,5.44077838367508,2.40341981708466));
#9062=CARTESIAN_POINT('Ctrl Pts',(-0.980198020559222,5.44491550368043,2.43820117941334));
#9063=CARTESIAN_POINT('Ctrl Pts',(-1.024571858391,5.44905262368578,2.47556568122309));
#9064=CARTESIAN_POINT('Ctrl Pts',(-1.06669768505826,5.45318974369113,2.51525653556924));
#9065=CARTESIAN_POINT('Ctrl Pts',(-1.10884096645356,5.45732857790152,2.55496383571891));
#9066=CARTESIAN_POINT('Ctrl Pts',(-1.14873401962118,5.46146741211192,2.59699903237818));
#9067=CARTESIAN_POINT('Ctrl Pts',(-1.18612377654658,5.46560624632231,2.64106915472424));
#9068=CARTESIAN_POINT('Ctrl Pts',(-1.2235862347266,5.46975312814961,2.68522496773667));
#9069=CARTESIAN_POINT('Ctrl Pts',(-1.25853535357741,5.4739000099769,2.73142319730467));
#9070=CARTESIAN_POINT('Ctrl Pts',(-1.29075963708497,5.4780468918042,2.77933928036534));
#9071=CARTESIAN_POINT('Ctrl Pts',(-1.32100771353262,5.48193945929921,2.82431683101129));
#9072=CARTESIAN_POINT('Ctrl Pts',(-1.34885515567857,5.48583202679421,2.8708074098687));
#9073=CARTESIAN_POINT('Ctrl Pts',(-1.37416452409191,5.48972459428922,2.91852403348268));
#9074=CARTESIAN_POINT('Ctrl Pts',(-1.40113808296194,5.49387311339754,2.96937821265902));
#9075=CARTESIAN_POINT('Ctrl Pts',(-1.42534134831133,5.49802163250586,3.02183823319597));
#9076=CARTESIAN_POINT('Ctrl Pts',(-1.44658140734488,5.50217015161417,3.07557064758022));
#9077=CARTESIAN_POINT('Ctrl Pts',(-1.46778375951885,5.50631130597707,3.12920767237065));
#9078=CARTESIAN_POINT('Ctrl Pts',(-1.48603315695587,5.51045246033997,3.18411212726837));
#9079=CARTESIAN_POINT('Ctrl Pts',(-1.50118304248143,5.51459361470287,3.23992701809158));
#9080=CARTESIAN_POINT('Ctrl Pts',(-1.51631788336419,5.51873065667904,3.29568648175705));
#9081=CARTESIAN_POINT('Ctrl Pts',(-1.52835917507792,5.52286769865521,3.3523540900666));
#9082=CARTESIAN_POINT('Ctrl Pts',(-1.53720946298209,5.52700474063138,3.40955562175469));
#9083=CARTESIAN_POINT('Ctrl Pts',(-1.54605436215694,5.53113926366132,3.46672232479381));
#9084=CARTESIAN_POINT('Ctrl Pts',(-1.55171202954512,5.53527378669126,3.52442179328072));
#9085=CARTESIAN_POINT('Ctrl Pts',(-1.5541360973046,5.5394083097212,3.58226965692273));
#9086=CARTESIAN_POINT('Ctrl Pts',(-1.55655962032951,5.54354190364442,3.64010452103892));
#9087=CARTESIAN_POINT('Ctrl Pts',(-1.55575096456502,5.54767549756764,3.69808719414853));
#9088=CARTESIAN_POINT('Ctrl Pts',(-1.5517157883933,5.55180909149086,3.75583044963211));
#9089=CARTESIAN_POINT('Ctrl Pts',(-1.54767697120438,5.55594641523552,3.81362580796767));
#9090=CARTESIAN_POINT('Ctrl Pts',(-1.54040585086494,5.56008373898018,3.87118079622946));
#9091=CARTESIAN_POINT('Ctrl Pts',(-1.52996013383856,5.56422106272484,3.92811183302054));
#9092=CARTESIAN_POINT('Ctrl Pts',(-1.51951009409349,5.56836009860536,3.98506642940604));
#9093=CARTESIAN_POINT('Ctrl Pts',(-1.5058829600887,5.57249913448588,4.04139605210123));
#9094=CARTESIAN_POINT('Ctrl Pts',(-1.48918725521303,5.57663817036639,4.09672905287655));
#9095=CARTESIAN_POINT('Ctrl Pts',(-1.47245911320342,5.58078524774395,4.15216955698707));
#9096=CARTESIAN_POINT('Ctrl Pts',(-1.4526506642247,5.5849323251215,4.20660907835336));
#9097=CARTESIAN_POINT('Ctrl Pts',(-1.42991953843312,5.58907940249905,4.25969371179738));
#9098=CARTESIAN_POINT('Ctrl Pts',(-1.40859252316599,5.59297031328613,4.3094992866858));
#9099=CARTESIAN_POINT('Ctrl Pts',(-1.38469337269005,5.59686122407321,4.35811207240156));
#9100=CARTESIAN_POINT('Ctrl Pts',(-1.35838814834895,5.6007521348603,4.40526113757677));
#9101=CARTESIAN_POINT('Ctrl Pts',(-1.33034059139179,5.60490076102295,4.45553313198483));
#9102=CARTESIAN_POINT('Ctrl Pts',(-1.29943983349395,5.6090493871856,4.5043512258202));
#9103=CARTESIAN_POINT('Ctrl Pts',(-1.26586108932038,5.61319801334825,4.55137231787126));
#9104=CARTESIAN_POINT('Ctrl Pts',(-1.2323419222398,5.61733927881018,4.59830998274113));
#9105=CARTESIAN_POINT('Ctrl Pts',(-1.19615449993241,5.6214805442721,4.64345655405963));
#9106=CARTESIAN_POINT('Ctrl Pts',(-1.15751898488021,5.62562180973402,4.68649506478158));
#9107=CARTESIAN_POINT('Ctrl Pts',(-1.11892181377584,5.629758965183,4.72949086178772));
#9108=CARTESIAN_POINT('Ctrl Pts',(-1.07788170981581,5.63389612063199,4.77038235794144));
#9109=CARTESIAN_POINT('Ctrl Pts',(-1.03465996895199,5.63803327608097,4.80888445904929));
#9110=CARTESIAN_POINT('Ctrl Pts',(-0.991464521539586,5.64216791473878,4.84736313784457));
#9111=CARTESIAN_POINT('Ctrl Pts',(-0.946090456058851,5.64630255339659,4.88345495740179));
#9112=CARTESIAN_POINT('Ctrl Pts',(-0.898835336805198,5.6504371920544,4.91691220636802));
#9113=CARTESIAN_POINT('Ctrl Pts',(-0.851590814222675,5.65457090354481,4.95036195275104));
#9114=CARTESIAN_POINT('Ctrl Pts',(-0.802466500010218,5.65870461503523,4.98117800074386));
#9115=CARTESIAN_POINT('Ctrl Pts',(-0.751790614076356,5.66283832652564,5.00915477119577));
#9116=CARTESIAN_POINT('Ctrl Pts',(-0.701068978425304,5.66697576989223,5.03715679881511));
#9117=CARTESIAN_POINT('Ctrl Pts',(-0.648793428175893,5.67111321325882,5.06231417327492));
#9118=CARTESIAN_POINT('Ctrl Pts',(-0.595317392221518,5.67525065662541,5.08446699690536));
#9119=CARTESIAN_POINT('Ctrl Pts',(-0.54181921002405,5.67938981344785,5.10662899477261));
#9120=CARTESIAN_POINT('Ctrl Pts',(-0.487120043010132,5.68352897027029,5.12578378759072));
#9121=CARTESIAN_POINT('Ctrl Pts',(-0.431590901758725,5.68766812709273,5.1418206268876));
#9122=CARTESIAN_POINT('Ctrl Pts',(-0.375953871087437,5.69181532602096,5.15788862469422));
#9123=CARTESIAN_POINT('Ctrl Pts',(-0.31948415272831,5.69596252494919,5.17082644518591));
#9124=CARTESIAN_POINT('Ctrl Pts',(-0.262564532221247,5.70010972387742,5.18057420869901));
#9125=CARTESIAN_POINT('Ctrl Pts',(-0.209175146173626,5.70399970772874,5.1897174022879));
#9126=CARTESIAN_POINT('Ctrl Pts',(-0.155390369769416,5.70788969158005,5.19605443380858));
#9127=CARTESIAN_POINT('Ctrl Pts',(-0.10152764302057,5.71177967543137,5.19957757207758));
#9128=CARTESIAN_POINT('Ctrl Pts',(-0.0440976842286706,5.71592728595477,
5.20333404149196));
#9129=CARTESIAN_POINT('Ctrl Pts',(0.0136615881029582,5.72007489647816,5.20390677509005));
#9130=CARTESIAN_POINT('Ctrl Pts',(0.0713670981046381,5.72422250700156,5.20125642718116));
#9131=CARTESIAN_POINT('Ctrl Pts',(0.1289701615635,5.72836275413177,5.19861078452452));
#9132=CARTESIAN_POINT('Ctrl Pts',(0.186519136065157,5.73250300126198,5.1927534414133));
#9133=CARTESIAN_POINT('Ctrl Pts',(0.24362845718739,5.73664324839219,5.18369698564446));
#9134=CARTESIAN_POINT('Ctrl Pts',(0.300681072802416,5.74077938455052,5.17464952229416));
#9135=CARTESIAN_POINT('Ctrl Pts',(0.357294388064168,5.74491552070884,5.16240932097463));
#9136=CARTESIAN_POINT('Ctrl Pts',(0.413087244050112,5.74905165686716,5.14704081952908));
#9137=CARTESIAN_POINT('Ctrl Pts',(0.468846160906999,5.75318527698905,5.13168166683518));
#9138=CARTESIAN_POINT('Ctrl Pts',(0.523785106630126,5.75731889711093,5.11319812425796));
#9139=CARTESIAN_POINT('Ctrl Pts',(0.577534600719311,5.76145251723282,5.09170538874802));
#9140=CARTESIAN_POINT('Ctrl Pts',(0.631272070913041,5.7655852126536,5.07021746121644));
#9141=CARTESIAN_POINT('Ctrl Pts',(0.683820134277734,5.76971790807439,5.045721870491));
#9142=CARTESIAN_POINT('Ctrl Pts',(0.734828029057464,5.77385060349518,5.01838243967951));
#9143=CARTESIAN_POINT('Ctrl Pts',(0.785882132555134,5.77798704277871,4.99101824172064));
#9144=CARTESIAN_POINT('Ctrl Pts',(0.835392818450878,5.78212348206224,4.960805301017));
#9145=CARTESIAN_POINT('Ctrl Pts',(0.883033984203594,5.78625992134577,4.92795342153106));
#9146=CARTESIAN_POINT('Ctrl Pts',(0.930694940833089,5.79039807897013,4.89508789486649));
#9147=CARTESIAN_POINT('Ctrl Pts',(0.976484415800411,5.79453623659449,4.85958156294093));
#9148=CARTESIAN_POINT('Ctrl Pts',(1.02010802560609,5.79867439421885,4.82168568688939));
#9149=CARTESIAN_POINT('Ctrl Pts',(1.0638166387669,5.80282061530434,4.7837159683332));
#9150=CARTESIAN_POINT('Ctrl Pts',(1.10535057742059,5.80696683638983,4.74334776458119));
#9151=CARTESIAN_POINT('Ctrl Pts',(1.14445177490565,5.81111305747533,4.70086985238894));
#9152=CARTESIAN_POINT('Ctrl Pts',(1.18121260623956,5.8150111103177,4.66093441649563));
#9153=CARTESIAN_POINT('Ctrl Pts',(1.21582333906809,5.81890916316007,4.61913487527535));
#9154=CARTESIAN_POINT('Ctrl Pts',(1.24810396751098,5.82280721600245,4.57573531963284));
#9155=CARTESIAN_POINT('Ctrl Pts',(1.28262086856108,5.82697531032832,4.52932921665439));
#9156=CARTESIAN_POINT('Ctrl Pts',(1.31461877168976,5.83114340465419,4.48089784141524));
#9157=CARTESIAN_POINT('Ctrl Pts',(1.34385418886972,5.83531149898005,4.43074379588766));
#9158=CARTESIAN_POINT('Ctrl Pts',(1.37304289061388,5.8394729330848,4.38066989178852));
#9159=CARTESIAN_POINT('Ctrl Pts',(1.39947760178787,5.84363436718955,4.3288792150418));
#9160=CARTESIAN_POINT('Ctrl Pts',(1.42295681421145,5.8477958012943,4.27570502436996));
#9161=CARTESIAN_POINT('Ctrl Pts',(1.4464053075886,5.8519517907834,4.22260040419319));
#9162=CARTESIAN_POINT('Ctrl Pts',(1.46690577030673,5.85610778027249,4.16811633035345));
#9163=CARTESIAN_POINT('Ctrl Pts',(1.48430262546914,5.86026376976159,4.11261051059691));
#9164=CARTESIAN_POINT('Ctrl Pts',(1.50168590311237,5.86441651567439,4.05714801081549));
#9165=CARTESIAN_POINT('Ctrl Pts',(1.51597022498911,5.86856926158719,4.00066583607904));
#9166=CARTESIAN_POINT('Ctrl Pts',(1.52704887102887,5.87272200749999,3.94353969530846));
#9167=CARTESIAN_POINT('Ctrl Pts',(1.53812567839228,5.87687406419899,3.88642303552353));
#9168=CARTESIAN_POINT('Ctrl Pts',(1.54599775636003,5.881026120898,3.82866312385785));
#9169=CARTESIAN_POINT('Ctrl Pts',(1.5506092566561,5.885178177597,3.77064698619895));
#9170=CARTESIAN_POINT('Ctrl Pts',(1.55389607119802,5.88813752693257,3.72929639036671));
#9171=CARTESIAN_POINT('Ctrl Pts',(1.55552757156221,5.89109687626813,3.68781588946909));
#9172=CARTESIAN_POINT('Ctrl Pts',(1.55549964733864,5.8940562256037,3.64634702884922));
#9173=CARTESIAN_POINT('Ctrl Pts',(1.5554999873946,5.05594377443823,3.64759249708933));
#9174=CARTESIAN_POINT('Ctrl Pts',(1.55550729033478,5.06007749260067,3.59022850230281));
#9175=CARTESIAN_POINT('Ctrl Pts',(1.55233707856484,5.06421121076312,3.53274024496008));
#9176=CARTESIAN_POINT('Ctrl Pts',(1.54597416002809,5.06834492892557,3.47551036045119));
#9177=CARTESIAN_POINT('Ctrl Pts',(1.53962245335763,5.07247136321427,3.41838131863089));
#9178=CARTESIAN_POINT('Ctrl Pts',(1.5300892612969,5.07659779750297,3.36151026343843));
#9179=CARTESIAN_POINT('Ctrl Pts',(1.51741138191812,5.08072423179167,3.30527906666428));
#9180=CARTESIAN_POINT('Ctrl Pts',(1.50474592422412,5.08484662303307,3.24910296476678));
#9181=CARTESIAN_POINT('Ctrl Pts',(1.48894199726885,5.08896901427447,3.19356598886568));
#9182=CARTESIAN_POINT('Ctrl Pts',(1.47008786542628,5.09309140551588,3.13904230892344));
#9183=CARTESIAN_POINT('Ctrl Pts',(1.45124482651563,5.09721137132577,3.08455070828747));
#9184=CARTESIAN_POINT('Ctrl Pts',(1.42935531067883,5.10133133713567,3.03107171707727));
#9185=CARTESIAN_POINT('Ctrl Pts',(1.40455747949938,5.10545130294556,2.97896456411864));
#9186=CARTESIAN_POINT('Ctrl Pts',(1.37976453193656,5.10957045738073,2.92686767299931));
#9187=CARTESIAN_POINT('Ctrl Pts',(1.35206463182601,5.1136896118159,2.87614255733828));
#9188=CARTESIAN_POINT('Ctrl Pts',(1.3216432290437,5.11780876625106,2.82712656989765));
#9189=CARTESIAN_POINT('Ctrl Pts',(1.29119393642363,5.12193169705873,2.7780656454123));
#9190=CARTESIAN_POINT('Ctrl Pts',(1.25801843387563,5.1260546278664,2.7307174264883));
#9191=CARTESIAN_POINT('Ctrl Pts',(1.22234637900804,5.13017755867407,2.68539156822279));
#9192=CARTESIAN_POINT('Ctrl Pts',(1.18665819797229,5.13430235332377,2.64004521962066));
#9193=CARTESIAN_POINT('Ctrl Pts',(1.14847156347857,5.13842714797348,2.59672344769715));
#9194=CARTESIAN_POINT('Ctrl Pts',(1.10805533127371,5.14255194262319,2.55570145610695));
#9195=CARTESIAN_POINT('Ctrl Pts',(1.06756285499791,5.14668451858052,2.514602077698));
#9196=CARTESIAN_POINT('Ctrl Pts',(1.02483276916788,5.15081709453785,2.47581149899184));
#9197=CARTESIAN_POINT('Ctrl Pts',(0.980168736436743,5.15494967049518,2.43956604581982));
#9198=CARTESIAN_POINT('Ctrl Pts',(0.945182812488144,5.15818677156542,2.41117450590241));
#9199=CARTESIAN_POINT('Ctrl Pts',(0.909010995181922,5.16142387263566,2.38434383327528));
#9200=CARTESIAN_POINT('Ctrl Pts',(0.87181086109517,5.16466097370589,2.35916852828868));
#9201=CARTESIAN_POINT('Ctrl Pts',(0.824137977463899,5.16880939807082,2.32690575788551));
#9202=CARTESIAN_POINT('Ctrl Pts',(0.77457193097481,5.17295782243575,2.29722530939668));
#9203=CARTESIAN_POINT('Ctrl Pts',(0.723423584422977,5.17710624680067,2.27035468399998));
#9204=CARTESIAN_POINT('Ctrl Pts',(0.672366023848988,5.18124730790192,2.24353175273548));
#9205=CARTESIAN_POINT('Ctrl Pts',(0.61973219489561,5.18538836900317,2.21950898557959));
#9206=CARTESIAN_POINT('Ctrl Pts',(0.565861335505652,5.18952943010441,2.19847031603167));
#9207=CARTESIAN_POINT('Ctrl Pts',(0.512043961482645,5.19366637977742,2.17745253460348));
#9208=CARTESIAN_POINT('Ctrl Pts',(0.456992472997552,5.19780332945043,2.15941316913124));
#9209=CARTESIAN_POINT('Ctrl Pts',(0.401068493576888,5.20194027912344,2.14448917736898));
#9210=CARTESIAN_POINT('Ctrl Pts',(0.345178550803582,5.20607471095171,2.12957426869863));
#9211=CARTESIAN_POINT('Ctrl Pts',(0.288417671795299,5.21020914277998,2.11777110909836));
#9212=CARTESIAN_POINT('Ctrl Pts',(0.231163040437577,5.21434357460825,2.10916694976275));
#9213=CARTESIAN_POINT('Ctrl Pts',(0.173921258329439,5.2184770785754,2.1005647213974));
#9214=CARTESIAN_POINT('Ctrl Pts',(0.116186458521773,5.22261058254255,2.09516014532916));
#9215=CARTESIAN_POINT('Ctrl Pts',(0.0583442347286331,5.2267440865097,2.09298905132408));
#9216=CARTESIAN_POINT('Ctrl Pts',(0.000449780542036197,5.23088132294985,
2.09081599686371));
#9217=CARTESIAN_POINT('Ctrl Pts',(-0.0575517699355378,5.23501855939,2.09188227998785));
#9218=CARTESIAN_POINT('Ctrl Pts',(-0.115272874994606,5.23915579583016,2.09617159123155));
#9219=CARTESIAN_POINT('Ctrl Pts',(-0.173017885302765,5.24329474571061,2.10046267889747));
#9220=CARTESIAN_POINT('Ctrl Pts',(-0.230481701072578,5.24743369559106,2.10797938931007));
#9221=CARTESIAN_POINT('Ctrl Pts',(-0.287283205457954,5.25157264547151,2.11865361062951));
#9222=CARTESIAN_POINT('Ctrl Pts',(-0.344195114036731,5.25571964016395,2.12934857926554));
#9223=CARTESIAN_POINT('Ctrl Pts',(-0.400441631037956,5.25986663485638,2.14321319915192));
#9224=CARTESIAN_POINT('Ctrl Pts',(-0.455654023891854,5.26401362954881,2.16012863444274));
#9225=CARTESIAN_POINT('Ctrl Pts',(-0.507466510599438,5.26790525779153,2.17600243959509));
#9226=CARTESIAN_POINT('Ctrl Pts',(-0.558368129507022,5.27179688603425,2.19456229161848));
#9227=CARTESIAN_POINT('Ctrl Pts',(-0.608071567144028,5.27568851427696,2.21567200242989));
#9228=CARTESIAN_POINT('Ctrl Pts',(-0.661054498308607,5.27983691690472,2.23817455774595));
#9229=CARTESIAN_POINT('Ctrl Pts',(-0.712897604072605,5.28398531953248,2.26366927627782));
#9230=CARTESIAN_POINT('Ctrl Pts',(-0.763241019271799,5.28813372216024,2.29201872831324));
#9231=CARTESIAN_POINT('Ctrl Pts',(-0.813495076661055,5.2922747615177,2.32031786105789));
#9232=CARTESIAN_POINT('Ctrl Pts',(-0.86225427703073,5.29641580087517,2.35146141648696));
#9233=CARTESIAN_POINT('Ctrl Pts',(-0.909179922442212,5.30055684023263,2.38526447552244));
#9234=CARTESIAN_POINT('Ctrl Pts',(-0.956058977874828,5.30469376817225,2.41903397329749));
#9235=CARTESIAN_POINT('Ctrl Pts',(-1.00110766483905,5.30883069611187,2.45545744026071));
#9236=CARTESIAN_POINT('Ctrl Pts',(-1.04401456758374,5.31296762405148,2.49430564574116));
#9237=CARTESIAN_POINT('Ctrl Pts',(-1.08689535652621,5.317102034193,2.53313020760509));
#9238=CARTESIAN_POINT('Ctrl Pts',(-1.12763656001698,5.32123644433453,2.57437623387093));
#9239=CARTESIAN_POINT('Ctrl Pts',(-1.16596004471818,5.32537085447605,2.61777442957018));
#9240=CARTESIAN_POINT('Ctrl Pts',(-1.20427492947551,5.32950433683933,2.66116288654003));
#9241=CARTESIAN_POINT('Ctrl Pts',(-1.24017282806981,5.33363781920261,2.70670216401744));
#9242=CARTESIAN_POINT('Ctrl Pts',(-1.27341421348183,5.33777130156589,2.75408797502276));
#9243=CARTESIAN_POINT('Ctrl Pts',(-1.30668561779893,5.34190851670424,2.80151657817242));
#9244=CARTESIAN_POINT('Ctrl Pts',(-1.3372954141674,5.34604573184259,2.85079462055183));
#9245=CARTESIAN_POINT('Ctrl Pts',(-1.36504679451197,5.35018294698094,2.90158785877133));
#9246=CARTESIAN_POINT('Ctrl Pts',(-1.39280966904651,5.35432187568943,2.95240213475981));
#9247=CARTESIAN_POINT('Ctrl Pts',(-1.41771154198753,5.35846080439793,3.00473238704087));
#9248=CARTESIAN_POINT('Ctrl Pts',(-1.43960258938021,5.36259973310642,3.05822162891514));
#9249=CARTESIAN_POINT('Ctrl Pts',(-1.4615361889018,5.36674670712333,3.11181484393767));
#9250=CARTESIAN_POINT('Ctrl Pts',(-1.48044709586664,5.37089368114024,3.16657105698246));
#9251=CARTESIAN_POINT('Ctrl Pts',(-1.49623480202499,5.37504065515716,3.22211612741844));
#9252=CARTESIAN_POINT('Ctrl Pts',(-1.51105104947427,5.37893245505412,3.27424336489757));
#9253=CARTESIAN_POINT('Ctrl Pts',(-1.52311703828431,5.38282425495108,3.3270648830507));
#9254=CARTESIAN_POINT('Ctrl Pts',(-1.53239104897987,5.38671605484804,3.3802654301649));
#9255=CARTESIAN_POINT('Ctrl Pts',(-1.54227659502676,5.39086448300385,3.43697406200514));
#9256=CARTESIAN_POINT('Ctrl Pts',(-1.54903070265896,5.39501291115965,3.49435094749466));
#9257=CARTESIAN_POINT('Ctrl Pts',(-1.55257329113124,5.39916133931545,3.55201928458328));
#9258=CARTESIAN_POINT('Ctrl Pts',(-1.55610959145807,5.40330240395166,3.60958525954484));
#9259=CARTESIAN_POINT('Ctrl Pts',(-1.55644565569209,5.40744346858788,3.66744114383862));
#9260=CARTESIAN_POINT('Ctrl Pts',(-1.55355277362111,5.41158453322409,3.72520211298642));
#9261=CARTESIAN_POINT('Ctrl Pts',(-1.55066276383851,5.41572148627485,3.78290573235077));
#9262=CARTESIAN_POINT('Ctrl Pts',(-1.54455018566779,5.41985843932562,3.84051410586874));
#9263=CARTESIAN_POINT('Ctrl Pts',(-1.53523835277222,5.42399539237639,3.89764124683908));
#9264=CARTESIAN_POINT('Ctrl Pts',(-1.52593218763453,5.42812982742145,3.9547336166953));
#9265=CARTESIAN_POINT('Ctrl Pts',(-1.51343071143483,5.43226426246652,4.01134482177342));
#9266=CARTESIAN_POINT('Ctrl Pts',(-1.49780895477391,5.43639869751158,4.06709505798932));
#9267=CARTESIAN_POINT('Ctrl Pts',(-1.48219070461306,5.44053220453062,4.1228327803624));
#9268=CARTESIAN_POINT('Ctrl Pts',(-1.46345370489614,5.44466571154965,4.1777094164092));
#9269=CARTESIAN_POINT('Ctrl Pts',(-1.44172333621145,5.44879921856869,4.23135856976901));
#9270=CARTESIAN_POINT('Ctrl Pts',(-1.41997334691544,5.45293645778094,4.28505616359482));
#9271=CARTESIAN_POINT('Ctrl Pts',(-1.39522478243097,5.4570736969932,4.33752357571357));
#9272=CARTESIAN_POINT('Ctrl Pts',(-1.36765137923411,5.46121093620545,4.38841400573146));
#9273=CARTESIAN_POINT('Ctrl Pts',(-1.3400665574826,5.46534988870974,4.43932551023016));
#9274=CARTESIAN_POINT('Ctrl Pts',(-1.3096548376794,5.46948884121402,4.48865828586489));
#9275=CARTESIAN_POINT('Ctrl Pts',(-1.27663457277853,5.47362779371831,4.53609262715818));
#9276=CARTESIAN_POINT('Ctrl Pts',(-1.24355012920008,5.47777479075219,4.58361916254213));
#9277=CARTESIAN_POINT('Ctrl Pts',(-1.20784733002482,5.48192178778608,4.62923947777169));
#9278=CARTESIAN_POINT('Ctrl Pts',(-1.16978571820343,5.48606878481996,4.67266595598227));
#9279=CARTESIAN_POINT('Ctrl Pts',(-1.13406813706516,5.48996038835301,4.71341800732246));
#9280=CARTESIAN_POINT('Ctrl Pts',(-1.09627396077845,5.49385199188607,4.75223819906194));
#9281=CARTESIAN_POINT('Ctrl Pts',(-1.05664517948853,5.49774359541912,4.78892029570244));
#9282=CARTESIAN_POINT('Ctrl Pts',(-1.01440083906866,5.50189205063471,4.82802346585696));
#9283=CARTESIAN_POINT('Ctrl Pts',(-0.969894475223351,5.50604050585029,4.8648603570922));
#9284=CARTESIAN_POINT('Ctrl Pts',(-0.923398966675603,5.51018896106588,4.8991590621043));
#9285=CARTESIAN_POINT('Ctrl Pts',(-0.876985981675346,5.51433005330703,4.93339689132646));
#9286=CARTESIAN_POINT('Ctrl Pts',(-0.82859127507044,5.51847114554817,4.96510516952084));
#9287=CARTESIAN_POINT('Ctrl Pts',(-0.778522364130129,5.52261223778932,4.99405076390991));
#9288=CARTESIAN_POINT('Ctrl Pts',(-0.728503161574028,5.52674921875662,5.02296762113054));
#9289=CARTESIAN_POINT('Ctrl Pts',(-0.676813496421531,5.53088619972392,5.04912696958259));
#9290=CARTESIAN_POINT('Ctrl Pts',(-0.623790119403965,5.53502318069121,5.07233872576694));
#9291=CARTESIAN_POINT('Ctrl Pts',(-0.570799012131173,5.53915764391393,5.09553635540014));
#9292=CARTESIAN_POINT('Ctrl Pts',(-0.516476278018669,5.54329210713666,5.11578974041624));
#9293=CARTESIAN_POINT('Ctrl Pts',(-0.461181567724967,5.54742657035938,5.13295557829946));
#9294=CARTESIAN_POINT('Ctrl Pts',(-0.405899266118428,5.55156010576712,5.15011756399662));
#9295=CARTESIAN_POINT('Ctrl Pts',(-0.349645918398432,5.55569364117485,5.1641932238359));
#9296=CARTESIAN_POINT('Ctrl Pts',(-0.292797266397992,5.55982717658259,5.17508881297127));
#9297=CARTESIAN_POINT('Ctrl Pts',(-0.235897284068059,5.56396444428172,5.18599424005637));
#9298=CARTESIAN_POINT('Ctrl Pts',(-0.178401435691084,5.56810171198085,5.19371375896985));
#9299=CARTESIAN_POINT('Ctrl Pts',(-0.120695275443355,5.57223897967997,5.19820486948888));
#9300=CARTESIAN_POINT('Ctrl Pts',(-0.0629652169800224,5.57637796077183,
5.2026978399398));
#9301=CARTESIAN_POINT('Ctrl Pts',(-0.00502519466757172,5.58051694186369,
5.2039597239652));
#9302=CARTESIAN_POINT('Ctrl Pts',(0.0527377522754739,5.58465592295555,5.20200019948549));
#9303=CARTESIAN_POINT('Ctrl Pts',(0.110612964446322,5.58880294836786,5.20003686657021));
#9304=CARTESIAN_POINT('Ctrl Pts',(0.168309892939886,5.59294997378016,5.19483965925701));
#9305=CARTESIAN_POINT('Ctrl Pts',(0.225446067434111,5.59709699919247,5.18647026910672));
#9306=CARTESIAN_POINT('Ctrl Pts',(0.279060039765969,5.60098837812505,5.17861681626491));
#9307=CARTESIAN_POINT('Ctrl Pts',(0.332179991546601,5.60487975705762,5.16797080129299));
#9308=CARTESIAN_POINT('Ctrl Pts',(0.384501375266136,5.6087711359902,5.15462336344825));
#9309=CARTESIAN_POINT('Ctrl Pts',(0.440277239262835,5.61291944031003,5.14039467099007));
#9310=CARTESIAN_POINT('Ctrl Pts',(0.495379075984238,5.61706774462986,5.12303596400893));
#9311=CARTESIAN_POINT('Ctrl Pts',(0.549430385440946,5.62121604894968,5.10262864241332));
#9312=CARTESIAN_POINT('Ctrl Pts',(0.603385754467325,5.62535699007876,5.08225754357041));
#9313=CARTESIAN_POINT('Ctrl Pts',(0.656293814205358,5.62949793120784,5.05884875313529));
#9314=CARTESIAN_POINT('Ctrl Pts',(0.707791803327991,5.63363887233692,5.03253381619862));
#9315=CARTESIAN_POINT('Ctrl Pts',(0.759238663028474,5.63777570216126,5.006245005865));
#9316=CARTESIAN_POINT('Ctrl Pts',(0.809277764542756,5.64191253198559,4.97705600153326));
#9317=CARTESIAN_POINT('Ctrl Pts',(0.857566610935065,5.64604936180993,4.94514627730181));
#9318=CARTESIAN_POINT('Ctrl Pts',(0.905826070514475,5.65018367411204,4.91325597215295));
#9319=CARTESIAN_POINT('Ctrl Pts',(0.952336952841351,5.65431798641414,4.87864851575008));
#9320=CARTESIAN_POINT('Ctrl Pts',(0.996783599410229,5.65845229871625,4.8415480203645));
#9321=CARTESIAN_POINT('Ctrl Pts',(1.04122027645305,5.66258568367879,4.80445584673959));
#9322=CARTESIAN_POINT('Ctrl Pts',(1.08359323739862,5.66671906864133,4.7648720778326));
#9323=CARTESIAN_POINT('Ctrl Pts',(1.12361969242522,5.67085245360386,4.72306125534864));
#9324=CARTESIAN_POINT('Ctrl Pts',(1.16368230868329,5.67498957280393,4.68121265957627));
#9325=CARTESIAN_POINT('Ctrl Pts',(1.20139382085382,5.67912669200399,4.6371333657748));
#9326=CARTESIAN_POINT('Ctrl Pts',(1.23650913495829,5.68326381120405,4.59112398947344));
#9327=CARTESIAN_POINT('Ctrl Pts',(1.27163899905214,5.68740264461462,4.54509554924077));
#9328=CARTESIAN_POINT('Ctrl Pts',(1.30417022656156,5.69154147802519,4.49713586336888));
#9329=CARTESIAN_POINT('Ctrl Pts',(1.33390072694397,5.69568031143576,4.44757513579487));
#9330=CARTESIAN_POINT('Ctrl Pts',(1.36368903594959,5.69982719248287,4.39791804127818));
#9331=CARTESIAN_POINT('Ctrl Pts',(1.39066549083344,5.70397407352997,4.34665414594402));
#9332=CARTESIAN_POINT('Ctrl Pts',(1.41467415468491,5.70812095457708,4.29413806977254));
#9333=CARTESIAN_POINT('Ctrl Pts',(1.4372104897027,5.71201352857181,4.24484253655411));
#9334=CARTESIAN_POINT('Ctrl Pts',(1.45713220257539,5.71590610256655,4.19444423214131));
#9335=CARTESIAN_POINT('Ctrl Pts',(1.47435032060801,5.71979867656128,4.14324866270301));
#9336=CARTESIAN_POINT('Ctrl Pts',(1.49606381173456,5.72470753888491,4.07868675526277));
#9337=CARTESIAN_POINT('Ctrl Pts',(1.51355274598842,5.72961640120853,4.01263698113696));
#9338=CARTESIAN_POINT('Ctrl Pts',(1.52664550808754,5.73452526353215,3.94561207781779));
#9339=CARTESIAN_POINT('Ctrl Pts',(1.53959353558512,5.73937986058868,3.879328104686));
#9340=CARTESIAN_POINT('Ctrl Pts',(1.54824196854562,5.7442344576452,3.81209054589745));
#9341=CARTESIAN_POINT('Ctrl Pts',(1.55247128364616,5.74908905470172,3.74441592701353));
#9342=CARTESIAN_POINT('Ctrl Pts',(1.55446188960699,5.75137396126658,3.71256360659188));
#9343=CARTESIAN_POINT('Ctrl Pts',(1.55547421228667,5.75365886783144,3.68061475333113));
#9344=CARTESIAN_POINT('Ctrl Pts',(1.5554995134887,5.7559437743963,3.64862472695888));
#9345=CARTESIAN_POINT('Origin',(-2.67773308947627E-16,1.2059437743963,3.64739446828387));
#9346=CARTESIAN_POINT('',(1.55549999978821,6.5940562256037,3.64736879997355));
#9347=CARTESIAN_POINT('',(1.55498804050902,6.4559437743963,3.64654572419703));
#9348=CARTESIAN_POINT('',(1.5555,1.2059437743963,3.64739446828386));
#9349=CARTESIAN_POINT('Ctrl Pts',(1.55549964733824,5.89405622564623,3.64634702825329));
#9350=CARTESIAN_POINT('Ctrl Pts',(1.55545520190131,5.8987664550661,3.58034338179295));
#9351=CARTESIAN_POINT('Ctrl Pts',(1.5512056609363,5.90347668448598,3.51450400917047));
#9352=CARTESIAN_POINT('Ctrl Pts',(1.54283758956271,5.90818691390586,3.44932270797381));
#9353=CARTESIAN_POINT('Ctrl Pts',(1.53439597916476,5.91293853705441,3.38356859028426));
#9354=CARTESIAN_POINT('Ctrl Pts',(1.5217632534121,5.91769016020297,3.31848438005986));
#9355=CARTESIAN_POINT('Ctrl Pts',(1.50507796139441,5.92244178335153,3.25455788632538));
#9356=CARTESIAN_POINT('Ctrl Pts',(1.49174251234781,5.9262394410922,3.20346567295443));
#9357=CARTESIAN_POINT('Ctrl Pts',(1.47581937761426,5.93003709883287,3.15311264217503));
#9358=CARTESIAN_POINT('Ctrl Pts',(1.4574010096598,5.93383475657353,3.10373782384495));
#9359=CARTESIAN_POINT('Ctrl Pts',(1.43727628109979,5.93798424644059,3.0497886998482));
#9360=CARTESIAN_POINT('Ctrl Pts',(1.41410998760309,5.94213373630765,2.99684609065117));
#9361=CARTESIAN_POINT('Ctrl Pts',(1.38802361564244,5.94628322617471,2.94527575152801));
#9362=CARTESIAN_POINT('Ctrl Pts',(1.36198340764074,5.95042537286349,2.89379667427224));
#9363=CARTESIAN_POINT('Ctrl Pts',(1.33303361120312,5.95456751955227,2.84368550740763));
#9364=CARTESIAN_POINT('Ctrl Pts',(1.30134408932062,5.95870966624105,2.79528895181876));
#9365=CARTESIAN_POINT('Ctrl Pts',(1.26968593451922,5.96284771292947,2.74694030035068));
#9366=CARTESIAN_POINT('Ctrl Pts',(1.2352937110507,5.9669857596179,2.70030333063741));
#9367=CARTESIAN_POINT('Ctrl Pts',(1.1983827542823,5.97112380630632,2.65569944246254));
#9368=CARTESIAN_POINT('Ctrl Pts',(1.16149417217826,5.97525934459577,2.61112259224915));
#9369=CARTESIAN_POINT('Ctrl Pts',(1.1220902145225,5.97939488288523,2.56857678059709));
#9370=CARTESIAN_POINT('Ctrl Pts',(1.08042771304446,5.98353042117469,2.52835192803551));
#9371=CARTESIAN_POINT('Ctrl Pts',(1.03877448374495,5.98766503908135,2.48813602769717));
#9372=CARTESIAN_POINT('Ctrl Pts',(0.994864082749182,5.99179965698802,2.45024042219376));
#9373=CARTESIAN_POINT('Ctrl Pts',(0.948990009129902,5.99593427489469,2.41491801310445));
#9374=CARTESIAN_POINT('Ctrl Pts',(0.903074494523561,6.00007262786636,2.37956369502206));
#9375=CARTESIAN_POINT('Ctrl Pts',(0.855192174987022,6.00421098083804,2.34678753775245));
#9376=CARTESIAN_POINT('Ctrl Pts',(0.805668371193128,6.00834933380971,2.31680109476249));
#9377=CARTESIAN_POINT('Ctrl Pts',(0.756124023673007,6.01248940347485,2.28680221263765));
#9378=CARTESIAN_POINT('Ctrl Pts',(0.704937294292784,6.01662947314,2.2595955977478));
#9379=CARTESIAN_POINT('Ctrl Pts',(0.652458312882739,6.02076954280514,2.23534687703554));
#9380=CARTESIAN_POINT('Ctrl Pts',(0.599877475057094,6.02491764792839,2.21105109199946));
#9381=CARTESIAN_POINT('Ctrl Pts',(0.5459998582304,6.02906575305163,2.18972486694803));
#9382=CARTESIAN_POINT('Ctrl Pts',(0.491194922589105,6.03321385817488,2.17148532540865));
#9383=CARTESIAN_POINT('Ctrl Pts',(0.439895037533934,6.03709667116479,2.15441229405699));
#9384=CARTESIAN_POINT('Ctrl Pts',(0.387783153444932,6.0409794841547,2.14004335041999));
#9385=CARTESIAN_POINT('Ctrl Pts',(0.335170067944931,6.04486229714461,2.12843387776357));
#9386=CARTESIAN_POINT('Ctrl Pts',(0.279034259797698,6.04900508487512,2.11604708988489));
#9387=CARTESIAN_POINT('Ctrl Pts',(0.22209136397401,6.05314787260562,2.10675003836955));
#9388=CARTESIAN_POINT('Ctrl Pts',(0.164713239438893,6.05729066033612,2.10063986630153));
#9389=CARTESIAN_POINT('Ctrl Pts',(0.107437185811349,6.06142607839208,2.09454056372103));
#9390=CARTESIAN_POINT('Ctrl Pts',(0.0497279550305338,6.06556149644804,2.09161694391283));
#9391=CARTESIAN_POINT('Ctrl Pts',(-0.00803220328827441,6.06969691450401,
2.09191520654158));
#9392=CARTESIAN_POINT('Ctrl Pts',(-0.0657349316439698,6.07382822078269,
2.09221317261277));
#9393=CARTESIAN_POINT('Ctrl Pts',(-0.123487967648636,6.07795952706138,2.09572667211675));
#9394=CARTESIAN_POINT('Ctrl Pts',(-0.180905515729008,6.08209083334007,2.10244998889996));
#9395=CARTESIAN_POINT('Ctrl Pts',(-0.238288194124668,6.08621963067589,2.10916922261198));
#9396=CARTESIAN_POINT('Ctrl Pts',(-0.295335270781317,6.09034842801172,2.11909434928145));
#9397=CARTESIAN_POINT('Ctrl Pts',(-0.351664776387442,6.09447722534754,2.13216770801055));
#9398=CARTESIAN_POINT('Ctrl Pts',(-0.407981870661645,6.09860511296698,2.14523818622805));
#9399=CARTESIAN_POINT('Ctrl Pts',(-0.463581199258403,6.10273300058642,2.16145540146297));
#9400=CARTESIAN_POINT('Ctrl Pts',(-0.518091919598055,6.10686088820586,2.18071078976038));
#9401=CARTESIAN_POINT('Ctrl Pts',(-0.572652892458911,6.11099258125585,2.19998392927815));
#9402=CARTESIAN_POINT('Ctrl Pts',(-0.626122757588664,6.11512427430583,2.22230066550838));
#9403=CARTESIAN_POINT('Ctrl Pts',(-0.678148079973918,6.11925596735582,2.24750324692855));
#9404=CARTESIAN_POINT('Ctrl Pts',(-0.730195361219324,6.12338940431177,2.27271646586013));
#9405=CARTESIAN_POINT('Ctrl Pts',(-0.780796426362216,6.12752284126771,2.30081770465715));
#9406=CARTESIAN_POINT('Ctrl Pts',(-0.829622938255556,6.13165627822366,2.331603439921));
#9407=CARTESIAN_POINT('Ctrl Pts',(-0.878545941878122,6.13579788374344,2.36245001444442));
#9408=CARTESIAN_POINT('Ctrl Pts',(-0.925686956785633,6.13993948926323,2.39599138361088));
#9409=CARTESIAN_POINT('Ctrl Pts',(-0.970747883840826,6.14408109478302,2.43198145370053));
#9410=CARTESIAN_POINT('Ctrl Pts',(-1.01357450436761,6.14801734242724,2.46618698774501));
#9411=CARTESIAN_POINT('Ctrl Pts',(-1.05452218822353,6.15195359007147,2.50260381659366));
#9412=CARTESIAN_POINT('Ctrl Pts',(-1.09336663524267,6.15588983771569,2.54099054071577));
#9413=CARTESIAN_POINT('Ctrl Pts',(-1.13438238376156,6.16004611115688,2.58152298084243));
#9414=CARTESIAN_POINT('Ctrl Pts',(-1.17322572607311,6.16420238459808,2.62442275623432));
#9415=CARTESIAN_POINT('Ctrl Pts',(-1.20961240641222,6.16835865803927,2.66942817221143));
#9416=CARTESIAN_POINT('Ctrl Pts',(-1.24593408982706,6.17250750719808,2.7143531957596));
#9417=CARTESIAN_POINT('Ctrl Pts',(-1.27980749926491,6.17665635635688,2.76137599322715));
#9418=CARTESIAN_POINT('Ctrl Pts',(-1.31098563418946,6.18080520551568,2.81019860294001));
#9419=CARTESIAN_POINT('Ctrl Pts',(-1.34213255272879,6.18494990073539,2.85897233014607));
#9420=CARTESIAN_POINT('Ctrl Pts',(-1.37058926659056,6.1890945959551,2.90954186382704));
#9421=CARTESIAN_POINT('Ctrl Pts',(-1.39615050966621,6.19323929117481,2.96157816317092));
#9422=CARTESIAN_POINT('Ctrl Pts',(-1.42169588327082,6.19738141319725,3.0135821562399));
#9423=CARTESIAN_POINT('Ctrl Pts',(-1.44434912188288,6.20152353521969,3.06705064508012));
#9424=CARTESIAN_POINT('Ctrl Pts',(-1.46395068420033,6.20566565724214,3.12162964991982));
#9425=CARTESIAN_POINT('Ctrl Pts',(-1.48354753270481,6.20980678316089,3.17619552951894));
#9426=CARTESIAN_POINT('Ctrl Pts',(-1.50009398675634,6.21394790907964,3.23187090709963));
#9427=CARTESIAN_POINT('Ctrl Pts',(-1.513479294399,6.2180890349984,3.28828351686981));
#9428=CARTESIAN_POINT('Ctrl Pts',(-1.52687612511417,6.22223372590763,3.34474469082773));
#9429=CARTESIAN_POINT('Ctrl Pts',(-1.53710624944037,6.22637841681685,3.40194385993304));
#9430=CARTESIAN_POINT('Ctrl Pts',(-1.5441096675528,6.23052310772608,3.4594966647576));
#9431=CARTESIAN_POINT('Ctrl Pts',(-1.55111584629894,6.23466943240518,3.51707215596341));
#9432=CARTESIAN_POINT('Ctrl Pts',(-1.55489274683005,6.23881575708427,3.57500104238098));
#9433=CARTESIAN_POINT('Ctrl Pts',(-1.55543242157753,6.24296208176336,3.63289509224643));
#9434=CARTESIAN_POINT('Ctrl Pts',(-1.55597311345118,6.24711622102969,3.69089825515483));
#9435=CARTESIAN_POINT('Ctrl Pts',(-1.55326440933669,6.25127036029601,3.74886593033459));
#9436=CARTESIAN_POINT('Ctrl Pts',(-1.54735052601686,6.25542449956233,3.80641207622512));
#9437=CARTESIAN_POINT('Ctrl Pts',(-1.54189672524708,6.25925545913714,3.85948130295519));
#9438=CARTESIAN_POINT('Ctrl Pts',(-1.53371769744795,6.26308641871195,3.91219178420149));
#9439=CARTESIAN_POINT('Ctrl Pts',(-1.52288640708489,6.26691737828676,3.96424970512882));
#9440=CARTESIAN_POINT('Ctrl Pts',(-1.51114266458232,6.27107106646946,4.02069310181546));
#9441=CARTESIAN_POINT('Ctrl Pts',(-1.49623281783691,6.27522475465216,4.07659759798717));
#9442=CARTESIAN_POINT('Ctrl Pts',(-1.47822260570092,6.27937844283486,4.13158263211565));
#9443=CARTESIAN_POINT('Ctrl Pts',(-1.460243690403,6.28352491304002,4.1864721172469));
#9444=CARTESIAN_POINT('Ctrl Pts',(-1.43917526453003,6.28767138324519,4.24044482260319));
#9445=CARTESIAN_POINT('Ctrl Pts',(-1.41513374529266,6.29181785345036,4.29313182428395));
#9446=CARTESIAN_POINT('Ctrl Pts',(-1.39111557691066,6.29596029630497,4.34576765255325));
#9447=CARTESIAN_POINT('Ctrl Pts',(-1.36413025170531,6.30010273915958,4.39711978172299));
#9448=CARTESIAN_POINT('Ctrl Pts',(-1.33434292531336,6.30424518201418,4.44683752921203));
#9449=CARTESIAN_POINT('Ctrl Pts',(-1.30457317577932,6.30838518050274,4.49652593933218));
#9450=CARTESIAN_POINT('Ctrl Pts',(-1.2720049692522,6.31252517899129,4.54458143538888));
#9451=CARTESIAN_POINT('Ctrl Pts',(-1.23684919659392,6.31666517747985,4.59067826168063));
#9452=CARTESIAN_POINT('Ctrl Pts',(-1.20170076825582,6.32080431108983,4.63676545797918));
#9453=CARTESIAN_POINT('Ctrl Pts',(-1.1639661618001,6.32494344469982,4.68089438451617));
#9454=CARTESIAN_POINT('Ctrl Pts',(-1.12389806613617,6.3290825783098,4.72277039647614));
#9455=CARTESIAN_POINT('Ctrl Pts',(-1.08379334396079,6.33322549552921,4.76468468757582));
#9456=CARTESIAN_POINT('Ctrl Pts',(-1.04135122909556,6.33736841274863,4.80434157222005));
#9457=CARTESIAN_POINT('Ctrl Pts',(-0.996862078378742,6.34151132996804,4.84148250804075));
#9458=CARTESIAN_POINT('Ctrl Pts',(-0.952354128903536,6.34565599776481,4.87863913765347));
#9459=CARTESIAN_POINT('Ctrl Pts',(-0.905797835747481,6.34980066556158,4.91327738756306));
#9460=CARTESIAN_POINT('Ctrl Pts',(-0.857514990188483,6.35394533335835,4.94518038730212));
#9461=CARTESIAN_POINT('Ctrl Pts',(-0.809138592895801,6.35809803176834,4.97714520156145));
#9462=CARTESIAN_POINT('Ctrl Pts',(-0.759029407425855,6.36225073017833,5.0063639114422));
#9463=CARTESIAN_POINT('Ctrl Pts',(-0.707535639226758,6.36640342858832,5.03266468352131));
#9464=CARTESIAN_POINT('Ctrl Pts',(-0.659830527519038,6.37025059201149,5.05703037501979));
#9465=CARTESIAN_POINT('Ctrl Pts',(-0.610937638366417,6.37409775543467,5.07889208943651));
#9466=CARTESIAN_POINT('Ctrl Pts',(-0.561147201320725,6.37794491885785,5.09815084633289));
#9467=CARTESIAN_POINT('Ctrl Pts',(-0.508025345062969,6.38204949143226,5.11869818385905));
#9468=CARTESIAN_POINT('Ctrl Pts',(-0.453648599692884,6.38615406400668,5.13637204992538));
#9469=CARTESIAN_POINT('Ctrl Pts',(-0.398362951921492,6.3902586365811,5.15101915833668));
#9470=CARTESIAN_POINT('Ctrl Pts',(-0.342962769754882,6.39437171253309,5.16569661092899));
#9471=CARTESIAN_POINT('Ctrl Pts',(-0.286650394655885,6.39848478848509,5.17733450259257));
#9472=CARTESIAN_POINT('Ctrl Pts',(-0.22979457218428,6.40259786443708,5.18582701623475));
#9473=CARTESIAN_POINT('Ctrl Pts',(-0.173213084478156,6.40669109440536,5.19427855268872));
#9474=CARTESIAN_POINT('Ctrl Pts',(-0.116093905813107,6.41078432437364,5.19961488454923));
#9475=CARTESIAN_POINT('Ctrl Pts',(-0.0588132952565892,6.41487755434192,
5.20178220829634));
#9476=CARTESIAN_POINT('Ctrl Pts',(-0.00156603026122423,6.41896840146112,
5.20394827034903));
#9477=CARTESIAN_POINT('Ctrl Pts',(0.055841949335377,6.42305924858032,5.20294895786843));
#9478=CARTESIAN_POINT('Ctrl Pts',(0.113030086156636,6.42715009569952,5.19878237903457));
#9479=CARTESIAN_POINT('Ctrl Pts',(0.170208018481566,6.43124021285903,5.19461654367376));
#9480=CARTESIAN_POINT('Ctrl Pts',(0.22716565483362,6.43533033001855,5.18728460211642));
#9481=CARTESIAN_POINT('Ctrl Pts',(0.283525656181328,6.43942044717806,5.17683667127388));
#9482=CARTESIAN_POINT('Ctrl Pts',(0.340426053087732,6.4435497815323,5.16628856272926));
#9483=CARTESIAN_POINT('Ctrl Pts',(0.396716744592929,6.44767911588654,5.15256446132537));
#9484=CARTESIAN_POINT('Ctrl Pts',(0.452020739194503,6.45180845024077,5.13576858164988));
#9485=CARTESIAN_POINT('Ctrl Pts',(0.506884898051872,6.45590494376928,5.11910628053937));
#9486=CARTESIAN_POINT('Ctrl Pts',(0.560777515795683,6.4600014372978,5.09942113678421));
#9487=CARTESIAN_POINT('Ctrl Pts',(0.613349278357484,6.46409793082631,5.0768639197722));
#9488=CARTESIAN_POINT('Ctrl Pts',(0.666553227964308,6.46824368559341,5.05403544724826));
#9489=CARTESIAN_POINT('Ctrl Pts',(0.718403838885254,6.47238944036051,5.02826561058249));
#9490=CARTESIAN_POINT('Ctrl Pts',(0.768565993296087,6.47653519512761,4.99975779370674));
#9491=CARTESIAN_POINT('Ctrl Pts',(0.818728147706923,6.48068094989471,4.97124997683099));
#9492=CARTESIAN_POINT('Ctrl Pts',(0.867201424458467,6.48482670466182,4.94000455072265));
#9493=CARTESIAN_POINT('Ctrl Pts',(0.913684566917058,6.48897245942892,4.90626728242261));
#9494=CARTESIAN_POINT('Ctrl Pts',(0.962777192462072,6.4933509496862,4.87063606232941));
#9495=CARTESIAN_POINT('Ctrl Pts',(1.00987680836232,6.49772943994348,4.83206076559068));
#9496=CARTESIAN_POINT('Ctrl Pts',(1.05462032230712,6.50210793020077,4.79079126108015));
#9497=CARTESIAN_POINT('Ctrl Pts',(1.09777523852538,6.50633096419064,4.75098701120122));
#9498=CARTESIAN_POINT('Ctrl Pts',(1.13873813199973,6.51055399818052,4.70867701401803));
#9499=CARTESIAN_POINT('Ctrl Pts',(1.17721363608817,6.5147770321704,4.66412860512008));
#9500=CARTESIAN_POINT('Ctrl Pts',(1.21564211240262,6.51899490443744,4.61963464677593));
#9501=CARTESIAN_POINT('Ctrl Pts',(1.25158891032137,6.52321277670449,4.57290807962868));
#9502=CARTESIAN_POINT('Ctrl Pts',(1.28479547448401,6.52743064897153,4.52425297382819));
#9503=CARTESIAN_POINT('Ctrl Pts',(1.31797247820949,6.53164476649456,4.4756411807351));
#9504=CARTESIAN_POINT('Ctrl Pts',(1.34841381229424,6.53585888401758,4.42510466592981));
#9505=CARTESIAN_POINT('Ctrl Pts',(1.37590239079675,6.54007300154061,4.37297896439703));
#9506=CARTESIAN_POINT('Ctrl Pts',(1.40337562050346,6.54428476602711,4.32088236828884));
#9507=CARTESIAN_POINT('Ctrl Pts',(1.42789913910851,6.5484965305136,4.26719878661907));
#9508=CARTESIAN_POINT('Ctrl Pts',(1.44930121642437,6.5527082950001,4.21228935591415));
#9509=CARTESIAN_POINT('Ctrl Pts',(1.47070504865124,6.55692040483961,4.15737542278817));
#9510=CARTESIAN_POINT('Ctrl Pts',(1.48898673885858,6.56113251467912,4.10123589863118));
#9511=CARTESIAN_POINT('Ctrl Pts',(1.50402284555276,6.56534462451862,4.04425153330273));
#9512=CARTESIAN_POINT('Ctrl Pts',(1.51905965343888,6.56955693078514,3.9872645105724));
#9513=CARTESIAN_POINT('Ctrl Pts',(1.53085045935565,6.57376923705166,3.92943305062013));
#9514=CARTESIAN_POINT('Ctrl Pts',(1.53932242567221,6.57798154331818,3.87115040635621));
#9515=CARTESIAN_POINT('Ctrl Pts',(1.54780101708119,6.58219714361554,3.81282218496285));
#9516=CARTESIAN_POINT('Ctrl Pts',(1.55295552961869,6.58641274391291,3.75404256799067));
#9517=CARTESIAN_POINT('Ctrl Pts',(1.55476488354476,6.59062834421027,3.69521085560087));
#9518=CARTESIAN_POINT('Ctrl Pts',(1.55525530406377,6.59177097134141,3.67926467806828));
#9519=CARTESIAN_POINT('Ctrl Pts',(1.55550026292146,6.59291359847256,3.66331467869636));
#9520=CARTESIAN_POINT('Ctrl Pts',(1.55549999978821,6.5940562256037,3.64736879997355));
#9521=CARTESIAN_POINT('Ctrl Pts',(1.55415988380114,5.7559437743963,3.64862366743361));
#9522=CARTESIAN_POINT('Ctrl Pts',(1.55156969786396,5.78090458864165,3.29945639063284));
#9523=CARTESIAN_POINT('Ctrl Pts',(1.26257785748727,5.84287458307736,2.42869791902303));
#9524=CARTESIAN_POINT('Ctrl Pts',(-0.17968266065122,5.94185375770343,1.81826775193874));
#9525=CARTESIAN_POINT('Ctrl Pts',(-1.63338127522104,6.05288129827452,2.80478342088779));
#9526=CARTESIAN_POINT('Ctrl Pts',(-1.5946610617751,6.16390883884559,4.56100604319437));
#9527=CARTESIAN_POINT('Ctrl Pts',(-0.0991443931483716,6.27493637941668,
5.48278383251785));
#9528=CARTESIAN_POINT('Ctrl Pts',(1.29176384967164,6.37228135793357,4.82025828670267));
#9529=CARTESIAN_POINT('Ctrl Pts',(1.55167090461383,6.43261715626011,3.97306868873034));
#9530=CARTESIAN_POINT('Ctrl Pts',(1.55356356749417,6.4559437743963,3.64654650170336));
#9531=CARTESIAN_POINT('Origin',(0.,0.,3.64739446828387));
#9532=CARTESIAN_POINT('',(1.95399957629683,2.72586969217418,3.64868125956088));
#9533=CARTESIAN_POINT('',(1.95399895847038,2.6241303079204,3.64941196591101));
#9534=CARTESIAN_POINT('',(1.954,4.33875158023511E-16,3.64739446828387));
#9535=CARTESIAN_POINT('',(-0.861527974718931,2.50004110459941,5.40121474093917));
#9536=CARTESIAN_POINT('Ctrl Pts',(1.95399957629626,2.72586969212423,3.64868126043293));
#9537=CARTESIAN_POINT('Ctrl Pts',(1.95395422424648,2.72192515475357,3.71754854884412));
#9538=CARTESIAN_POINT('Ctrl Pts',(1.95026833624108,2.71798061738291,3.78630291233304));
#9539=CARTESIAN_POINT('Ctrl Pts',(1.94297611333583,2.71403608001225,3.85466198384382));
#9540=CARTESIAN_POINT('Ctrl Pts',(1.93571830868517,2.71011016029676,3.92269841026301));
#9541=CARTESIAN_POINT('Ctrl Pts',(1.9248684896971,2.70618424058127,3.99048552896689));
#9542=CARTESIAN_POINT('Ctrl Pts',(1.91045410367944,2.70225832086578,4.05761528410676));
#9543=CARTESIAN_POINT('Ctrl Pts',(1.8960614340148,2.69833831584263,4.12464390323853));
#9544=CARTESIAN_POINT('Ctrl Pts',(1.87811495873726,2.69441831081948,4.19101664947787));
#9545=CARTESIAN_POINT('Ctrl Pts',(1.85669380632823,2.69049830579632,4.25633133655707));
#9546=CARTESIAN_POINT('Ctrl Pts',(1.83529812509749,2.68658296192047,4.32156836011904));
#9547=CARTESIAN_POINT('Ctrl Pts',(1.81043612540151,2.68266761804462,4.38574936031787));
#9548=CARTESIAN_POINT('Ctrl Pts',(1.7822374088651,2.67875227416877,4.44848486171136));
#9549=CARTESIAN_POINT('Ctrl Pts',(1.75405663245768,2.67483942124935,4.51118045054408));
#9550=CARTESIAN_POINT('Ctrl Pts',(1.72254355119803,2.67092656832992,4.57243191939909));
#9551=CARTESIAN_POINT('Ctrl Pts',(1.68787623580038,2.6670137154105,4.63186885221691));
#9552=CARTESIAN_POINT('Ctrl Pts',(1.65321921124911,2.66310202400496,4.69128814143188));
#9553=CARTESIAN_POINT('Ctrl Pts',(1.61541005819025,2.65919033259943,4.74889354119141));
#9554=CARTESIAN_POINT('Ctrl Pts',(1.57467238540507,2.65527864119389,4.80433996338842));
#9555=CARTESIAN_POINT('Ctrl Pts',(1.5339329814046,2.65136678355451,4.85978874187353));
#9556=CARTESIAN_POINT('Ctrl Pts',(1.49026510259552,2.64745492591513,4.91307796744393));
#9557=CARTESIAN_POINT('Ctrl Pts',(1.44393413822844,2.64354306827575,4.96389369139739));
#9558=CARTESIAN_POINT('Ctrl Pts',(1.39755578074633,2.63962720909827,5.01476139603986));
#9559=CARTESIAN_POINT('Ctrl Pts',(1.34850923151036,2.6357113499208,5.06315018672279));
#9560=CARTESIAN_POINT('Ctrl Pts',(1.29709774028559,2.63179549074332,5.10878197751816));
#9561=CARTESIAN_POINT('Ctrl Pts',(1.24565650863508,2.62787736632676,5.15444016530871));
#9562=CARTESIAN_POINT('Ctrl Pts',(1.19184799458143,2.6239592419102,5.1973378728402));
#9563=CARTESIAN_POINT('Ctrl Pts',(1.13600746521101,2.62004111749364,5.23723818355429));
#9564=CARTESIAN_POINT('Ctrl Pts',(1.08007370311047,2.61611645127957,5.27720511281484));
#9565=CARTESIAN_POINT('Ctrl Pts',(1.02210156682617,2.61219178506549,5.31416439325118));
#9566=CARTESIAN_POINT('Ctrl Pts',(0.962453365994499,2.60826711885142,5.34792365600335));
#9567=CARTESIAN_POINT('Ctrl Pts',(0.935812900823456,2.606514259048,5.36300143623828));
#9568=CARTESIAN_POINT('Ctrl Pts',(0.908838399944807,2.60476139924459,5.37744152154718));
#9569=CARTESIAN_POINT('Ctrl Pts',(0.881563413985291,2.60300853944117,5.39122988113756));
#9570=CARTESIAN_POINT('Ctrl Pts',(0.821169396672914,2.59912724522269,5.4217609482863));
#9571=CARTESIAN_POINT('Ctrl Pts',(0.759058631374219,2.59524595100421,5.44921582459446));
#9572=CARTESIAN_POINT('Ctrl Pts',(0.695580341215194,2.59136465678573,5.47339665582773));
#9573=CARTESIAN_POINT('Ctrl Pts',(0.632208367608052,2.58748986314906,5.49753698781957));
#9574=CARTESIAN_POINT('Ctrl Pts',(0.567473881608393,2.58361506951239,5.51841398464903));
#9575=CARTESIAN_POINT('Ctrl Pts',(0.50174941555491,2.57974027587572,5.53587627227095));
#9576=CARTESIAN_POINT('Ctrl Pts',(0.436086388368659,2.5758691043747,5.55332223624302));
#9577=CARTESIAN_POINT('Ctrl Pts',(0.369435697939357,2.57199793287368,5.56735968916256));
#9578=CARTESIAN_POINT('Ctrl Pts',(0.302187103605554,2.56812676137267,5.5778863627021));
#9579=CARTESIAN_POINT('Ctrl Pts',(0.234977238724878,2.56425781933617,5.58840697377575));
#9580=CARTESIAN_POINT('Ctrl Pts',(0.167170647737113,2.56038887729967,5.5954207372019));
#9581=CARTESIAN_POINT('Ctrl Pts',(0.0991674998867616,2.55651993526318,5.59887641976746));
#9582=CARTESIAN_POINT('Ctrl Pts',(0.0311791136326737,2.55265183306663,5.60233135220024));
#9583=CARTESIAN_POINT('Ctrl Pts',(-0.0370052435432233,2.54878373087009,
5.60222971205842));
#9584=CARTESIAN_POINT('Ctrl Pts',(-0.10498201457924,2.54491562867354,5.59857226044298));
#9585=CARTESIAN_POINT('Ctrl Pts',(-0.173013569664411,2.54104440908413,5.59491186120284));
#9586=CARTESIAN_POINT('Ctrl Pts',(-0.240836701824025,2.53717318949472,5.58768995036119));
#9587=CARTESIAN_POINT('Ctrl Pts',(-0.308050758921072,2.53330196990531,5.5769593751808));
#9588=CARTESIAN_POINT('Ctrl Pts',(-0.37529051978522,2.52942926989751,5.56622469645098));
#9589=CARTESIAN_POINT('Ctrl Pts',(-0.441920249618324,2.5255565698897,5.55197878458949));
#9590=CARTESIAN_POINT('Ctrl Pts',(-0.507550177318502,2.5216838698819,5.5343255262465));
#9591=CARTESIAN_POINT('Ctrl Pts',(-0.573294272066751,2.51780443308885,5.51664155904149));
#9592=CARTESIAN_POINT('Ctrl Pts',(-0.638034611784078,2.51392499629581,5.49553856038446));
#9593=CARTESIAN_POINT('Ctrl Pts',(-0.701398004787334,2.51004555950277,5.47116990371455));
#9594=CARTESIAN_POINT('Ctrl Pts',(-0.755866066488291,2.50671074120165,5.45022226451539));
#9595=CARTESIAN_POINT('Ctrl Pts',(-0.8093167998603,2.50337592290053,5.42686240189678));
#9596=CARTESIAN_POINT('Ctrl Pts',(-0.861527974718931,2.50004110459941,5.40121474093917));
#9597=CARTESIAN_POINT('',(0.861525859670532,2.5,5.40121577991141));
#9598=CARTESIAN_POINT('Origin',(-5.55111512312578E-16,2.5,3.64739446828387));
#9599=CARTESIAN_POINT('Ctrl Pts',(0.861525859670531,2.5,5.40121577991141));
#9600=CARTESIAN_POINT('Ctrl Pts',(0.924640824599862,2.50400926879465,5.37021195183707));
#9601=CARTESIAN_POINT('Ctrl Pts',(0.98612780568499,2.5080185375893,5.33577388677797));
#9602=CARTESIAN_POINT('Ctrl Pts',(1.04560615745964,2.51202780638395,5.2980984888407));
#9603=CARTESIAN_POINT('Ctrl Pts',(1.10680124187082,2.51615279530842,5.25933566021137));
#9604=CARTESIAN_POINT('Ctrl Pts',(1.16586949339281,2.52027778423288,5.21714593155204));
#9605=CARTESIAN_POINT('Ctrl Pts',(1.22242491847299,2.52440277315734,5.1717937987404));
#9606=CARTESIAN_POINT('Ctrl Pts',(1.27735367946414,2.52840911791387,5.12774609756729));
#9607=CARTESIAN_POINT('Ctrl Pts',(1.3299118591709,2.53241546267039,5.08071578688038));
#9608=CARTESIAN_POINT('Ctrl Pts',(1.37977792362144,2.53642180742692,5.03098721236969));
#9609=CARTESIAN_POINT('Ctrl Pts',(1.42964495246872,2.54042822966511,4.98125767612126));
#9610=CARTESIAN_POINT('Ctrl Pts',(1.47681943741636,2.5444346519033,4.92883009647145));
#9611=CARTESIAN_POINT('Ctrl Pts',(1.52101670404325,2.5484410741415,4.87402570301639));
#9612=CARTESIAN_POINT('Ctrl Pts',(1.56522679197008,2.55244865861313,4.81920541121239));
#9613=CARTESIAN_POINT('Ctrl Pts',(1.60645765682533,2.55645624308476,4.76200729257364));
#9614=CARTESIAN_POINT('Ctrl Pts',(1.6444657981191,2.5604638275564,4.7027845567424));
#9615=CARTESIAN_POINT('Ctrl Pts',(1.68442820694257,2.56467747030762,4.64051676093939));
#9616=CARTESIAN_POINT('Ctrl Pts',(1.72082726588756,2.56889111305884,4.57601102517069));
#9617=CARTESIAN_POINT('Ctrl Pts',(1.75343383018526,2.57310475581007,4.5097086819913));
#9618=CARTESIAN_POINT('Ctrl Pts',(1.78451254633702,2.57712095959758,4.44651307251045));
#9619=CARTESIAN_POINT('Ctrl Pts',(1.81214608686432,2.5811371633851,4.3816859091714));
#9620=CARTESIAN_POINT('Ctrl Pts',(1.83618572392648,2.58515336717261,4.3156294473508));
#9621=CARTESIAN_POINT('Ctrl Pts',(1.86024744854126,2.58917326103715,4.24951229303422));
#9622=CARTESIAN_POINT('Ctrl Pts',(1.88070855939279,2.59319315490169,4.18216402918135));
#9623=CARTESIAN_POINT('Ctrl Pts',(1.89747052412524,2.59721304876623,4.11400095138918));
#9624=CARTESIAN_POINT('Ctrl Pts',(1.91426290407195,2.6012402368791,4.04571418913342));
#9625=CARTESIAN_POINT('Ctrl Pts',(1.92734265511498,2.60526742499197,3.97661011190263));
#9626=CARTESIAN_POINT('Ctrl Pts',(1.93666260885463,2.60929461310484,3.90711343074976));
#9627=CARTESIAN_POINT('Ctrl Pts',(1.93799942281075,2.60987225559359,3.89714512662895));
#9628=CARTESIAN_POINT('Ctrl Pts',(1.93925897094148,2.61044989808234,3.88716874862352));
#9629=CARTESIAN_POINT('Ctrl Pts',(1.94044120187923,2.61102754057108,3.87718555176946));
#9630=CARTESIAN_POINT('Ctrl Pts',(1.94938012008528,2.61539512967265,3.80170200852605));
#9631=CARTESIAN_POINT('Ctrl Pts',(1.95392024650498,2.61976271877421,3.72564652348674));
#9632=CARTESIAN_POINT('Ctrl Pts',(1.95399895846957,2.62413030787577,3.64941196669006));
#9633=CARTESIAN_POINT('Origin',(0.,0.,3.64739446828387));
#9634=CARTESIAN_POINT('',(1.95399979033444,3.42586969208078,3.64829966051471));
#9635=CARTESIAN_POINT('',(1.95399983251307,3.3241303078362,3.64820350405597));
#9636=CARTESIAN_POINT('',(1.954,4.33875158023511E-16,3.64739446828387));
#9637=CARTESIAN_POINT('Ctrl Pts',(1.95399979033444,3.42586969208078,3.64829966051471));
#9638=CARTESIAN_POINT('Ctrl Pts',(1.95396480342058,3.42158392528816,3.72382441647484));
#9639=CARTESIAN_POINT('Ctrl Pts',(1.94954693631289,3.41729815849555,3.79920428739692));
#9640=CARTESIAN_POINT('Ctrl Pts',(1.94082130003993,3.41301239170294,3.87395280803618));
#9641=CARTESIAN_POINT('Ctrl Pts',(1.93206695591947,3.40871252448995,3.94894725562724));
#9642=CARTESIAN_POINT('Ctrl Pts',(1.91897658649658,3.40441265727697,4.0233058867645));
#9643=CARTESIAN_POINT('Ctrl Pts',(1.90167612158761,3.40011279006398,4.09655360331678));
#9644=CARTESIAN_POINT('Ctrl Pts',(1.88429615383603,3.39579316317008,4.17013792363729));
#9645=CARTESIAN_POINT('Ctrl Pts',(1.86266745413099,3.39147353627618,4.24260079990362));
#9646=CARTESIAN_POINT('Ctrl Pts',(1.83696603276115,3.38715390938228,4.31348139540507));
#9647=CARTESIAN_POINT('Ctrl Pts',(1.8231769297256,3.38483638073443,4.35150963596523));
#9648=CARTESIAN_POINT('Ctrl Pts',(1.80821632797973,3.38251885208658,4.38908280851349));
#9649=CARTESIAN_POINT('Ctrl Pts',(1.79211686507899,3.38020132343873,4.4261326411632));
#9650=CARTESIAN_POINT('Ctrl Pts',(1.76489513180678,3.37628273639694,4.48877825042292));
#9651=CARTESIAN_POINT('Ctrl Pts',(1.73433083910883,3.37236414935515,4.55011866002973));
#9652=CARTESIAN_POINT('Ctrl Pts',(1.70057119742648,3.36844556231337,4.60977360484257));
#9653=CARTESIAN_POINT('Ctrl Pts',(1.66686231904713,3.36453286752669,4.66933884840599));
#9654=CARTESIAN_POINT('Ctrl Pts',(1.62996786774875,3.36062017274002,4.72722323253675));
#9655=CARTESIAN_POINT('Ctrl Pts',(1.59008264753988,3.35670747795335,4.7830674731548));
#9656=CARTESIAN_POINT('Ctrl Pts',(1.55024424507099,3.35279937593377,4.83884616314725));
#9657=CARTESIAN_POINT('Ctrl Pts',(1.50742233031503,3.3488912739142,4.89258906739672));
#9658=CARTESIAN_POINT('Ctrl Pts',(1.46185610518547,3.34498317189463,4.94396406831773));
#9659=CARTESIAN_POINT('Ctrl Pts',(1.4163183760412,3.34107751390498,4.99530694058937));
#9660=CARTESIAN_POINT('Ctrl Pts',(1.36804006657401,3.33717185591533,5.044284479995));
#9661=CARTESIAN_POINT('Ctrl Pts',(1.31730095029969,3.33326619792568,5.09059722823811));
#9662=CARTESIAN_POINT('Ctrl Pts',(1.26657617424462,3.3293616437785,5.13689688727091));
#9663=CARTESIAN_POINT('Ctrl Pts',(1.21339233509797,3.32545708963133,5.18053291892599));
#9664=CARTESIAN_POINT('Ctrl Pts',(1.15806508986361,3.32155253548416,5.22124365027025));
#9665=CARTESIAN_POINT('Ctrl Pts',(1.10273451884996,3.3176477466301,5.26195682877967));
#9666=CARTESIAN_POINT('Ctrl Pts',(1.04526068354755,3.31374295777605,5.29974406850755));
#9667=CARTESIAN_POINT('Ctrl Pts',(0.985989779129751,3.30983816892199,5.33438591919631));
#9668=CARTESIAN_POINT('Ctrl Pts',(0.926655846197206,3.30592922772634,5.36906460793265));
#9669=CARTESIAN_POINT('Ctrl Pts',(0.865521455784724,3.30202028653069,5.40059098391652));
#9670=CARTESIAN_POINT('Ctrl Pts',(0.802958182434712,3.29811134533503,5.42879115551026));
#9671=CARTESIAN_POINT('Ctrl Pts',(0.740357429382511,3.29420006241485,5.45700822094564));
#9672=CARTESIAN_POINT('Ctrl Pts',(0.676326548180425,3.29028877949467,5.4818949381124));
#9673=CARTESIAN_POINT('Ctrl Pts',(0.61125527900254,3.28637749657449,5.50332630536505));
#9674=CARTESIAN_POINT('Ctrl Pts',(0.546072049952875,3.28245948400634,5.52479454685053));
#9675=CARTESIAN_POINT('Ctrl Pts',(0.479845334551204,3.27854147143819,5.54279544405977));
#9676=CARTESIAN_POINT('Ctrl Pts',(0.412977281260173,3.27462345887005,5.55725461111186));
#9677=CARTESIAN_POINT('Ctrl Pts',(0.381974383829435,3.27280690020258,5.56395850110099));
#9678=CARTESIAN_POINT('Ctrl Pts',(0.350833722259817,3.27099034153511,5.56990177297914));
#9679=CARTESIAN_POINT('Ctrl Pts',(0.319595685371466,3.26917378286764,5.57508080114302));
#9680=CARTESIAN_POINT('Ctrl Pts',(0.252208833978639,3.2652550933095,5.58625302692934));
#9681=CARTESIAN_POINT('Ctrl Pts',(0.184102294733262,3.26133640375136,5.59390957506826));
#9682=CARTESIAN_POINT('Ctrl Pts',(0.115675333849662,3.25741771419322,5.59796751668241));
#9683=CARTESIAN_POINT('Ctrl Pts',(0.047351216489819,3.25350491429959,5.60201935934068));
#9684=CARTESIAN_POINT('Ctrl Pts',(-0.0212918798043706,3.24959211440596,
5.60248330086764));
#9685=CARTESIAN_POINT('Ctrl Pts',(-0.0898464570696235,3.24567931451232,
5.59932776994969));
#9686=CARTESIAN_POINT('Ctrl Pts',(-0.158320623613156,3.24177110411623,5.59617594029471));
#9687=CARTESIAN_POINT('Ctrl Pts',(-0.226705988457172,3.23786289372013,5.58941309229315));
#9688=CARTESIAN_POINT('Ctrl Pts',(-0.294593750439108,3.23395468332403,5.57905968829541));
#9689=CARTESIAN_POINT('Ctrl Pts',(-0.362439092315836,3.23004891499837,5.56871275368882));
#9690=CARTESIAN_POINT('Ctrl Pts',(-0.429786963122477,3.2261431466727,5.55477978767468));
#9691=CARTESIAN_POINT('Ctrl Pts',(-0.496233948595555,3.22223737834703,5.53733305677326));
#9692=CARTESIAN_POINT('Ctrl Pts',(-0.562662185118731,3.21833271208874,5.51989124871193));
#9693=CARTESIAN_POINT('Ctrl Pts',(-0.628189565578085,3.21442804583045,5.49893776883437));
#9694=CARTESIAN_POINT('Ctrl Pts',(-0.692424912524393,3.21052337957215,5.4745955356313));
#9695=CARTESIAN_POINT('Ctrl Pts',(-0.756664146815767,3.20661847701428,5.45025182930378));
#9696=CARTESIAN_POINT('Ctrl Pts',(-0.819610733474382,3.20271357445642,5.42251913914845));
#9697=CARTESIAN_POINT('Ctrl Pts',(-0.880892360436774,3.19880867189855,5.39156895764098));
#9698=CARTESIAN_POINT('Ctrl Pts',(-0.942239177187545,3.1948996154077,5.36058585214172));
#9699=CARTESIAN_POINT('Ctrl Pts',(-1.00191705989154,3.19099055891685,5.32637864684416));
#9700=CARTESIAN_POINT('Ctrl Pts',(-1.05957816435751,3.187081502426,5.28916488878023));
#9701=CARTESIAN_POINT('Ctrl Pts',(-1.11727382662157,3.18317010313603,5.25192882754417));
#9702=CARTESIAN_POINT('Ctrl Pts',(-1.17294990653501,3.17925870384606,5.21168291548391));
#9703=CARTESIAN_POINT('Ctrl Pts',(-1.22628974279194,3.17534730455608,5.16868650688898));
#9704=CARTESIAN_POINT('Ctrl Pts',(-1.2797213569444,3.17142917521179,5.12561611756646));
#9705=CARTESIAN_POINT('Ctrl Pts',(-1.33080833887659,3.1675110458675,5.07978611454225));
#9706=CARTESIAN_POINT('Ctrl Pts',(-1.37926978606367,3.16359291652321,5.03149376286208));
#9707=CARTESIAN_POINT('Ctrl Pts',(-1.40172554595874,3.16177735844766,5.00911635737701));
#9708=CARTESIAN_POINT('Ctrl Pts',(-1.42361812047924,3.15996180037211,4.9862107284678));
#9709=CARTESIAN_POINT('Ctrl Pts',(-1.44492256927573,3.15814624229656,4.96280876378078));
#9710=CARTESIAN_POINT('Ctrl Pts',(-1.49089463538647,3.15422851803745,4.91231054728196));
#9711=CARTESIAN_POINT('Ctrl Pts',(-1.53430736323659,3.15031079377834,4.85929933663351));
#9712=CARTESIAN_POINT('Ctrl Pts',(-1.57487428716369,3.14639306951922,4.8040651126899));
#9713=CARTESIAN_POINT('Ctrl Pts',(-1.61538019121469,3.14248123821491,4.74891397085298));
#9714=CARTESIAN_POINT('Ctrl Pts',(-1.65304849789035,3.13856940691059,4.69154684530576));
#9715=CARTESIAN_POINT('Ctrl Pts',(-1.68763137962661,3.13465757560628,4.63228853695298));
#9716=CARTESIAN_POINT('Ctrl Pts',(-1.72217368614137,3.13075033395481,4.57309975487638));
#9717=CARTESIAN_POINT('Ctrl Pts',(-1.7536375103363,3.12684309230334,4.51202461959079));
#9718=CARTESIAN_POINT('Ctrl Pts',(-1.78181799743233,3.12293585065187,4.44941730089292));
#9719=CARTESIAN_POINT('Ctrl Pts',(-1.80998087476159,3.11903105060526,4.38684910502059));
#9720=CARTESIAN_POINT('Ctrl Pts',(-1.83486428347826,3.11512625055865,4.3227510726286));
#9721=CARTESIAN_POINT('Ctrl Pts',(-1.85630978619131,3.11122145051204,4.25750099807222));
#9722=CARTESIAN_POINT('Ctrl Pts',(-1.87774924678108,3.10731775061605,4.19226930727673));
#9723=CARTESIAN_POINT('Ctrl Pts',(-1.89575257068176,3.10341405072007,4.12588668583091));
#9724=CARTESIAN_POINT('Ctrl Pts',(-1.91021049363009,3.09951035082408,4.05874817256463));
#9725=CARTESIAN_POINT('Ctrl Pts',(-1.92466930422709,3.09560641125923,3.99160553730842));
#9726=CARTESIAN_POINT('Ctrl Pts',(-1.93558218067504,3.09170247169437,3.92370739958933));
#9727=CARTESIAN_POINT('Ctrl Pts',(-1.94289088911684,3.08779853212952,3.85545934515347));
#9728=CARTESIAN_POINT('Ctrl Pts',(-1.95020739604261,3.08389042701197,3.78713846918391));
#9729=CARTESIAN_POINT('Ctrl Pts',(-1.95391200778782,3.07998232189443,3.7184674215022));
#9730=CARTESIAN_POINT('Ctrl Pts',(-1.95399844922611,3.07607421677689,3.64985626071562));
#9731=CARTESIAN_POINT('Ctrl Pts',(-1.95408494259971,3.07216376361086,3.58120387730902));
#9732=CARTESIAN_POINT('Ctrl Pts',(-1.95054896473042,3.06825331044483,3.51261194378149));
#9733=CARTESIAN_POINT('Ctrl Pts',(-1.9434362803453,3.0643428572788,3.44448704053018));
#9734=CARTESIAN_POINT('Ctrl Pts',(-1.93631132208703,3.0604256561111,3.37624457879103));
#9735=CARTESIAN_POINT('Ctrl Pts',(-1.92559741588042,3.0565084549434,3.30847124143881));
#9736=CARTESIAN_POINT('Ctrl Pts',(-1.9113915795902,3.0525912537757,3.24156417188934));
#9737=CARTESIAN_POINT('Ctrl Pts',(-1.90477612677183,3.05076706975896,3.21040651578392));
#9738=CARTESIAN_POINT('Ctrl Pts',(-1.8974041141819,3.04894288574222,3.17943651304367));
#9739=CARTESIAN_POINT('Ctrl Pts',(-1.88928897332868,3.04711870172548,3.1486929791557));
#9740=CARTESIAN_POINT('Ctrl Pts',(-1.87185313432429,3.04319933921465,3.08263875816404));
#9741=CARTESIAN_POINT('Ctrl Pts',(-1.85091457533122,3.03927997670381,3.01736962809995));
#9742=CARTESIAN_POINT('Ctrl Pts',(-1.82656137564055,3.03536061419298,2.95328385676861));
#9743=CARTESIAN_POINT('Ctrl Pts',(-1.8022448089673,3.03144714733762,2.88929448571347));
#9744=CARTESIAN_POINT('Ctrl Pts',(-1.77452396902811,3.02753368048226,2.82648539634389));
#9745=CARTESIAN_POINT('Ctrl Pts',(-1.74353715277275,3.0236202136269,2.76524130873553));
#9746=CARTESIAN_POINT('Ctrl Pts',(-1.71258677063199,3.01971134820263,2.70406923156182));
#9747=CARTESIAN_POINT('Ctrl Pts',(-1.67837825975926,3.01580248277837,2.64445893807871));
#9748=CARTESIAN_POINT('Ctrl Pts',(-1.64109791096865,3.0118936173541,2.58677500466163));
#9749=CARTESIAN_POINT('Ctrl Pts',(-1.60384092725405,3.00798720177113,2.52912722405782));
#9750=CARTESIAN_POINT('Ctrl Pts',(-1.56351619100123,3.00408078618815,2.47340382040299));
#9751=CARTESIAN_POINT('Ctrl Pts',(-1.5203550367178,3.00017437060518,2.41994322186843));
#9752=CARTESIAN_POINT('Ctrl Pts',(-1.47720615483415,2.99626906576854,2.3664978242674));
#9753=CARTESIAN_POINT('Ctrl Pts',(-1.43122276464043,2.99236376093189,2.315314336752));
#9754=CARTESIAN_POINT('Ctrl Pts',(-1.38267738706858,2.98845845609525,2.26669926539179));
#9755=CARTESIAN_POINT('Ctrl Pts',(-1.33412919142794,2.98455292455488,2.21808137191705));
#9756=CARTESIAN_POINT('Ctrl Pts',(-1.28301906227187,2.98064739301452,2.17203253660852));
#9757=CARTESIAN_POINT('Ctrl Pts',(-1.22965609646498,2.97674186147416,2.12882215047135));
#9758=CARTESIAN_POINT('Ctrl Pts',(-1.17623662792966,2.97283219460914,2.08556601154146));
#9759=CARTESIAN_POINT('Ctrl Pts',(-1.12055994499601,2.96892252774412,2.04515462963031));
#9760=CARTESIAN_POINT('Ctrl Pts',(-1.06296712617754,2.96501286087911,2.00781620279428));
#9761=CARTESIAN_POINT('Ctrl Pts',(-1.00533993935781,2.96110086095524,1.97045549458486));
#9762=CARTESIAN_POINT('Ctrl Pts',(-0.945794766954578,2.95718886103137,1.93617163639363));
#9763=CARTESIAN_POINT('Ctrl Pts',(-0.884698047574256,2.9532768611075,1.90514725143481));
#9764=CARTESIAN_POINT('Ctrl Pts',(-0.823496549589744,2.94935815224908,1.87406966080824));
#9765=CARTESIAN_POINT('Ctrl Pts',(-0.760738643192554,2.94543944339066,1.84626289884297));
#9766=CARTESIAN_POINT('Ctrl Pts',(-0.696810697122993,2.94152073453224,1.82186143588622));
#9767=CARTESIAN_POINT('Ctrl Pts',(-0.667285540868792,2.93971087673963,1.81059160710359));
#9768=CARTESIAN_POINT('Ctrl Pts',(-0.637511017076782,2.93790101894702,1.80004744746111));
#9769=CARTESIAN_POINT('Ctrl Pts',(-0.607526056778454,2.93609116115441,1.79023855389886));
#9770=CARTESIAN_POINT('Ctrl Pts',(-0.54258923585884,2.93217164916575,1.76899595900015));
#9771=CARTESIAN_POINT('Ctrl Pts',(-0.476409137968989,2.9282521371771,1.75112150272362));
#9772=CARTESIAN_POINT('Ctrl Pts',(-0.409368097857574,2.92433262518844,1.73675746444026));
#9773=CARTESIAN_POINT('Ctrl Pts',(-0.342427594251089,2.92041899100293,1.72241496684607));
#9774=CARTESIAN_POINT('Ctrl Pts',(-0.274629187590647,2.91650535681741,1.71157254128802));
#9775=CARTESIAN_POINT('Ctrl Pts',(-0.206371096701374,2.9125917226319,1.70432293834827));
#9776=CARTESIAN_POINT('Ctrl Pts',(-0.138192820382465,2.9086826646809,1.6970818124101));
#9777=CARTESIAN_POINT('Ctrl Pts',(-0.0695564137906668,2.90477360672989,
1.69342521710811));
#9778=CARTESIAN_POINT('Ctrl Pts',(-0.000869236631244366,2.90086454877889,
1.69339466162378));
#9779=CARTESIAN_POINT('Ctrl Pts',(0.0677751655907483,2.8969579251936,1.69336412516787));
#9780=CARTESIAN_POINT('Ctrl Pts',(0.136469785285936,2.89305130160832,1.69695514921585));
#9781=CARTESIAN_POINT('Ctrl Pts',(0.204804767933492,2.88914467802303,1.70415721899296));
#9782=CARTESIAN_POINT('Ctrl Pts',(0.273120583999533,2.8852391501667,1.71135726873506));
#9783=CARTESIAN_POINT('Ctrl Pts',(0.341076474743505,2.88133362231037,1.72216630200453));
#9784=CARTESIAN_POINT('Ctrl Pts',(0.408267032846791,2.87742809445405,1.73652188490986));
#9785=CARTESIAN_POINT('Ctrl Pts',(0.475461741904409,2.87352232531876,1.75087835468636));
#9786=CARTESIAN_POINT('Ctrl Pts',(0.541890544378558,2.86961655618348,1.76878170389678));
#9787=CARTESIAN_POINT('Ctrl Pts',(0.607159343224885,2.86571078704819,1.7901186320294));
#9788=CARTESIAN_POINT('Ctrl Pts',(0.672497582257442,2.86180086252257,1.81147826075234));
#9789=CARTESIAN_POINT('Ctrl Pts',(0.736672886707037,2.85789093799695,1.8362786056171));
#9790=CARTESIAN_POINT('Ctrl Pts',(0.799308385936824,2.85398101347132,1.86435714277129));
#9791=CARTESIAN_POINT('Ctrl Pts',(0.861981449243666,2.85006874406607,1.89245251932719));
#9792=CARTESIAN_POINT('Ctrl Pts',(0.923112432150434,2.84615647466082,1.9238297765482));
#9793=CARTESIAN_POINT('Ctrl Pts',(0.982348966787811,2.84224420525557,1.95828034915192));
#9794=CARTESIAN_POINT('Ctrl Pts',(1.04168731167449,2.83832521180534,1.99279013219741));
#9795=CARTESIAN_POINT('Ctrl Pts',(1.09912429892471,2.8344062183551,2.03038350381037));
#9796=CARTESIAN_POINT('Ctrl Pts',(1.15433717467102,2.83048722490487,2.07080901637442));
#9797=CARTESIAN_POINT('Ctrl Pts',(1.17980738747821,2.82867935679769,2.08945768109127));
#9798=CARTESIAN_POINT('Ctrl Pts',(1.20480477019518,2.82687148869051,2.10870848800464));
#9799=CARTESIAN_POINT('Ctrl Pts',(1.229300222574,2.82506362058333,2.12853405245248));
#9800=CARTESIAN_POINT('Ctrl Pts',(1.28164323011488,2.82120048498969,2.17089822900847));
#9801=CARTESIAN_POINT('Ctrl Pts',(1.33191182350579,2.81733734939605,2.21606720796799));
#9802=CARTESIAN_POINT('Ctrl Pts',(1.37978360123067,2.81347421380241,2.26380738617631));
#9803=CARTESIAN_POINT('Ctrl Pts',(1.42757306397375,2.80961772082684,2.31146547568672));
#9804=CARTESIAN_POINT('Ctrl Pts',(1.47297353608627,2.80576122785128,2.3616856339295));
#9805=CARTESIAN_POINT('Ctrl Pts',(1.51569521873076,2.80190473487571,2.4141937531054));
#9806=CARTESIAN_POINT('Ctrl Pts',(1.55837600201868,2.79805193389146,2.46665160393613));
#9807=CARTESIAN_POINT('Ctrl Pts',(1.59838275892303,2.79419913290722,2.52139268472609));
#9808=CARTESIAN_POINT('Ctrl Pts',(1.63546324370269,2.79034633192297,2.57810686501827));
#9809=CARTESIAN_POINT('Ctrl Pts',(1.67252178951752,2.78649581047918,2.63478748991296));
#9810=CARTESIAN_POINT('Ctrl Pts',(1.7066572187371,2.78264528903539,2.69343847657475));
#9811=CARTESIAN_POINT('Ctrl Pts',(1.73765945873494,2.7787947675916,2.7537191326787));
#9812=CARTESIAN_POINT('Ctrl Pts',(1.76865469033083,2.7749451166011,2.81398616166839));
#9813=CARTESIAN_POINT('Ctrl Pts',(1.79651790755941,2.7710954656106,2.87588167785104));
#9814=CARTESIAN_POINT('Ctrl Pts',(1.82108501638625,2.76724581462011,2.93904048679333));
#9815=CARTESIAN_POINT('Ctrl Pts',(1.84567006914102,2.76339335182703,3.00224542721672));
#9816=CARTESIAN_POINT('Ctrl Pts',(1.86695402027122,2.75954088903396,3.06671503024622));
#9817=CARTESIAN_POINT('Ctrl Pts',(1.88482147805864,2.75568842624088,3.13206545119979));
#9818=CARTESIAN_POINT('Ctrl Pts',(1.90269589233817,2.7518344635351,3.19744131559885));
#9819=CARTESIAN_POINT('Ctrl Pts',(1.91715105613523,2.74798050082931,3.26369818508322));
#9820=CARTESIAN_POINT('Ctrl Pts',(1.9281225718929,2.74412653812353,3.33044124183381));
#9821=CARTESIAN_POINT('Ctrl Pts',(1.93911105040701,2.74026661691281,3.39728748817467));
#9822=CARTESIAN_POINT('Ctrl Pts',(1.94660507416332,2.7364066957021,3.46462091816702));
#9823=CARTESIAN_POINT('Ctrl Pts',(1.95059216252502,2.73254677449139,3.53204189789213));
#9824=CARTESIAN_POINT('Ctrl Pts',(1.95289118330323,2.73032108038565,3.5709179445743));
#9825=CARTESIAN_POINT('Ctrl Pts',(1.95402516604589,2.72809538627992,3.60982308596676));
#9826=CARTESIAN_POINT('Ctrl Pts',(1.95399957629683,2.72586969217418,3.64868125956088));
#9827=CARTESIAN_POINT('Ctrl Pts',(1.95399895847038,2.6241303079204,3.64941196591101));
#9828=CARTESIAN_POINT('Ctrl Pts',(1.9540679267512,2.62795723854692,3.58261439099596));
#9829=CARTESIAN_POINT('Ctrl Pts',(1.95070752961312,2.63178416917345,3.51565940348065));
#9830=CARTESIAN_POINT('Ctrl Pts',(1.94389595297049,2.63561109979997,3.4489391231179));
#9831=CARTESIAN_POINT('Ctrl Pts',(1.93709490011831,2.6394321178723,3.38232192465326));
#9832=CARTESIAN_POINT('Ctrl Pts',(1.92685329612979,2.64325313594464,3.31593922231414));
#9833=CARTESIAN_POINT('Ctrl Pts',(1.91320133873364,2.64707415401697,3.25018339408302));
#9834=CARTESIAN_POINT('Ctrl Pts',(1.89956094128294,2.65089193660013,3.18448324532446));
#9835=CARTESIAN_POINT('Ctrl Pts',(1.88251601273264,2.65470971918328,3.11940942193869));
#9836=CARTESIAN_POINT('Ctrl Pts',(1.86214838250636,2.65852750176643,3.05534767830107));
#9837=CARTESIAN_POINT('Ctrl Pts',(1.84179033870873,2.66234348743458,2.99131608659214));
#9838=CARTESIAN_POINT('Ctrl Pts',(1.81811284795109,2.66615947310273,2.92829612128937));
#9839=CARTESIAN_POINT('Ctrl Pts',(1.79124798235703,2.66997545877088,2.86665977217906));
#9840=CARTESIAN_POINT('Ctrl Pts',(1.76438566184423,2.6737910829262,2.80502926227596));
#9841=CARTESIAN_POINT('Ctrl Pts',(1.73433677346291,2.67760670708152,2.74478258014629));
#9842=CARTESIAN_POINT('Ctrl Pts',(1.70128123276098,2.68142233123684,2.68627108023461));
#9843=CARTESIAN_POINT('Ctrl Pts',(1.6681942594413,2.68524158368119,2.62770394155341));
#9844=CARTESIAN_POINT('Ctrl Pts',(1.63209518231189,2.68906083612553,2.57087572753031));
#9845=CARTESIAN_POINT('Ctrl Pts',(1.59320886633498,2.69288008856988,2.51611134358359));
#9846=CARTESIAN_POINT('Ctrl Pts',(1.55430239227122,2.69670132085779,2.46131857059618));
#9847=CARTESIAN_POINT('Ctrl Pts',(1.51260612827238,2.7005225531457,2.40859215759322));
#9848=CARTESIAN_POINT('Ctrl Pts',(1.4683851679231,2.7043437854336,2.35822380517388));
#9849=CARTESIAN_POINT('Ctrl Pts',(1.42408702466098,2.70817168726999,2.30776754023242));
#9850=CARTESIAN_POINT('Ctrl Pts',(1.37725575526897,2.71199958910637,2.25967791329002));
#9851=CARTESIAN_POINT('Ctrl Pts',(1.32819236692964,2.71582749094275,2.21420884303157));
#9852=CARTESIAN_POINT('Ctrl Pts',(1.30158539097332,2.71790335434255,2.18955105847833));
#9853=CARTESIAN_POINT('Ctrl Pts',(1.27432254066745,2.71997921774235,2.16566323416876));
#9854=CARTESIAN_POINT('Ctrl Pts',(1.24645540150732,2.72205508114215,2.14258054887282));
#9855=CARTESIAN_POINT('Ctrl Pts',(1.1937797887706,2.72597896352972,2.09894870763555));
#9856=CARTESIAN_POINT('Ctrl Pts',(1.13870787370658,2.72990284591728,2.05800107044378));
#9857=CARTESIAN_POINT('Ctrl Pts',(1.08154398218446,2.73382672830484,2.02001048943912));
#9858=CARTESIAN_POINT('Ctrl Pts',(1.02446590816368,2.73774471994961,1.98207694193321));
#9859=CARTESIAN_POINT('Ctrl Pts',(0.965302496310353,2.74166271159438,1.94709190850394));
#9860=CARTESIAN_POINT('Ctrl Pts',(0.904390978508841,2.74558070323915,1.91528795943639));
#9861=CARTESIAN_POINT('Ctrl Pts',(0.843551259159137,2.74949407661557,1.88352149875176));
#9862=CARTESIAN_POINT('Ctrl Pts',(0.780967959127656,2.753407449992,1.85492890052287));
#9863=CARTESIAN_POINT('Ctrl Pts',(0.717005575465429,2.75732082336843,1.82969839777277));
#9864=CARTESIAN_POINT('Ctrl Pts',(0.653083455404389,2.76123173332033,1.80448377734041));
#9865=CARTESIAN_POINT('Ctrl Pts',(0.587784428964954,2.76514264327222,1.78262723308196));
#9866=CARTESIAN_POINT('Ctrl Pts',(0.521494381419933,2.76905355322412,1.76426950956567));
#9867=CARTESIAN_POINT('Ctrl Pts',(0.455223518419318,2.7729633313466,1.74591709883123));
#9868=CARTESIAN_POINT('Ctrl Pts',(0.387962675909299,2.77687310946909,1.73106162924773));
#9869=CARTESIAN_POINT('Ctrl Pts',(0.32011264658097,2.78078288759157,1.71979391487584));
#9870=CARTESIAN_POINT('Ctrl Pts',(0.252259179413601,2.78469286381549,1.70852562958912));
#9871=CARTESIAN_POINT('Ctrl Pts',(0.183816950128407,2.7886028400394,1.70084553823989));
#9872=CARTESIAN_POINT('Ctrl Pts',(0.115194905210794,2.79251281626332,1.69679298827483));
#9873=CARTESIAN_POINT('Ctrl Pts',(0.0465016013761671,2.79642685270828,1.69273623003643));
#9874=CARTESIAN_POINT('Ctrl Pts',(-0.0223714004930565,2.80034088915324,
1.69231455996694));
#9875=CARTESIAN_POINT('Ctrl Pts',(-0.091013102577,2.80425492559821,1.69551521608631));
#9876=CARTESIAN_POINT('Ctrl Pts',(-0.15969507348771,2.80817125822248,1.69871774987863));
#9877=CARTESIAN_POINT('Ctrl Pts',(-0.228144986629474,2.81208759084674,1.7055467912717));
#9878=CARTESIAN_POINT('Ctrl Pts',(-0.295957695995734,2.81600392347101,1.71593775321597));
#9879=CARTESIAN_POINT('Ctrl Pts',(-0.36388478966922,2.81992686203977,1.72634624230219));
#9880=CARTESIAN_POINT('Ctrl Pts',(-0.431172054604574,2.82384980060853,1.74032854398264));
#9881=CARTESIAN_POINT('Ctrl Pts',(-0.497426112609263,2.82777273917729,1.7577693037355));
#9882=CARTESIAN_POINT('Ctrl Pts',(-0.527318777624549,2.8295427000226,1.7656382676089));
#9883=CARTESIAN_POINT('Ctrl Pts',(-0.557001347279252,2.83131266086792,1.77421058611087));
#9884=CARTESIAN_POINT('Ctrl Pts',(-0.586438997343526,2.83308262171323,1.78347244674039));
#9885=CARTESIAN_POINT('Ctrl Pts',(-0.651721774515719,2.83700779777912,1.80401212916603));
#9886=CARTESIAN_POINT('Ctrl Pts',(-0.716048236771028,2.840932973845,1.82802469709651));
#9887=CARTESIAN_POINT('Ctrl Pts',(-0.779023915909538,2.84485814991089,1.85540179574278));
#9888=CARTESIAN_POINT('Ctrl Pts',(-0.841907393739568,2.84877757921272,1.88273881218029));
#9889=CARTESIAN_POINT('Ctrl Pts',(-0.903443568159146,2.85269700851455,1.91343038786888));
#9890=CARTESIAN_POINT('Ctrl Pts',(-0.963254062177318,2.85661643781638,1.94731870182554));
#9891=CARTESIAN_POINT('Ctrl Pts',(-1.02299724079491,2.8605314558864,1.98116887522732));
#9892=CARTESIAN_POINT('Ctrl Pts',(-1.08101817229141,2.86444647395642,2.01820840058983));
#9893=CARTESIAN_POINT('Ctrl Pts',(-1.13696100915546,2.86836149202645,2.05823253076454));
#9894=CARTESIAN_POINT('Ctrl Pts',(-1.19287047242155,2.87227417452955,2.09823278390147));
#9895=CARTESIAN_POINT('Ctrl Pts',(-1.24670390311217,2.87618685703266,2.1412138249301));
#9896=CARTESIAN_POINT('Ctrl Pts',(-1.29813382908812,2.88009953953577,2.1869272273719));
#9897=CARTESIAN_POINT('Ctrl Pts',(-1.34955052697988,2.88401121567356,2.23262887205352));
#9898=CARTESIAN_POINT('Ctrl Pts',(-1.39856458168765,2.88792289181135,2.28106115747686));
#9899=CARTESIAN_POINT('Ctrl Pts',(-1.44488245081826,2.89183456794915,2.33193610584231));
#9900=CARTESIAN_POINT('Ctrl Pts',(-1.49120412448933,2.89574656539123,2.38281523306579));
#9901=CARTESIAN_POINT('Ctrl Pts',(-1.53482884503849,2.89965856283332,2.43613705771116));
#9902=CARTESIAN_POINT('Ctrl Pts',(-1.57550194059858,2.9035705602754,2.49157889684951));
#9903=CARTESIAN_POINT('Ctrl Pts',(-1.61621905320479,2.90748679134096,2.5470807359942));
#9904=CARTESIAN_POINT('Ctrl Pts',(-1.65397787595341,2.91140302240651,2.60470677256771));
#9905=CARTESIAN_POINT('Ctrl Pts',(-1.68856643707487,2.91531925347206,2.66410438515262));
#9906=CARTESIAN_POINT('Ctrl Pts',(-1.7231761825105,2.91923788309559,2.72353837674968));
#9907=CARTESIAN_POINT('Ctrl Pts',(-1.75461157795402,2.92315651271912,2.78474566821658));
#9908=CARTESIAN_POINT('Ctrl Pts',(-1.7827073987967,2.92707514234265,2.84735051306922));
#9909=CARTESIAN_POINT('Ctrl Pts',(-1.81085154643919,2.93100051228641,2.91006304268471));
#9910=CARTESIAN_POINT('Ctrl Pts',(-1.83564447823671,2.93492588223016,2.97417746692706));
#9911=CARTESIAN_POINT('Ctrl Pts',(-1.85697002178243,2.93885125217391,3.03930044742743));
#9912=CARTESIAN_POINT('Ctrl Pts',(-1.86649346527689,2.94060422221071,3.06838270850352));
#9913=CARTESIAN_POINT('Ctrl Pts',(-1.87532608795658,2.94235719224752,3.0976659397136));
#9914=CARTESIAN_POINT('Ctrl Pts',(-1.88346084202322,2.94411016228432,3.1271144892676));
#9915=CARTESIAN_POINT('Ctrl Pts',(-1.90162139336457,2.9480236060212,3.19285733677376));
#9916=CARTESIAN_POINT('Ctrl Pts',(-1.91637244034916,2.95193704975809,3.25968545217464));
#9917=CARTESIAN_POINT('Ctrl Pts',(-1.92758891674177,2.95585049349497,3.32721175786013));
#9918=CARTESIAN_POINT('Ctrl Pts',(-1.9387882931745,2.9597579710328,3.39463511703396));
#9919=CARTESIAN_POINT('Ctrl Pts',(-1.94646371236131,2.96366544857062,3.46275407167371));
#9920=CARTESIAN_POINT('Ctrl Pts',(-1.95054027558794,2.96757292610845,3.53116782198737));
#9921=CARTESIAN_POINT('Ctrl Pts',(-1.95461195960121,2.97147572681053,3.59949968830557));
#9922=CARTESIAN_POINT('Ctrl Pts',(-1.95509331260624,2.97537852751261,3.66812515965355));
#9923=CARTESIAN_POINT('Ctrl Pts',(-1.95196102673354,2.97928132821469,3.73663655540286));
#9924=CARTESIAN_POINT('Ctrl Pts',(-1.94883074188931,2.98318163565287,3.8051041833548));
#9925=CARTESIAN_POINT('Ctrl Pts',(-1.94209141961327,2.98708194309104,3.87345738869428));
#9926=CARTESIAN_POINT('Ctrl Pts',(-1.93177183353249,2.99098225052921,3.94128829804304));
#9927=CARTESIAN_POINT('Ctrl Pts',(-1.92145527712735,2.99488141289564,4.00909929325458));
#9928=CARTESIAN_POINT('Ctrl Pts',(-1.90756061749005,2.99878057526207,4.07638780946985));
#9929=CARTESIAN_POINT('Ctrl Pts',(-1.89016829610917,3.0026797376285,4.14275273497955));
#9930=CARTESIAN_POINT('Ctrl Pts',(-1.87277507622576,3.00657910142907,4.20912108895934));
#9931=CARTESIAN_POINT('Ctrl Pts',(-1.8518839634225,3.01047846522964,4.27456528104632));
#9932=CARTESIAN_POINT('Ctrl Pts',(-1.82762570351912,3.01437782903021,4.33869779377583));
#9933=CARTESIAN_POINT('Ctrl Pts',(-1.80334169593423,3.0182813316098,4.40289837666036));
#9934=CARTESIAN_POINT('Ctrl Pts',(-1.77568358378601,3.0221848341894,4.46578403956177));
#9935=CARTESIAN_POINT('Ctrl Pts',(-1.74483050183565,3.02608833676899,4.52698671464804));
#9936=CARTESIAN_POINT('Ctrl Pts',(-1.7139590360075,3.02999416525931,4.58822585748494));
#9937=CARTESIAN_POINT('Ctrl Pts',(-1.67988905689824,3.03389999374963,4.64777958873407));
#9938=CARTESIAN_POINT('Ctrl Pts',(-1.64284456515466,3.03780582223995,4.70530643756194));
#9939=CARTESIAN_POINT('Ctrl Pts',(-1.60573593719212,3.04171841300611,4.76293288431649));
#9940=CARTESIAN_POINT('Ctrl Pts',(-1.56564280702322,3.04563100377227,4.81852504529715));
#9941=CARTESIAN_POINT('Ctrl Pts',(-1.52283064471853,3.04954359453842,4.87177301575445));
#9942=CARTESIAN_POINT('Ctrl Pts',(-1.50242678382174,3.05140829731074,4.89715048149687));
#9943=CARTESIAN_POINT('Ctrl Pts',(-1.48140588582237,3.05327300008307,4.92199601484893));
#9944=CARTESIAN_POINT('Ctrl Pts',(-1.45979955695045,3.05513770285539,4.94627908730408));
#9945=CARTESIAN_POINT('Ctrl Pts',(-1.41438376966936,3.05905724628881,4.99732130089307));
#9946=CARTESIAN_POINT('Ctrl Pts',(-1.36619821726608,3.06297678972223,5.04607926715034));
#9947=CARTESIAN_POINT('Ctrl Pts',(-1.31550159430479,3.06689633315565,5.09223755851255));
#9948=CARTESIAN_POINT('Ctrl Pts',(-1.26488111481419,3.07080998965572,5.13832652272237));
#9949=CARTESIAN_POINT('Ctrl Pts',(-1.21175741053956,3.07472364615579,5.18182323319362));
#9950=CARTESIAN_POINT('Ctrl Pts',(-1.15642783819742,3.07863730265586,5.22244705630817));
#9951=CARTESIAN_POINT('Ctrl Pts',(-1.10116315425486,3.08254636936974,5.2630232373616));
#9952=CARTESIAN_POINT('Ctrl Pts',(-1.04369813440811,3.08645543608362,5.30073293304388));
#9953=CARTESIAN_POINT('Ctrl Pts',(-0.984363832718973,3.0903645027975,5.33533517957524));
#9954=CARTESIAN_POINT('Ctrl Pts',(-0.925066609102487,3.09427112673115,5.36991580312336));
#9955=CARTESIAN_POINT('Ctrl Pts',(-0.863902844489848,3.09817775066479,5.40139258262396));
#9956=CARTESIAN_POINT('Ctrl Pts',(-0.801231943442468,3.10208437459844,5.42956824567131));
#9957=CARTESIAN_POINT('Ctrl Pts',(-0.738578754873705,3.10598989441531,5.45773594552009));
#9958=CARTESIAN_POINT('Ctrl Pts',(-0.67441972353548,3.10989541423219,5.4826041796896));
#9959=CARTESIAN_POINT('Ctrl Pts',(-0.609136553961639,3.11380093404906,5.50402277212601));
#9960=CARTESIAN_POINT('Ctrl Pts',(-0.543849491170423,3.11770668677493,5.52544264187841));
#9961=CARTESIAN_POINT('Ctrl Pts',(-0.477438624815021,3.12161243950081,5.54341231069829));
#9962=CARTESIAN_POINT('Ctrl Pts',(-0.410301499895405,3.12551819222668,5.55783124535439));
#9963=CARTESIAN_POINT('Ctrl Pts',(-0.34309316134728,3.12942808785894,5.5722654744494));
#9964=CARTESIAN_POINT('Ctrl Pts',(-0.275157508270687,3.1333379834912,5.58314134960714));
#9965=CARTESIAN_POINT('Ctrl Pts',(-0.2069019859915,3.13724787912346,5.59040953981388));
#9966=CARTESIAN_POINT('Ctrl Pts',(-0.138605654105284,3.14116011246113,5.59768207563218));
#9967=CARTESIAN_POINT('Ctrl Pts',(-0.06998956321348,3.14507234579881,5.60134260730781));
#9968=CARTESIAN_POINT('Ctrl Pts',(-0.00146317179453743,3.14898457913649,
5.60139392046606));
#9969=CARTESIAN_POINT('Ctrl Pts',(0.067180811382858,3.15290352589345,5.60144532167804));
#9970=CARTESIAN_POINT('Ctrl Pts',(0.135734297357666,3.15682247265042,5.59787516888493));
#9971=CARTESIAN_POINT('Ctrl Pts',(0.203791822252832,3.16074141940738,5.59073820864039));
#9972=CARTESIAN_POINT('Ctrl Pts',(0.235189036955191,3.16254936074708,5.5874456899444));
#9973=CARTESIAN_POINT('Ctrl Pts',(0.266480827608339,3.16435730208677,5.5833947714429));
#9974=CARTESIAN_POINT('Ctrl Pts',(0.297628256975104,3.16616524342647,5.57859446327402));
#9975=CARTESIAN_POINT('Ctrl Pts',(0.365149803826224,3.17008450733859,5.56818833218988));
#9976=CARTESIAN_POINT('Ctrl Pts',(0.432257843245372,3.17400377125071,5.55421627178064));
#9977=CARTESIAN_POINT('Ctrl Pts',(0.498547063155325,3.17792303516283,5.53672419753157));
#9978=CARTESIAN_POINT('Ctrl Pts',(0.564736937701917,3.18183642540955,5.51925833804978));
#9979=CARTESIAN_POINT('Ctrl Pts',(0.630109956738292,3.18574981565627,5.49828305905186));
#9980=CARTESIAN_POINT('Ctrl Pts',(0.694269029376427,3.18966320590299,5.47389563577562));
#9981=CARTESIAN_POINT('Ctrl Pts',(0.758353199621903,3.19357202746938,5.44953668355233));
#9982=CARTESIAN_POINT('Ctrl Pts',(0.821225780809522,3.19748084903577,5.42177367228877));
#9983=CARTESIAN_POINT('Ctrl Pts',(0.882504692402788,3.20138967060216,5.39075371636989));
#9984=CARTESIAN_POINT('Ctrl Pts',(0.943745516642623,3.20529606267585,5.35975304062414));
#9985=CARTESIAN_POINT('Ctrl Pts',(1.00339419865734,3.20920245474955,5.32549965745886));
#9986=CARTESIAN_POINT('Ctrl Pts',(1.06108995211054,3.21310884682324,5.28818821325307));
#9987=CARTESIAN_POINT('Ctrl Pts',(1.11876960040286,3.21701414846879,5.25088718414328));
#9988=CARTESIAN_POINT('Ctrl Pts',(1.17449698980804,3.22091945011435,5.21053005545053));
#9989=CARTESIAN_POINT('Ctrl Pts',(1.22793877375832,3.22482475175991,5.1673557730219));
#9990=CARTESIAN_POINT('Ctrl Pts',(1.28138393793849,3.2287303004185,5.12417875978995));
#9991=CARTESIAN_POINT('Ctrl Pts',(1.33254282891518,3.2326358490771,5.07818454995102));
#9992=CARTESIAN_POINT('Ctrl Pts',(1.38111518643653,3.23654139773569,5.02965234646521));
#9993=CARTESIAN_POINT('Ctrl Pts',(1.42973935265201,3.24045111216647,4.98106837711474));
#9994=CARTESIAN_POINT('Ctrl Pts',(1.4757711312666,3.24436082659725,4.92994135975646));
#9995=CARTESIAN_POINT('Ctrl Pts',(1.51894788216805,3.24827054102802,4.87658661406792));
#9996=CARTESIAN_POINT('Ctrl Pts',(1.56215059095571,3.25218260598125,4.82319979147714));
#9997=CARTESIAN_POINT('Ctrl Pts',(1.60249456730862,3.25609467093448,4.7675829729797));
#9998=CARTESIAN_POINT('Ctrl Pts',(1.63975984437483,3.26000673588771,4.71008146489945));
#9999=CARTESIAN_POINT('Ctrl Pts',(1.67708927762243,3.26392553588139,4.65248096179022));
#10000=CARTESIAN_POINT('Ctrl Pts',(1.71132918811499,3.26784433587508,4.59298971906681));
#10001=CARTESIAN_POINT('Ctrl Pts',(1.74230541245396,3.27176313586877,4.53197790116833));
#10002=CARTESIAN_POINT('Ctrl Pts',(1.75661166256366,3.27357301857836,4.50379982765775));
#10003=CARTESIAN_POINT('Ctrl Pts',(1.77022243794752,3.27538290128796,4.47529769357851));
#10004=CARTESIAN_POINT('Ctrl Pts',(1.78312412104051,3.27719278399755,4.44650920908366));
#10005=CARTESIAN_POINT('Ctrl Pts',(1.81367060805643,3.28147792712892,4.37834856201985));
#10006=CARTESIAN_POINT('Ctrl Pts',(1.84034342649058,3.28576307026028,4.3083488830867));
#10007=CARTESIAN_POINT('Ctrl Pts',(1.8629392632891,3.29004821339165,4.2369479444808));
#10008=CARTESIAN_POINT('Ctrl Pts',(1.88547113914471,3.29432122677551,4.16574911706015));
#10009=CARTESIAN_POINT('Ctrl Pts',(1.903948906458,3.29859424015936,4.09315724465514));
#10010=CARTESIAN_POINT('Ctrl Pts',(1.9182171352479,3.30286725354322,4.0196296386283));
#10011=CARTESIAN_POINT('Ctrl Pts',(1.93241976769603,3.30712062229911,3.94644006628769));
#10012=CARTESIAN_POINT('Ctrl Pts',(1.94245134242074,3.311373991055,3.87232365766408));
#10013=CARTESIAN_POINT('Ctrl Pts',(1.9482066680862,3.31562735981089,3.79774997508184));
#10014=CARTESIAN_POINT('Ctrl Pts',(1.95204184265101,3.31846167581933,3.74805633352817));
#10015=CARTESIAN_POINT('Ctrl Pts',(1.95397914847566,3.32129599182777,3.6981600165373));
#10016=CARTESIAN_POINT('Ctrl Pts',(1.95399983251307,3.3241303078362,3.64820350405597));
#10017=CARTESIAN_POINT('Origin',(0.,0.,3.64739446828387));
#10018=CARTESIAN_POINT('',(1.95399924590383,4.12586969212423,3.64567778332304));
#10019=CARTESIAN_POINT('',(1.95399922086733,4.02413030792419,3.64564951846532));
#10020=CARTESIAN_POINT('',(1.954,4.33875158023511E-16,3.64739446828387));
#10021=CARTESIAN_POINT('Ctrl Pts',(1.95399924590383,4.12586969212423,3.64567778332304));
#10022=CARTESIAN_POINT('Ctrl Pts',(1.95405905160708,4.12199411980701,3.71375101849606));
#10023=CARTESIAN_POINT('Ctrl Pts',(1.95055728305734,4.11811854748978,3.78189644852607));
#10024=CARTESIAN_POINT('Ctrl Pts',(1.94349799785706,4.11424297517256,3.84970989608312));
#10025=CARTESIAN_POINT('Ctrl Pts',(1.93644199829586,4.1103692066827,3.91749178088177));
#10026=CARTESIAN_POINT('Ctrl Pts',(1.92583181766028,4.10649543819285,3.98494149260626));
#10027=CARTESIAN_POINT('Ctrl Pts',(1.91172349358429,4.10262166970299,4.05165834754822));
#10028=CARTESIAN_POINT('Ctrl Pts',(1.89761670747935,4.09874832349886,4.11836792957879));
#10029=CARTESIAN_POINT('Ctrl Pts',(1.88001263979034,4.09487497729472,4.1843443241814));
#10030=CARTESIAN_POINT('Ctrl Pts',(1.85901836975731,4.09100163109058,4.24919734373801));
#10031=CARTESIAN_POINT('Ctrl Pts',(1.83800398835006,4.08712457443046,4.31411248897668));
#10032=CARTESIAN_POINT('Ctrl Pts',(1.81359307231295,4.08324751777033,4.37790163250655));
#10033=CARTESIAN_POINT('Ctrl Pts',(1.78594218915486,4.07937046111021,4.44019109857233));
#10034=CARTESIAN_POINT('Ctrl Pts',(1.75827826652902,4.07549157612673,4.50250993879877));
#10035=CARTESIAN_POINT('Ctrl Pts',(1.72737156188945,4.07161269114325,4.56332724688238));
#10036=CARTESIAN_POINT('Ctrl Pts',(1.69342499635001,4.06773380615978,4.622293325467));
#10037=CARTESIAN_POINT('Ctrl Pts',(1.65941549088065,4.06384772938105,4.6813687323679));
#10038=CARTESIAN_POINT('Ctrl Pts',(1.62235514002204,4.05996165260232,4.73858563361944));
#10039=CARTESIAN_POINT('Ctrl Pts',(1.58249024166095,4.05607557582359,4.79362334379167));
#10040=CARTESIAN_POINT('Ctrl Pts',(1.54929063553274,4.05283923950412,4.83945891280191));
#10041=CARTESIAN_POINT('Ctrl Pts',(1.514146763539,4.04960290318465,4.88378353901681));
#10042=CARTESIAN_POINT('Ctrl Pts',(1.47722071628238,4.04636656686519,4.92643119777453));
#10043=CARTESIAN_POINT('Ctrl Pts',(1.43251138708057,4.04244807472577,4.97806814125332));
#10044=CARTESIAN_POINT('Ctrl Pts',(1.38500289026924,4.03852958258635,5.02746012816026));
#10045=CARTESIAN_POINT('Ctrl Pts',(1.33494940519801,4.03461109044694,5.07428832753251));
#10046=CARTESIAN_POINT('Ctrl Pts',(1.28497117715546,4.0306984898868,5.12104611919712));
#10047=CARTESIAN_POINT('Ctrl Pts',(1.23245591134347,4.02678588932666,5.16524744040498));
#10048=CARTESIAN_POINT('Ctrl Pts',(1.17769692864332,4.02287328876652,5.20660771356628));
#10049=CARTESIAN_POINT('Ctrl Pts',(1.12300220412355,4.01896527953697,5.24791945156929));
#10050=CARTESIAN_POINT('Ctrl Pts',(1.06606938237354,4.01505727030743,5.28639646773842));
#10051=CARTESIAN_POINT('Ctrl Pts',(1.0072260265981,4.01114926107788,5.3217933847143));
#10052=CARTESIAN_POINT('Ctrl Pts',(0.948419456670251,4.00724369493524,5.35716817335342));
#10053=CARTESIAN_POINT('Ctrl Pts',(0.887705142447654,4.0033381287926,5.38946642953763));
#10054=CARTESIAN_POINT('Ctrl Pts',(0.825439595234405,3.99943256264996,5.4184860736559));
#10055=CARTESIAN_POINT('Ctrl Pts',(0.76319162922557,3.99552809927698,5.44749752383196));
#10056=CARTESIAN_POINT('Ctrl Pts',(0.699393745278743,3.99162363590401,5.47323199209065));
#10057=CARTESIAN_POINT('Ctrl Pts',(0.634425395957633,3.98771917253103,5.49553418620673));
#10058=CARTESIAN_POINT('Ctrl Pts',(0.569453121200777,3.98381447324749,5.51783772783789));
#10059=CARTESIAN_POINT('Ctrl Pts',(0.503310706621938,3.97990977396395,5.53670842637455));
#10060=CARTESIAN_POINT('Ctrl Pts',(0.436394118017655,3.97600507468041,5.55204041274693));
#10061=CARTESIAN_POINT('Ctrl Pts',(0.369406327617285,3.97209622064828,5.56738871293611));
#10062=CARTESIAN_POINT('Ctrl Pts',(0.301643199517571,3.96818736661615,5.57919067659138));
#10063=CARTESIAN_POINT('Ctrl Pts',(0.233511292378915,3.96427851258401,5.58739149826395));
#10064=CARTESIAN_POINT('Ctrl Pts',(0.165338546892023,3.96036731558001,5.59559723551904));
#10065=CARTESIAN_POINT('Ctrl Pts',(0.0967970731610387,3.956456118576,5.60019750197605));
#10066=CARTESIAN_POINT('Ctrl Pts',(0.028296142099444,3.952544921572,5.60118957738367));
#10067=CARTESIAN_POINT('Ctrl Pts',(-0.0403227014498265,3.94862699211981,
5.60218336047726));
#10068=CARTESIAN_POINT('Ctrl Pts',(-0.108900371926817,3.94470906266763,
5.59955657561388));
#10069=CARTESIAN_POINT('Ctrl Pts',(-0.177030896040787,3.94079113321544,
5.59335851261948));
#10070=CARTESIAN_POINT('Ctrl Pts',(-0.208633889969856,3.93897376424167,
5.59048348193784));
#10071=CARTESIAN_POINT('Ctrl Pts',(-0.240140795167361,3.93715639526789,
5.58684076103463));
#10072=CARTESIAN_POINT('Ctrl Pts',(-0.271511933329573,3.93533902629411,
5.58243898199916));
#10073=CARTESIAN_POINT('Ctrl Pts',(-0.339152417294976,3.93142052909792,
5.57294814163728));
#10074=CARTESIAN_POINT('Ctrl Pts',(-0.40642843104342,3.92750203190173,5.55988765115014));
#10075=CARTESIAN_POINT('Ctrl Pts',(-0.472934213080374,3.92358353470554,
5.54329774379611));
#10076=CARTESIAN_POINT('Ctrl Pts',(-0.539340002519933,3.91967092903788,
5.52673277965569));
#10077=CARTESIAN_POINT('Ctrl Pts',(-0.604977385279366,3.91575832337022,
5.50664904841401));
#10078=CARTESIAN_POINT('Ctrl Pts',(-0.669448099005873,3.91184571770256,
5.48313825289474));
#10079=CARTESIAN_POINT('Ctrl Pts',(-0.733843159012434,3.90793770331606,
5.45965504632302));
#10080=CARTESIAN_POINT('Ctrl Pts',(-0.797073809109829,3.90402968892957,
5.4327529300141));
#10081=CARTESIAN_POINT('Ctrl Pts',(-0.858756100669926,3.90012167454307,
5.4025736498953));
#10082=CARTESIAN_POINT('Ctrl Pts',(-0.920399832111471,3.89621610321591,
5.37241323607654));
#10083=CARTESIAN_POINT('Ctrl Pts',(-0.980496684385748,3.89231053188874,
5.33897993808291));
#10084=CARTESIAN_POINT('Ctrl Pts',(-1.03868333861991,3.88840496056158,5.30246332548389));
#10085=CARTESIAN_POINT('Ctrl Pts',(-1.09685356367207,3.88450049198457,5.26595702346353));
#10086=CARTESIAN_POINT('Ctrl Pts',(-1.15311424506699,3.88059602340757,5.2263693964088));
#10087=CARTESIAN_POINT('Ctrl Pts',(-1.20712888640225,3.87669155483056,5.18393468956455));
#10088=CARTESIAN_POINT('Ctrl Pts',(-1.26114679149635,3.87278685033153,5.14149741866273));
#10089=CARTESIAN_POINT('Ctrl Pts',(-1.31291800198358,3.86888214583249,5.09621303225255));
#10090=CARTESIAN_POINT('Ctrl Pts',(-1.36213854850426,3.86497744133346,5.04835648585562));
#10091=CARTESIAN_POINT('Ctrl Pts',(-1.4114114672533,3.86106858210453,5.00044901856988));
#10092=CARTESIAN_POINT('Ctrl Pts',(-1.45812795256841,3.85715972287561,4.9499642728998));
#10093=CARTESIAN_POINT('Ctrl Pts',(-1.50202115528851,3.85325086364669,4.8972138348588));
#10094=CARTESIAN_POINT('Ctrl Pts',(-1.54594066757739,3.84933966144905,4.84443177822558));
#10095=CARTESIAN_POINT('Ctrl Pts',(-1.58703323512614,3.84542845925141,4.78938172056153));
#10096=CARTESIAN_POINT('Ctrl Pts',(-1.62507426724822,3.84151725705377,4.73240581657829));
#10097=CARTESIAN_POINT('Ctrl Pts',(-1.66318077975211,3.83759932246748,4.67533183944249));
#10098=CARTESIAN_POINT('Ctrl Pts',(-1.69822502260319,3.83368138788118,4.61632582249903));
#10099=CARTESIAN_POINT('Ctrl Pts',(-1.73002786493552,3.82976345329488,4.55575540235504));
#10100=CARTESIAN_POINT('Ctrl Pts',(-1.74477952053953,3.82794613077093,4.52765998973696));
#10101=CARTESIAN_POINT('Ctrl Pts',(-1.75883445140532,3.82612880824699,4.49922828152494));
#10102=CARTESIAN_POINT('Ctrl Pts',(-1.77217835395763,3.82431148572304,4.47049827811835));
#10103=CARTESIAN_POINT('Ctrl Pts',(-1.80095022580009,3.82039300905922,4.40855118484428));
#10104=CARTESIAN_POINT('Ctrl Pts',(-1.82652701787644,3.8164745323954,4.34497116695147));
#10105=CARTESIAN_POINT('Ctrl Pts',(-1.84872211032283,3.81255605573158,4.28012075887366));
#10106=CARTESIAN_POINT('Ctrl Pts',(-1.87088383166217,3.80864347063612,4.21536785567966));
#10107=CARTESIAN_POINT('Ctrl Pts',(-1.88967378643487,3.80473088554065,4.1493488147063));
#10108=CARTESIAN_POINT('Ctrl Pts',(-1.90495264280262,3.80081830044519,4.08244783130882));
#10109=CARTESIAN_POINT('Ctrl Pts',(-1.92021357012784,3.79691030659025,4.01562535317036));
#10110=CARTESIAN_POINT('Ctrl Pts',(-1.93197147273751,3.79300231273531,3.94792346515413));
#10111=CARTESIAN_POINT('Ctrl Pts',(-1.94013681071579,3.78909431888038,3.87974152702479));
#10112=CARTESIAN_POINT('Ctrl Pts',(-1.94829704425871,3.78518876804765,3.81160221178471));
#10113=CARTESIAN_POINT('Ctrl Pts',(-1.95286910989962,3.78128321721492,3.74298392892437));
#10114=CARTESIAN_POINT('Ctrl Pts',(-1.95381482691184,3.7773776663822,3.6742946939234));
#10115=CARTESIAN_POINT('Ctrl Pts',(-1.95476027691291,3.77347321823198,3.60562485245253));
#10116=CARTESIAN_POINT('Ctrl Pts',(-1.95208140407651,3.76956877008176,3.53688459010394));
#10117=CARTESIAN_POINT('Ctrl Pts',(-1.94579210753576,3.76566432193154,3.46848366857752));
#10118=CARTESIAN_POINT('Ctrl Pts',(-1.93950243081286,3.76175963776104,3.40007861227875));
#10119=CARTESIAN_POINT('Ctrl Pts',(-1.92960194468175,3.75785495359055,3.33201342699231));
#10120=CARTESIAN_POINT('Ctrl Pts',(-1.91615639730603,3.75395026942005,3.26469267698523));
#10121=CARTESIAN_POINT('Ctrl Pts',(-1.90269654238134,3.75004143023389,3.19730029025706));
#10122=CARTESIAN_POINT('Ctrl Pts',(-1.88568419438451,3.74613259104773,3.13065440286264));
#10123=CARTESIAN_POINT('Ctrl Pts',(-1.86523601993762,3.74222375186157,3.06514830906317));
#10124=CARTESIAN_POINT('Ctrl Pts',(-1.84477558809876,3.73831256957264,2.99960294848852));
#10125=CARTESIAN_POINT('Ctrl Pts',(-1.82087540201023,3.73440138728372,2.93519920237455));
#10126=CARTESIAN_POINT('Ctrl Pts',(-1.79370074809983,3.73049020499479,2.87231148803844));
#10127=CARTESIAN_POINT('Ctrl Pts',(-1.76647931509474,3.72657228990378,2.8093155172972));
#10128=CARTESIAN_POINT('Ctrl Pts',(-1.73597238288092,3.72265437481276,2.74784122711604));
#10129=CARTESIAN_POINT('Ctrl Pts',(-1.70239132559573,3.71873645972175,2.68823870693099));
#10130=CARTESIAN_POINT('Ctrl Pts',(-1.68681320986639,3.71691895486515,2.66058934052428));
#10131=CARTESIAN_POINT('Ctrl Pts',(-1.67057415673792,3.71510145000855,2.63334236909012));
#10132=CARTESIAN_POINT('Ctrl Pts',(-1.65369831032235,3.71328394515195,2.60653045294036));
#10133=CARTESIAN_POINT('Ctrl Pts',(-1.61731435401473,3.70936544437499,2.54872454728717));
#10134=CARTESIAN_POINT('Ctrl Pts',(-1.57782384186812,3.70544694359802,2.49271435131032));
#10135=CARTESIAN_POINT('Ctrl Pts',(-1.53542980063064,3.70152844282106,2.43885347711504));
#10136=CARTESIAN_POINT('Ctrl Pts',(-1.4930995010845,3.69761583371801,2.38507358560312));
#10137=CARTESIAN_POINT('Ctrl Pts',(-1.44787463843241,3.69370322461497,2.33343698552257));
#10138=CARTESIAN_POINT('Ctrl Pts',(-1.40000211194091,3.68979061551192,2.2842693505632));
#10139=CARTESIAN_POINT('Ctrl Pts',(-1.35218576462597,3.68588259791832,2.23515941461092));
#10140=CARTESIAN_POINT('Ctrl Pts',(-1.30172826565808,3.68197458032472,2.18851304019544));
#10141=CARTESIAN_POINT('Ctrl Pts',(-1.24891629228561,3.67806656273112,2.14462233157666));
#10142=CARTESIAN_POINT('Ctrl Pts',(-1.19613733574055,3.67416098833996,2.10075906241637));
#10143=CARTESIAN_POINT('Ctrl Pts',(-1.14100720208999,3.6702554139488,2.05964835518215));
#10144=CARTESIAN_POINT('Ctrl Pts',(-1.0838477331168,3.66634983955765,2.02154389353305));
#10145=CARTESIAN_POINT('Ctrl Pts',(-1.02670440542699,3.66244536806307,1.98345019221683));
#10146=CARTESIAN_POINT('Ctrl Pts',(-0.967533289053187,3.6585408965685,1.94836132382118));
#10147=CARTESIAN_POINT('Ctrl Pts',(-0.906685980488979,3.65463642507392,
1.91648819329821));
#10148=CARTESIAN_POINT('Ctrl Pts',(-0.845834997649865,3.65073171780719,
1.88461313811092));
#10149=CARTESIAN_POINT('Ctrl Pts',(-0.783308058478771,3.64682701054045,
1.85595443221954));
#10150=CARTESIAN_POINT('Ctrl Pts',(-0.719480558857405,3.64292230327371,
1.8306766240862));
#10151=CARTESIAN_POINT('Ctrl Pts',(-0.655585148751602,3.63901344151927,
1.80537192114723));
#10152=CARTESIAN_POINT('Ctrl Pts',(-0.590386874763926,3.63510457976483,
1.78345547613733));
#10153=CARTESIAN_POINT('Ctrl Pts',(-0.524279328070026,3.63119571801039,
1.76504296387285));
#10154=CARTESIAN_POINT('Ctrl Pts',(-0.458132158838919,3.62728451342177,
1.74661941579644));
#10155=CARTESIAN_POINT('Ctrl Pts',(-0.391075112364722,3.62337330883315,
1.73170408691508));
#10156=CARTESIAN_POINT('Ctrl Pts',(-0.323512339793095,3.61946210424453,
1.72036157650397));
#10157=CARTESIAN_POINT('Ctrl Pts',(-0.255833274830453,3.61554416749681,
1.70899954280207));
#10158=CARTESIAN_POINT('Ctrl Pts',(-0.1876472347705,3.6116262307491,1.70122265691393));
#10159=CARTESIAN_POINT('Ctrl Pts',(-0.119362978636752,3.60770829400139,
1.69704360771263));
#10160=CARTESIAN_POINT('Ctrl Pts',(-0.0876899972033133,3.60589099752789,
1.69510519679251));
#10161=CARTESIAN_POINT('Ctrl Pts',(-0.0559958742506681,3.60407370105439,
1.69394011591222));
#10162=CARTESIAN_POINT('Ctrl Pts',(-0.0243211323379373,3.60225640458088,
1.69354583481151));
#10163=CARTESIAN_POINT('Ctrl Pts',(0.0439771955415224,3.59833787824392,
1.69269567035027));
#10164=CARTESIAN_POINT('Ctrl Pts',(0.112455204635595,3.59441935190696,1.69542926853147));
#10165=CARTESIAN_POINT('Ctrl Pts',(0.180705710999457,3.59050082557,1.70176823336305));
#10166=CARTESIAN_POINT('Ctrl Pts',(0.248853606178245,3.58658819053923,1.70809766788154));
#10167=CARTESIAN_POINT('Ctrl Pts',(0.316774191731649,3.58267555550847,1.71802166608982));
#10168=CARTESIAN_POINT('Ctrl Pts',(0.384059911532946,3.57876292047771,1.73150982030704));
#10169=CARTESIAN_POINT('Ctrl Pts',(0.451266678062233,3.57485487654501,1.74498214748233));
#10170=CARTESIAN_POINT('Ctrl Pts',(0.517839578447494,3.57094683261231,1.76201022850722));
#10171=CARTESIAN_POINT('Ctrl Pts',(0.583377636205858,3.5670387886796,1.78251202330916));
#10172=CARTESIAN_POINT('Ctrl Pts',(0.648874725369101,3.5631331877102,1.80300100220291));
#10173=CARTESIAN_POINT('Ctrl Pts',(0.713337786868064,3.55922758674079,1.82695924084991));
#10174=CARTESIAN_POINT('Ctrl Pts',(0.776379002836208,3.55532198577139,1.85425430534204));
#10175=CARTESIAN_POINT('Ctrl Pts',(0.839402419871464,3.55141748750168,1.88154166339936));
#10176=CARTESIAN_POINT('Ctrl Pts',(0.901004337256454,3.54751298923197,1.91216378171598));
#10177=CARTESIAN_POINT('Ctrl Pts',(0.960816693257145,3.54360849096226,1.94594000754788));
#10178=CARTESIAN_POINT('Ctrl Pts',(1.02063266338498,3.53970375676549,1.97971827428876));
#10179=CARTESIAN_POINT('Ctrl Pts',(1.07865843051714,3.53579902256872,2.01665078287664));
#10180=CARTESIAN_POINT('Ctrl Pts',(1.13455192769971,3.53189428837195,2.05651171856507));
#10181=CARTESIAN_POINT('Ctrl Pts',(1.19050489408076,3.52798539964157,2.09641506523179));
#10182=CARTESIAN_POINT('Ctrl Pts',(1.24432066185116,3.52407651091118,2.13925277096345));
#10183=CARTESIAN_POINT('Ctrl Pts',(1.29568831620735,3.5201676221808,2.18475719703588));
#10184=CARTESIAN_POINT('Ctrl Pts',(1.34708675917241,3.51625639055102,2.23028889743092));
#10185=CARTESIAN_POINT('Ctrl Pts',(1.39603381800536,3.51234515892124,2.27849015414639));
#10186=CARTESIAN_POINT('Ctrl Pts',(1.44225572602455,3.50843392729146,2.32905671916592));
#10187=CARTESIAN_POINT('Ctrl Pts',(1.48855719073511,3.50451596368844,2.37971031885751));
#10188=CARTESIAN_POINT('Ctrl Pts',(1.53212383128939,3.50059800008543,2.43273697234043));
#10189=CARTESIAN_POINT('Ctrl Pts',(1.57272296308911,3.49668003648242,2.48780036629291));
#10190=CARTESIAN_POINT('Ctrl Pts',(1.59155186606893,3.49486297899154,2.51333744692767));
#10191=CARTESIAN_POINT('Ctrl Pts',(1.60974311680235,3.49304592150067,2.53931221537671));
#10192=CARTESIAN_POINT('Ctrl Pts',(1.62727683669187,3.4912288640098,2.5656892881326));
#10193=CARTESIAN_POINT('Ctrl Pts',(1.66576335091087,3.48724042291459,2.6235869614199));
#10194=CARTESIAN_POINT('Ctrl Pts',(1.70122719124069,3.48325198181939,2.68364762603427));
#10195=CARTESIAN_POINT('Ctrl Pts',(1.73342304991814,3.47926354072418,2.74552943957254));
#10196=CARTESIAN_POINT('Ctrl Pts',(1.76556540124553,3.47528172814962,2.8073084097019));
#10197=CARTESIAN_POINT('Ctrl Pts',(1.79445034260505,3.47129991557505,2.87090210568559));
#10198=CARTESIAN_POINT('Ctrl Pts',(1.81987604929994,3.46731810300049,2.93594020750215));
#10199=CARTESIAN_POINT('Ctrl Pts',(1.84526035100446,3.46334277468665,3.00087239674718));
#10200=CARTESIAN_POINT('Ctrl Pts',(1.86719645127401,3.45936744637281,3.06724388003212));
#10201=CARTESIAN_POINT('Ctrl Pts',(1.8855294599692,3.45539211805897,3.13466193022113));
#10202=CARTESIAN_POINT('Ctrl Pts',(1.90384492772801,3.45142059332054,3.20201547513723));
#10203=CARTESIAN_POINT('Ctrl Pts',(1.91856402806963,3.44744906858211,3.2704131477722));
#10204=CARTESIAN_POINT('Ctrl Pts',(1.92958115826743,3.44347754384368,3.3394455217695));
#10205=CARTESIAN_POINT('Ctrl Pts',(1.94059067635588,3.43950876316655,3.40843019895554));
#10206=CARTESIAN_POINT('Ctrl Pts',(1.94790323385188,3.43553998248942,3.47804824402431));
#10207=CARTESIAN_POINT('Ctrl Pts',(1.95146428769477,3.43157120181229,3.54787997762083));
#10208=CARTESIAN_POINT('Ctrl Pts',(1.95316954552555,3.42967069858293,3.58131982880137));
#10209=CARTESIAN_POINT('Ctrl Pts',(1.9540153051049,3.42777019535358,3.61480856012882));
#10210=CARTESIAN_POINT('Ctrl Pts',(1.95399979033479,3.42586969212423,3.64829965974897));
#10211=CARTESIAN_POINT('Ctrl Pts',(1.95399983251336,3.32413030787577,3.64820350335859));
#10212=CARTESIAN_POINT('Ctrl Pts',(1.95402888143147,3.32811085978268,3.57804389856128));
#10213=CARTESIAN_POINT('Ctrl Pts',(1.95027489940238,3.3320914116896,3.507903037527));
#10214=CARTESIAN_POINT('Ctrl Pts',(1.94277019996063,3.33607196359651,3.43820567760683));
#10215=CARTESIAN_POINT('Ctrl Pts',(1.93526110496938,3.34005484693764,3.36846749550601));
#10216=CARTESIAN_POINT('Ctrl Pts',(1.92399697641739,3.34403773027876,3.2991737923561));
#10217=CARTESIAN_POINT('Ctrl Pts',(1.90906168828393,3.34802061361988,3.2307417707929));
#10218=CARTESIAN_POINT('Ctrl Pts',(1.89410146887175,3.35201014553542,3.16219551656222));
#10219=CARTESIAN_POINT('Ctrl Pts',(1.87545795844452,3.35599967745097,3.09451426921879));
#10220=CARTESIAN_POINT('Ctrl Pts',(1.8532655171138,3.35998920936651,3.0281021923132));
#10221=CARTESIAN_POINT('Ctrl Pts',(1.83105197340533,3.36398253485341,2.96162696540474));
#10222=CARTESIAN_POINT('Ctrl Pts',(1.80528295013382,3.3679758603403,2.89642374334015));
#10223=CARTESIAN_POINT('Ctrl Pts',(1.77614075125037,3.37196918582719,2.83287618626205));
#10224=CARTESIAN_POINT('Ctrl Pts',(1.74693910067287,3.37597065791846,2.76919898866038));
#10225=CARTESIAN_POINT('Ctrl Pts',(1.71435075203521,3.37997213000973,2.70718460986608));
#10226=CARTESIAN_POINT('Ctrl Pts',(1.67860342342437,3.383973602101,2.64719121550573));
#10227=CARTESIAN_POINT('Ctrl Pts',(1.66595732884495,3.38538917625688,2.62596775157977));
#10228=CARTESIAN_POINT('Ctrl Pts',(1.65291627738983,3.38680475041275,2.60499692950164));
#10229=CARTESIAN_POINT('Ctrl Pts',(1.63949157496413,3.38822032456863,2.58429363787236));
#10230=CARTESIAN_POINT('Ctrl Pts',(1.60232839550314,3.39213901376762,2.5269813699461));
#10231=CARTESIAN_POINT('Ctrl Pts',(1.56208293473805,3.3960577029666,2.47150688257573));
#10232=CARTESIAN_POINT('Ctrl Pts',(1.51896302007945,3.39997639216559,2.41822102908535));
#10233=CARTESIAN_POINT('Ctrl Pts',(1.47590791688916,3.40388919137145,2.36501526699665));
#10234=CARTESIAN_POINT('Ctrl Pts',(1.42998724131847,3.40780199057731,2.31399198913328));
#10235=CARTESIAN_POINT('Ctrl Pts',(1.3814523097093,3.41171478978318,2.26547351685472));
#10236=CARTESIAN_POINT('Ctrl Pts',(1.33297431285744,3.41562299901094,2.21701196002557));
#10237=CARTESIAN_POINT('Ctrl Pts',(1.28188849665375,3.4195312082387,2.17104971919529));
#10238=CARTESIAN_POINT('Ctrl Pts',(1.2284854962011,3.42343941746646,2.12787500949976));
#10239=CARTESIAN_POINT('Ctrl Pts',(1.17511586903215,3.4273451843263,2.08472728109412));
#10240=CARTESIAN_POINT('Ctrl Pts',(1.11943231171976,3.43125095118614,2.04436393660704));
#10241=CARTESIAN_POINT('Ctrl Pts',(1.06176009971694,3.43515671804598,2.00703429726987));
#10242=CARTESIAN_POINT('Ctrl Pts',(1.00410416509047,3.43906138254412,1.96971519383149));
#10243=CARTESIAN_POINT('Ctrl Pts',(0.944461102619404,3.44296604704227,1.93542836280035));
#10244=CARTESIAN_POINT('Ctrl Pts',(0.883185360289921,3.44687071154042,1.9043799475843));
#10245=CARTESIAN_POINT('Ctrl Pts',(0.821905914294495,3.45077561204669,1.87332965572091));
#10246=CARTESIAN_POINT('Ctrl Pts',(0.758994032295715,3.45468051255296,1.84551838823025));
#10247=CARTESIAN_POINT('Ctrl Pts',(0.694827332237139,3.45858541305923,1.82110561424784));
#10248=CARTESIAN_POINT('Ctrl Pts',(0.630592380268214,3.46249446707377,1.796666873238));
#10249=CARTESIAN_POINT('Ctrl Pts',(0.565100407054043,3.46640352108831,1.77563401497833));
#10250=CARTESIAN_POINT('Ctrl Pts',(0.498746563303162,3.47031257510285,1.75811739342341));
#10251=CARTESIAN_POINT('Ctrl Pts',(0.432352956123435,3.47422397167032,1.74059027479862));
#10252=CARTESIAN_POINT('Ctrl Pts',(0.365096931931761,3.47813536823779,1.72658368679371));
#10253=CARTESIAN_POINT('Ctrl Pts',(0.297383510811573,3.48204676480526,1.71615676994185));
#10254=CARTESIAN_POINT('Ctrl Pts',(0.229553586201177,3.48596489107778,1.70571191318701));
#10255=CARTESIAN_POINT('Ctrl Pts',(0.16126518299087,3.48988301735029,1.69885906877363));
#10256=CARTESIAN_POINT('Ctrl Pts',(0.092927228014007,3.49380114362281,1.69560540942181));
#10257=CARTESIAN_POINT('Ctrl Pts',(0.0612609174780538,3.49561671746177,
1.69409773499041));
#10258=CARTESIAN_POINT('Ctrl Pts',(0.0295839467281558,3.49743229130074,
1.69336213986674));
#10259=CARTESIAN_POINT('Ctrl Pts',(-0.0020633167638207,3.49924786513971,
1.69339555765881));
#10260=CARTESIAN_POINT('Ctrl Pts',(-0.070367973775412,3.50316643928061,
1.69346768366824));
#10261=CARTESIAN_POINT('Ctrl Pts',(-0.138803851921803,3.50708501342151,
1.6971257846081));
#10262=CARTESIAN_POINT('Ctrl Pts',(-0.206963501706444,3.51100358756241,
1.70438594824043));
#10263=CARTESIAN_POINT('Ctrl Pts',(-0.275020711479259,3.51491627231299,
1.71163520026668));
#10264=CARTESIAN_POINT('Ctrl Pts',(-0.342802031772617,3.51882895706358,
1.72247571894333));
#10265=CARTESIAN_POINT('Ctrl Pts',(-0.409900345716198,3.52274164181416,
1.73687158001958));
#10266=CARTESIAN_POINT('Ctrl Pts',(-0.476919971846414,3.52664973806484,
1.75125055872184));
#10267=CARTESIAN_POINT('Ctrl Pts',(-0.543257703856739,3.53055783431552,
1.7691764965273));
#10268=CARTESIAN_POINT('Ctrl Pts',(-0.608513703120392,3.53446593056619,
1.79056193056952));
#10269=CARTESIAN_POINT('Ctrl Pts',(-0.673728937109452,3.53837158543801,
1.81193400517965));
#10270=CARTESIAN_POINT('Ctrl Pts',(-0.737863312607149,3.54227724030983,
1.8367611361605));
#10271=CARTESIAN_POINT('Ctrl Pts',(-0.800530830918342,3.54618289518165,
1.86490564959546));
#10272=CARTESIAN_POINT('Ctrl Pts',(-0.863180680188064,3.55008744885815,
1.8930422277142));
#10273=CARTESIAN_POINT('Ctrl Pts',(-0.924364044941099,3.55399200253465,
1.92449413008883));
#10274=CARTESIAN_POINT('Ctrl Pts',(-0.983715333682362,3.55789655621115,
1.95907573585264));
#10275=CARTESIAN_POINT('Ctrl Pts',(-1.04307023031463,3.56180134724061,1.99365944378924));
#10276=CARTESIAN_POINT('Ctrl Pts',(-1.1005924062468,3.56570613827007,2.03137298304475));
#10277=CARTESIAN_POINT('Ctrl Pts',(-1.15594287369403,3.56961092929953,2.07198592674425));
#10278=CARTESIAN_POINT('Ctrl Pts',(-1.21135225688763,3.57351987663857,2.11264209938112));
#10279=CARTESIAN_POINT('Ctrl Pts',(-1.26458492120614,3.57742882397761,2.15620354395487));
#10280=CARTESIAN_POINT('Ctrl Pts',(-1.31533359401799,3.58133777131664,2.2023984349164));
#10281=CARTESIAN_POINT('Ctrl Pts',(-1.36611269826737,3.58524906265564,2.24862102664054));
#10282=CARTESIAN_POINT('Ctrl Pts',(-1.41440450085397,3.58916035399463,2.29747985777431));
#10283=CARTESIAN_POINT('Ctrl Pts',(-1.45993936916702,3.59307164533362,2.34866699942976));
#10284=CARTESIAN_POINT('Ctrl Pts',(-1.5055526230006,3.59698966972398,2.39994225665228));
#10285=CARTESIAN_POINT('Ctrl Pts',(-1.54839916383633,3.60090769411435,2.45355343977756));
#10286=CARTESIAN_POINT('Ctrl Pts',(-1.58825087105825,3.60482571850471,2.50916111321879));
#10287=CARTESIAN_POINT('Ctrl Pts',(-1.60672781397214,3.60664228090674,2.53494319081025));
#10288=CARTESIAN_POINT('Ctrl Pts',(-1.62456160331133,3.60845884330876,2.56115406024028));
#10289=CARTESIAN_POINT('Ctrl Pts',(-1.64173285670969,3.61027540571079,2.58775810273207));
#10290=CARTESIAN_POINT('Ctrl Pts',(-1.67877187594956,3.61419379700106,2.64514399174383));
#10291=CARTESIAN_POINT('Ctrl Pts',(-1.7128717211391,3.61811218829132,2.70458778327013));
#10292=CARTESIAN_POINT('Ctrl Pts',(-1.74379755342956,3.62203057958159,2.76575616792874));
#10293=CARTESIAN_POINT('Ctrl Pts',(-1.77467687365945,3.62594307766092,2.82683255611057));
#10294=CARTESIAN_POINT('Ctrl Pts',(-1.80239143499207,3.62985557574025,2.88962795431011));
#10295=CARTESIAN_POINT('Ctrl Pts',(-1.82675024602297,3.63376807381959,2.95378107549578));
#10296=CARTESIAN_POINT('Ctrl Pts',(-1.85108046000917,3.63767597865821,3.01785888144244));
#10297=CARTESIAN_POINT('Ctrl Pts',(-1.87206257414133,3.64158388349683,3.08329078713669));
#10298=CARTESIAN_POINT('Ctrl Pts',(-1.88955282088807,3.64549178833545,3.14969361729612));
#10299=CARTESIAN_POINT('Ctrl Pts',(-1.90703212830283,3.64939724896221,3.21605491558839));
#10300=CARTESIAN_POINT('Ctrl Pts',(-1.9210237757486,3.65330270958898,3.28338545919602));
#10301=CARTESIAN_POINT('Ctrl Pts',(-1.93143366978043,3.65720817021575,3.35128641496802));
#10302=CARTESIAN_POINT('Ctrl Pts',(-1.94184062184129,3.66111252710872,3.41916818104986));
#10303=CARTESIAN_POINT('Ctrl Pts',(-1.94866775551529,3.6650168840017,3.48761955338133));
#10304=CARTESIAN_POINT('Ctrl Pts',(-1.9518723184559,3.66892124089468,3.55623278529381));
#10305=CARTESIAN_POINT('Ctrl Pts',(-1.95507707436364,3.67282583289383,3.62485014884563));
#10306=CARTESIAN_POINT('Ctrl Pts',(-1.95465880608775,3.67673042489298,3.69362889995227));
#10307=CARTESIAN_POINT('Ctrl Pts',(-1.95062683160632,3.68063501689213,3.7621592878825));
#10308=CARTESIAN_POINT('Ctrl Pts',(-1.94659056733331,3.68454376315513,3.83076258824859));
#10309=CARTESIAN_POINT('Ctrl Pts',(-1.93893295289844,3.68845250941814,3.89911650621308));
#10310=CARTESIAN_POINT('Ctrl Pts',(-1.92771529253688,3.69236125568115,3.96681543021258));
#10311=CARTESIAN_POINT('Ctrl Pts',(-1.91649090935577,3.69627234448217,4.03455492663406));
#10312=CARTESIAN_POINT('Ctrl Pts',(-1.9017023399559,3.70018343328319,4.10163816753876));
#10313=CARTESIAN_POINT('Ctrl Pts',(-1.88346164729895,3.7040945220842,4.16767153212));
#10314=CARTESIAN_POINT('Ctrl Pts',(-1.86518955342549,3.70801234379545,4.23381857264636));
#10315=CARTESIAN_POINT('Ctrl Pts',(-1.84345363127516,3.7119301655067,4.29891166351186));
#10316=CARTESIAN_POINT('Ctrl Pts',(-1.81841494640218,3.71584798721795,4.36257492292532));
#10317=CARTESIAN_POINT('Ctrl Pts',(-1.80679411803862,3.71766630690592,4.39212199436546));
#10318=CARTESIAN_POINT('Ctrl Pts',(-1.79446252923637,3.7194846265939,4.42136139692646));
#10319=CARTESIAN_POINT('Ctrl Pts',(-1.78143961641532,3.72130294628187,4.45025740370065));
#10320=CARTESIAN_POINT('Ctrl Pts',(-1.75337490510792,3.72522147186894,4.51252903979293));
#10321=CARTESIAN_POINT('Ctrl Pts',(-1.72198563863023,3.72913999745601,4.57345050024927));
#10322=CARTESIAN_POINT('Ctrl Pts',(-1.6874241453808,3.73305852304309,4.63264355028591));
#10323=CARTESIAN_POINT('Ctrl Pts',(-1.65291461281587,3.73697115741272,4.69174760788883));
#10324=CARTESIAN_POINT('Ctrl Pts',(-1.61524256473294,3.74088379178235,4.74912799103301));
#10325=CARTESIAN_POINT('Ctrl Pts',(-1.57460763543134,3.74479642615199,4.804428086828));
#10326=CARTESIAN_POINT('Ctrl Pts',(-1.5340203858993,3.74870446955743,4.85966329520053));
#10327=CARTESIAN_POINT('Ctrl Pts',(-1.49047744950318,3.75261251296288,4.91282266960529));
#10328=CARTESIAN_POINT('Ctrl Pts',(-1.44422248756346,3.75652055636833,4.9635773607483));
#10329=CARTESIAN_POINT('Ctrl Pts',(-1.39799643915049,3.76042615689386,5.01430032562759));
#10330=CARTESIAN_POINT('Ctrl Pts',(-1.34906205859251,3.76433175741939,5.06262122638954));
#10331=CARTESIAN_POINT('Ctrl Pts',(-1.29770313383148,3.76823735794492,5.10824441829378));
#10332=CARTESIAN_POINT('Ctrl Pts',(-1.24635870854784,3.77214185585457,5.15385473001327));
#10333=CARTESIAN_POINT('Ctrl Pts',(-1.19259146538888,3.77604635376421,5.196768518388));
#10334=CARTESIAN_POINT('Ctrl Pts',(-1.13672056180759,3.77995085167385,5.23672840561858));
#10335=CARTESIAN_POINT('Ctrl Pts',(-1.08084628105307,3.78385558559481,5.27669070826492));
#10336=CARTESIAN_POINT('Ctrl Pts',(-1.0228684889009,3.78776031951578,5.31369847130271));
#10337=CARTESIAN_POINT('Ctrl Pts',(-0.963136307333334,3.79166505343674,
5.34753694863554));
#10338=CARTESIAN_POINT('Ctrl Pts',(-0.903340570335241,3.79557394202005,
5.3814114303288));
#10339=CARTESIAN_POINT('Ctrl Pts',(-0.841787147330356,3.79948283060335,
5.41210965379722));
#10340=CARTESIAN_POINT('Ctrl Pts',(-0.778849921474265,3.80339171918666,
5.43946277050327));
#10341=CARTESIAN_POINT('Ctrl Pts',(-0.715874971288074,3.80730295074269,
5.46683228256184));
#10342=CARTESIAN_POINT('Ctrl Pts',(-0.651515028264089,3.81121418229871,
5.49085252547173));
#10343=CARTESIAN_POINT('Ctrl Pts',(-0.586161478091735,3.81512541385474,
5.51140378199486));
#10344=CARTESIAN_POINT('Ctrl Pts',(-0.520695440139975,3.81904337749726,
5.53199041173343));
#10345=CARTESIAN_POINT('Ctrl Pts',(-0.454232857736644,3.82296134113978,
5.54909601583925));
#10346=CARTESIAN_POINT('Ctrl Pts',(-0.387176839061591,3.8268793047823,5.56265165605116));
#10347=CARTESIAN_POINT('Ctrl Pts',(-0.356077812451395,3.82869636547252,
5.56893844766209));
#10348=CARTESIAN_POINT('Ctrl Pts',(-0.324851235324715,3.83051342616273,
5.57446241188905));
#10349=CARTESIAN_POINT('Ctrl Pts',(-0.293537575865702,3.83233048685294,
5.57922046757959));
#10350=CARTESIAN_POINT('Ctrl Pts',(-0.226009535275472,3.83624898600517,
5.58948123503227));
#10351=CARTESIAN_POINT('Ctrl Pts',(-0.157809303592958,3.84016748515741,
5.59621731169598));
#10352=CARTESIAN_POINT('Ctrl Pts',(-0.0893371895893358,3.84408598430965,
5.59935114468739));
#10353=CARTESIAN_POINT('Ctrl Pts',(-0.0209680207510835,3.84799859215052,
5.60248026608256));
#10354=CARTESIAN_POINT('Ctrl Pts',(0.047671731832998,3.85191119999139,5.60201787010988));
#10355=CARTESIAN_POINT('Ctrl Pts',(0.116174217614918,3.85582380783227,5.59793786722724));
#10356=CARTESIAN_POINT('Ctrl Pts',(0.1845963240613,3.85973182470371,5.59386265173177));
#10357=CARTESIAN_POINT('Ctrl Pts',(0.252880995006168,3.86363984157514,5.5861782887665));
#10358=CARTESIAN_POINT('Ctrl Pts',(0.320619775904284,3.86754785844658,5.57491073521888));
#10359=CARTESIAN_POINT('Ctrl Pts',(0.3883162138864,3.87145343245106,5.56365022491987));
#10360=CARTESIAN_POINT('Ctrl Pts',(0.455466954707273,3.87535900645553,5.54881104769229));
#10361=CARTESIAN_POINT('Ctrl Pts',(0.52166962687112,3.87926458046,5.53047088744485));
#10362=CARTESIAN_POINT('Ctrl Pts',(0.587853609714223,3.88316905190286,5.51213590470953));
#10363=CARTESIAN_POINT('Ctrl Pts',(0.653089581535267,3.88707352334571,5.49030203224722));
#10364=CARTESIAN_POINT('Ctrl Pts',(0.71698808841942,3.89097799478857,5.46509743661084));
#10365=CARTESIAN_POINT('Ctrl Pts',(0.780890459305323,3.89488270233842,5.43989131682927));
#10366=CARTESIAN_POINT('Ctrl Pts',(0.843454748170452,3.89878740988827,5.41131425203811));
#10367=CARTESIAN_POINT('Ctrl Pts',(0.904311019378003,3.90269211743813,5.37954272413021));
#10368=CARTESIAN_POINT('Ctrl Pts',(0.965232047594523,3.90660097997771,5.34773738821737));
#10369=CARTESIAN_POINT('Ctrl Pts',(1.0244409942742,3.91050984251729,5.312731033499));
#10370=CARTESIAN_POINT('Ctrl Pts',(1.08159301051882,3.91441870505687,5.27474586229711));
#10371=CARTESIAN_POINT('Ctrl Pts',(1.13877928587347,3.91832991071854,5.23673792132706));
#10372=CARTESIAN_POINT('Ctrl Pts',(1.19390578221152,3.92224111638021,5.1957479036233));
#10373=CARTESIAN_POINT('Ctrl Pts',(1.24665939534098,3.92615232204189,5.15203939384208));
#10374=CARTESIAN_POINT('Ctrl Pts',(1.29950381638474,3.93007026029319,5.1082556460179));
#10375=CARTESIAN_POINT('Ctrl Pts',(1.34996684078175,3.93398819854449,5.0617443998175));
#10376=CARTESIAN_POINT('Ctrl Pts',(1.39777163204783,3.93790613679579,5.01280666415819));
#10377=CARTESIAN_POINT('Ctrl Pts',(1.41994541127994,3.93972343367186,4.99010737988375));
#10378=CARTESIAN_POINT('Ctrl Pts',(1.44154784196988,3.94154073054794,4.9668865155006));
#10379=CARTESIAN_POINT('Ctrl Pts',(1.46255434627851,3.94335802742402,4.94317638827729));
#10380=CARTESIAN_POINT('Ctrl Pts',(1.50741523544836,3.94723899460202,4.89254171941757));
#10381=CARTESIAN_POINT('Ctrl Pts',(1.54974101147076,3.95111996178002,4.83946434287415));
#10382=CARTESIAN_POINT('Ctrl Pts',(1.58925110793399,3.95500092895803,4.7842308311482));
#10383=CARTESIAN_POINT('Ctrl Pts',(1.62870618822605,3.95887649205015,4.72907422979723));
#10384=CARTESIAN_POINT('Ctrl Pts',(1.66535307107132,3.96275205514227,4.6717678481909));
#10385=CARTESIAN_POINT('Ctrl Pts',(1.69894984269427,3.96662761823439,4.61263300461006));
#10386=CARTESIAN_POINT('Ctrl Pts',(1.73251188796112,3.97049917545995,4.55355928409362));
#10387=CARTESIAN_POINT('Ctrl Pts',(1.76302982718898,3.97437073268551,4.49266128331332));
#10388=CARTESIAN_POINT('Ctrl Pts',(1.79030481181464,3.97824228991107,4.43028953200145));
#10389=CARTESIAN_POINT('Ctrl Pts',(1.81756762166772,3.98211211898428,4.36794562165441));
#10390=CARTESIAN_POINT('Ctrl Pts',(1.84159013640073,3.98598194805749,4.30412971952848));
#10391=CARTESIAN_POINT('Ctrl Pts',(1.86222007239024,3.9898517771307,4.23921572676222));
#10392=CARTESIAN_POINT('Ctrl Pts',(1.8828434276196,3.99372037176397,4.17432244096358));
#10393=CARTESIAN_POINT('Ctrl Pts',(1.90007620415411,3.99758896639724,4.10833223942768));
#10394=CARTESIAN_POINT('Ctrl Pts',(1.91381554134504,4.00145756103051,4.04163560478056));
#10395=CARTESIAN_POINT('Ctrl Pts',(1.9275638962301,4.00532869478213,3.97489519437901));
#10396=CARTESIAN_POINT('Ctrl Pts',(1.93781412805708,4.00919982853375,3.90744791692333));
#10397=CARTESIAN_POINT('Ctrl Pts',(1.94451449325912,4.01307096228536,3.83969471660724));
#10398=CARTESIAN_POINT('Ctrl Pts',(1.95089519540874,4.0167574108155,3.77517390649239));
#10399=CARTESIAN_POINT('Ctrl Pts',(1.95405702262766,4.02044385934563,3.71037610742826));
#10400=CARTESIAN_POINT('Ctrl Pts',(1.95399922086809,4.02413030787577,3.64564951931539));
#10401=CARTESIAN_POINT('Origin',(0.,0.,3.64739446828387));
#10402=CARTESIAN_POINT('',(1.95430222507481,4.82586969212423,3.64764326884654));
#10403=CARTESIAN_POINT('',(1.95427619993066,4.72413035081974,3.647777104142));
#10404=CARTESIAN_POINT('',(1.954,4.33875158023511E-16,3.64739446828387));
#10405=CARTESIAN_POINT('Ctrl Pts',(1.95715633972901,4.82586969212423,3.64764363220146));
#10406=CARTESIAN_POINT('Ctrl Pts',(1.95718052860821,4.8250995783704,3.66109012482265));
#10407=CARTESIAN_POINT('Ctrl Pts',(1.95096916696084,4.78732028442627,4.32070869776071));
#10408=CARTESIAN_POINT('Ctrl Pts',(1.21359828804361,4.71253181029161,5.61146159126724));
#10409=CARTESIAN_POINT('Ctrl Pts',(-0.989869636257424,4.60150426972061,
5.73318883630065));
#10410=CARTESIAN_POINT('Ctrl Pts',(-2.28894570144034,4.49047672914949,3.94923537617169));
#10411=CARTESIAN_POINT('Ctrl Pts',(-1.49673214248602,4.37944918857844,1.88950560619207));
#10412=CARTESIAN_POINT('Ctrl Pts',(0.662966995866533,4.26842164800734,1.4358667599271));
#10413=CARTESIAN_POINT('Ctrl Pts',(1.8460276791096,4.18389531480082,2.62877633203429));
#10414=CARTESIAN_POINT('Ctrl Pts',(1.95459509422112,4.13637816178466,3.46119040754886));
#10415=CARTESIAN_POINT('Ctrl Pts',(1.95303263999471,4.12587018895884,3.64566991009788));
#10416=CARTESIAN_POINT('Ctrl Pts',(1.95399922086733,4.02413030792418,3.64564951846532));
#10417=CARTESIAN_POINT('Ctrl Pts',(1.95392015614754,4.02917285126933,3.55711264524746));
#10418=CARTESIAN_POINT('Ctrl Pts',(1.94781926961924,4.03421539461449,3.46884243996873));
#10419=CARTESIAN_POINT('Ctrl Pts',(1.93583046129939,4.03925793795964,3.38154408723206));
#10420=CARTESIAN_POINT('Ctrl Pts',(1.92384165297954,4.0443004813048,3.29424573449538));
#10421=CARTESIAN_POINT('Ctrl Pts',(1.90596512136721,4.04934302464995,3.20791897386854));
#10422=CARTESIAN_POINT('Ctrl Pts',(1.88238740014386,4.05438556799511,3.12324403588909));
#10423=CARTESIAN_POINT('Ctrl Pts',(1.86406544961994,4.0583040649868,3.05744420690734));
#10424=CARTESIAN_POINT('Ctrl Pts',(1.84225301252199,4.06222256197849,2.99247609015031));
#10425=CARTESIAN_POINT('Ctrl Pts',(1.81704344396078,4.06614105897018,2.92873660618317));
#10426=CARTESIAN_POINT('Ctrl Pts',(1.79187177822554,4.0700536644644,2.86509295513607));
#10427=CARTESIAN_POINT('Ctrl Pts',(1.76331329734947,4.07396626995861,2.80267472432111));
#10428=CARTESIAN_POINT('Ctrl Pts',(1.73151138885157,4.07787887545283,2.74186461771168));
#10429=CARTESIAN_POINT('Ctrl Pts',(1.69974679820311,4.08178688971244,2.68112586853045));
#10430=CARTESIAN_POINT('Ctrl Pts',(1.66474656556215,4.08569490397205,2.62199192953867));
#10431=CARTESIAN_POINT('Ctrl Pts',(1.62670179878578,4.08960291823166,2.56482472095712));
#10432=CARTESIAN_POINT('Ctrl Pts',(1.58868081506504,4.0935084894609,2.50769324950887));
#10433=CARTESIAN_POINT('Ctrl Pts',(1.54761934451808,4.09741406069015,2.45252647804713));
#10434=CARTESIAN_POINT('Ctrl Pts',(1.50375318288286,4.10131963191939,2.39965957457861));
#10435=CARTESIAN_POINT('Ctrl Pts',(1.4598994066686,4.1052241004275,2.34680759785157));
#10436=CARTESIAN_POINT('Ctrl Pts',(1.41324282530691,4.1091285689356,2.29625457828357));
#10437=CARTESIAN_POINT('Ctrl Pts',(1.36405998580484,4.11303303744371,2.24830320781295));
#10438=CARTESIAN_POINT('Ctrl Pts',(1.31487417413199,4.11693774190295,2.20034893959053));
#10439=CARTESIAN_POINT('Ctrl Pts',(1.26316215513247,4.1208424463622,2.15499697404981));
#10440=CARTESIAN_POINT('Ctrl Pts',(1.20923654449737,4.12474715082145,2.11251239481631));
#10441=CARTESIAN_POINT('Ctrl Pts',(1.15525355468657,4.12865601005466,2.06998261015803));
#10442=CARTESIAN_POINT('Ctrl Pts',(1.09905265975308,4.13256486928788,2.03032660554034));
#10443=CARTESIAN_POINT('Ctrl Pts',(1.04097789456878,4.13647372852109,1.9937678408316));
#10444=CARTESIAN_POINT('Ctrl Pts',(0.982868319018386,4.14038493074821,1.95718716257781));
#10445=CARTESIAN_POINT('Ctrl Pts',(0.922883067278366,4.14429613297533,1.92370765872131));
#10446=CARTESIAN_POINT('Ctrl Pts',(0.861390907329166,4.14820733520245,1.89350687075356));
#10447=CARTESIAN_POINT('Ctrl Pts',(0.799792899752182,4.15212526985656,1.86325409759346));
#10448=CARTESIAN_POINT('Ctrl Pts',(0.736683259057928,4.15604320451067,1.83629149719215));
#10449=CARTESIAN_POINT('Ctrl Pts',(0.672450022014839,4.15996113916478,1.812748189599));
#10450=CARTESIAN_POINT('Ctrl Pts',(0.642655612984952,4.16177846229858,1.80182769160392));
#10451=CARTESIAN_POINT('Ctrl Pts',(0.612619657991374,4.16359578543238,1.79164216046192));
#10452=CARTESIAN_POINT('Ctrl Pts',(0.582381711025327,4.16541310856617,1.78220076717312));
#10453=CARTESIAN_POINT('Ctrl Pts',(0.517182985803051,4.16933160051186,1.76184333988339));
#10454=CARTESIAN_POINT('Ctrl Pts',(0.450786632722353,4.17325009245754,1.74486834658914));
#10455=CARTESIAN_POINT('Ctrl Pts',(0.383576620845942,4.17716858440322,1.73141300283583));
#10456=CARTESIAN_POINT('Ctrl Pts',(0.316467660640327,4.1810811848136,1.71797788947573));
#10457=CARTESIAN_POINT('Ctrl Pts',(0.248547947918729,4.18499378522397,1.70805201884359));
#10458=CARTESIAN_POINT('Ctrl Pts',(0.180216691748753,4.18890638563435,1.70172287625835));
#10459=CARTESIAN_POINT('Ctrl Pts',(0.111965619313498,4.1928143947796,1.69540116064457));
#10460=CARTESIAN_POINT('Ctrl Pts',(0.0433044499019053,4.19672240392485,
1.69266783597897));
#10461=CARTESIAN_POINT('Ctrl Pts',(-0.0253591372019967,4.2006304130701,
1.69355903146726));
#10462=CARTESIAN_POINT('Ctrl Pts',(-0.0939798000670684,4.20453597916911,
1.6944496698351));
#10463=CARTESIAN_POINT('Ctrl Pts',(-0.162602386999179,4.20844154526813,
1.69896032725903));
#10464=CARTESIAN_POINT('Ctrl Pts',(-0.230817406905043,4.21234711136715,
1.70707508100001));
#10465=CARTESIAN_POINT('Ctrl Pts',(-0.29901316643142,4.21625157473709,1.71518754355589));
#10466=CARTESIAN_POINT('Ctrl Pts',(-0.366801099285137,4.22015603810705,
1.72690202420201));
#10467=CARTESIAN_POINT('Ctrl Pts',(-0.433776846712719,4.224060501477,1.7421507444375));
#10468=CARTESIAN_POINT('Ctrl Pts',(-0.500756641560607,4.22796520079809,
1.75740038617044));
#10469=CARTESIAN_POINT('Ctrl Pts',(-0.566923674618833,4.23186990011919,
1.77618457983964));
#10470=CARTESIAN_POINT('Ctrl Pts',(-0.631885572091625,4.23577459944028,
1.79838483505249));
#10471=CARTESIAN_POINT('Ctrl Pts',(-0.696916592506127,4.2396834535708,1.82060871252711));
#10472=CARTESIAN_POINT('Ctrl Pts',(-0.760739452005128,4.24359230770132,
1.84625574620918));
#10473=CARTESIAN_POINT('Ctrl Pts',(-0.822979658704964,4.24750116183183,
1.87515845652983));
#10474=CARTESIAN_POINT('Ctrl Pts',(-0.885257172815169,4.25141235896911,
1.90407849142783));
#10475=CARTESIAN_POINT('Ctrl Pts',(-0.945949711592307,4.25532355610639,
1.93625785640227));
#10476=CARTESIAN_POINT('Ctrl Pts',(-1.00470790265019,4.25923475324366,1.97148336373439));
#10477=CARTESIAN_POINT('Ctrl Pts',(-1.06356723653612,4.26315268288125,2.00676950614337));
#10478=CARTESIAN_POINT('Ctrl Pts',(-1.12048516969907,4.26707061251884,2.04511198123528));
#10479=CARTESIAN_POINT('Ctrl Pts',(-1.17514251896323,4.27098854215643,2.08625512148463));
#10480=CARTESIAN_POINT('Ctrl Pts',(-1.20049585121116,4.27280591115004,2.10533975911357));
#10481=CARTESIAN_POINT('Ctrl Pts',(-1.22536326940057,4.27462328014365,2.12502645043354));
#10482=CARTESIAN_POINT('Ctrl Pts',(-1.24971558638332,4.27644064913727,2.14528696442451));
#10483=CARTESIAN_POINT('Ctrl Pts',(-1.30222242483607,4.2803591387095,2.18897133071489));
#10484=CARTESIAN_POINT('Ctrl Pts',(-1.3525398362606,4.28427762828174,2.23549850288803));
#10485=CARTESIAN_POINT('Ctrl Pts',(-1.40034404905102,4.28819611785397,2.28462062633965));
#10486=CARTESIAN_POINT('Ctrl Pts',(-1.44807638643017,4.29210871583145,2.33366889285233));
#10487=CARTESIAN_POINT('Ctrl Pts',(-1.49330268437293,4.29602131380893,2.38530401766588));
#10488=CARTESIAN_POINT('Ctrl Pts',(-1.53573264762283,4.2999339117864,2.43923833804847));
#10489=CARTESIAN_POINT('Ctrl Pts',(-1.57811282031323,4.30384191842259,2.49310936778025));
#10490=CARTESIAN_POINT('Ctrl Pts',(-1.6177028727059,4.30774992505877,2.54927384999246));
#10491=CARTESIAN_POINT('Ctrl Pts',(-1.65425102822595,4.31165793169495,2.60740911472673));
#10492=CARTESIAN_POINT('Ctrl Pts',(-1.69077633565019,4.31556349523904,2.66550803617417));
#10493=CARTESIAN_POINT('Ctrl Pts',(-1.72426325734885,4.31946905878312,2.72557488075027));
#10494=CARTESIAN_POINT('Ctrl Pts',(-1.75450273635882,4.3233746223272,2.78725718382899));
#10495=CARTESIAN_POINT('Ctrl Pts',(-1.7847336769792,4.32727908310019,2.84892207035321));
#10496=CARTESIAN_POINT('Ctrl Pts',(-1.8117187788626,4.33118354387319,2.91220106849711));
#10497=CARTESIAN_POINT('Ctrl Pts',(-1.83529531184882,4.33508800464618,2.97671785596931));
#10498=CARTESIAN_POINT('Ctrl Pts',(-1.85887326936181,4.3389927013321,3.04123854163511));
#10499=CARTESIAN_POINT('Ctrl Pts',(-1.87904208272449,4.34289739801802,3.10699670233851));
#10500=CARTESIAN_POINT('Ctrl Pts',(-1.89568811035567,4.34680209470394,3.17359853303731));
#10501=CARTESIAN_POINT('Ctrl Pts',(-1.91235185009414,4.35071094615929,3.24027123102034));
#10502=CARTESIAN_POINT('Ctrl Pts',(-1.92548520407721,4.35461979761464,3.30778891251314));
#10503=CARTESIAN_POINT('Ctrl Pts',(-1.93502537597305,4.35852864906998,3.37574617666332));
#10504=CARTESIAN_POINT('Ctrl Pts',(-1.94457126628318,4.36243984350533,3.44374417464873));
#10505=CARTESIAN_POINT('Ctrl Pts',(-1.95051964551699,4.36635103794068,3.51218178970454));
#10506=CARTESIAN_POINT('Ctrl Pts',(-1.95285973907249,4.37026223237603,3.58064988416092));
#10507=CARTESIAN_POINT('Ctrl Pts',(-1.95520386071968,4.37418015929856,3.64923583534251));
#10508=CARTESIAN_POINT('Ctrl Pts',(-1.95392730970642,4.37809808622109,3.71785187923863));
#10509=CARTESIAN_POINT('Ctrl Pts',(-1.94907137633539,4.38201601314361,3.7860911515538));
#10510=CARTESIAN_POINT('Ctrl Pts',(-1.94681887506376,4.38383340533185,3.81774501414217));
#10511=CARTESIAN_POINT('Ctrl Pts',(-1.9437969214201,4.3856507975201,3.8493179137455));
#10512=CARTESIAN_POINT('Ctrl Pts',(-1.94001336524288,4.38746818970834,3.8807700083025));
#10513=CARTESIAN_POINT('Ctrl Pts',(-1.93185561275431,4.39138668198172,3.94858409394713));
#10514=CARTESIAN_POINT('Ctrl Pts',(-1.92012173726112,4.39530517425511,4.01610403779491));
#10515=CARTESIAN_POINT('Ctrl Pts',(-1.90484397768049,4.39922366652849,4.08292336594094));
#10516=CARTESIAN_POINT('Ctrl Pts',(-1.88958918859449,4.40313626725048,4.14964222955151));
#10517=CARTESIAN_POINT('Ctrl Pts',(-1.8708011990718,4.40704886797247,4.2156620925364));
#10518=CARTESIAN_POINT('Ctrl Pts',(-1.84856385522709,4.41096146869446,4.28058296561144));
#10519=CARTESIAN_POINT('Ctrl Pts',(-1.82635260607385,4.41486947812581,4.34542765646958));
#10520=CARTESIAN_POINT('Ctrl Pts',(-1.80070020003047,4.41877748755716,4.40917545560964));
#10521=CARTESIAN_POINT('Ctrl Pts',(-1.77174079835073,4.42268549698851,4.47143969972419));
#10522=CARTESIAN_POINT('Ctrl Pts',(-1.74279950042004,4.42659106335758,4.53366501982148));
#10523=CARTESIAN_POINT('Ctrl Pts',(-1.71055551477642,4.43049662972664,4.59440817974515));
#10524=CARTESIAN_POINT('Ctrl Pts',(-1.67519122308986,4.4344021960957,4.65330220067422));
#10525=CARTESIAN_POINT('Ctrl Pts',(-1.63983691659179,4.43830665971919,4.71217959274204));
#10526=CARTESIAN_POINT('Ctrl Pts',(-1.60136430610727,4.44221112334267,4.76920846090665));
#10527=CARTESIAN_POINT('Ctrl Pts',(-1.56000096824237,4.44611558696615,4.82404776432433));
#10528=CARTESIAN_POINT('Ctrl Pts',(-1.51863513092428,4.45002028652379,4.87889038150437));
#10529=CARTESIAN_POINT('Ctrl Pts',(-1.47437851761472,4.45392498608142,4.93154278020573));
#10530=CARTESIAN_POINT('Ctrl Pts',(-1.42750004749011,4.45782968563906,4.98169563909042));
#10531=CARTESIAN_POINT('Ctrl Pts',(-1.38057169649302,4.46173853997863,5.03190186294952));
#10532=CARTESIAN_POINT('Ctrl Pts',(-1.33101625765954,4.4656473943182,5.07960287931863));
#10533=CARTESIAN_POINT('Ctrl Pts',(-1.27914000413541,4.46955624865777,5.12452575893493));
#10534=CARTESIAN_POINT('Ctrl Pts',(-1.22723265566561,4.47346744598868,5.16947556560178));
#10535=CARTESIAN_POINT('Ctrl Pts',(-1.17300211219332,4.4773786433196,5.21164361948927));
#10536=CARTESIAN_POINT('Ctrl Pts',(-1.11678604131831,4.48128984065052,5.25079864001244));
#10537=CARTESIAN_POINT('Ctrl Pts',(-1.0604732038458,4.48520777045584,5.29002105937819));
#10538=CARTESIAN_POINT('Ctrl Pts',(-1.00216843533805,4.48912570026116,5.32621983501009));
#10539=CARTESIAN_POINT('Ctrl Pts',(-0.942235775033817,4.49304363006647,
5.35920863584016));
#10540=CARTESIAN_POINT('Ctrl Pts',(-0.914435475194858,4.49486099680412,
5.37451078578224));
#10541=CARTESIAN_POINT('Ctrl Pts',(-0.886285215289913,4.49667836354177,
5.3891229312105));
#10542=CARTESIAN_POINT('Ctrl Pts',(-0.857822709676755,4.49849573027942,
5.40303002236759));
#10543=CARTESIAN_POINT('Ctrl Pts',(-0.79645365023014,4.50241422181615,5.43301561518744));
#10544=CARTESIAN_POINT('Ctrl Pts',(-0.733389092946571,4.50633271335287,
5.45983885890344));
#10545=CARTESIAN_POINT('Ctrl Pts',(-0.668987832150792,4.51025120488959,
5.48330603489981));
#10546=CARTESIAN_POINT('Ctrl Pts',(-0.604683400411588,4.51416380486715,
5.50673792735539));
#10547=CARTESIAN_POINT('Ctrl Pts',(-0.539046712223257,4.5180764048447,5.52682359956585));
#10548=CARTESIAN_POINT('Ctrl Pts',(-0.472459149121543,4.52198900482225,
5.54341618556755));
#10549=CARTESIAN_POINT('Ctrl Pts',(-0.405949724182622,4.52589701350138,
5.55998930075329));
#10550=CARTESIAN_POINT('Ctrl Pts',(-0.338492115304038,4.5298050221805,5.57307735214724));
#10551=CARTESIAN_POINT('Ctrl Pts',(-0.270483845284502,4.53371303085962,
5.58258295766678));
#10552=CARTESIAN_POINT('Ctrl Pts',(-0.202518090200716,4.53761859647207,
5.59208262081773));
#10553=CARTESIAN_POINT('Ctrl Pts',(-0.134002842795731,4.54152416208452,
5.59800421276478));
#10554=CARTESIAN_POINT('Ctrl Pts',(-0.0653452906021543,4.54542972769697,
5.60030153033166));
#10555=CARTESIAN_POINT('Ctrl Pts',(0.00329287591453474,4.54933419056063,
5.60259819924366));
#10556=CARTESIAN_POINT('Ctrl Pts',(0.0720727761918795,4.55323865342428,
5.60127260884809));
#10557=CARTESIAN_POINT('Ctrl Pts',(0.14058445188283,4.55714311628793,5.59633059137483));
#10558=CARTESIAN_POINT('Ctrl Pts',(0.209100267478285,4.56104781508368,5.59138827527392));
#10559=CARTESIAN_POINT('Ctrl Pts',(0.277347336006442,4.56495251387944,5.5828291361928));
#10560=CARTESIAN_POINT('Ctrl Pts',(0.344919875101767,4.56885721267519,5.5707109476392));
#10561=CARTESIAN_POINT('Ctrl Pts',(0.412564314572669,4.57276606625503,5.55857986476019));
#10562=CARTESIAN_POINT('Ctrl Pts',(0.47953230729278,4.57667491983486,5.54288226179697));
#10563=CARTESIAN_POINT('Ctrl Pts',(0.545428336570195,4.5805837734147,5.52372704266035));
#10564=CARTESIAN_POINT('Ctrl Pts',(0.61136386434293,4.58449496998601,5.50456034176464));
#10565=CARTESIAN_POINT('Ctrl Pts',(0.676225685518648,4.58840616655732,5.48193206200186));
#10566=CARTESIAN_POINT('Ctrl Pts',(0.739636199691951,4.59231736312863,5.45600008922649));
#10567=CARTESIAN_POINT('Ctrl Pts',(0.803155864651577,4.5962352921825,5.43002347881877));
#10568=CARTESIAN_POINT('Ctrl Pts',(0.865218792240826,4.60015322123638,5.40073203547596));
#10569=CARTESIAN_POINT('Ctrl Pts',(0.925470798061767,4.60407115029026,5.36833020268388));
#10570=CARTESIAN_POINT('Ctrl Pts',(0.953419338835436,4.60588852381034,5.35330026413508));
#10571=CARTESIAN_POINT('Ctrl Pts',(0.980978626059207,4.60770589733042,5.33760169347744));
#10572=CARTESIAN_POINT('Ctrl Pts',(1.00811553775735,4.6095232708505,5.32125798199465));
#10573=CARTESIAN_POINT('Ctrl Pts',(1.06662620765758,4.6134417617717,5.28601883915663));
#10574=CARTESIAN_POINT('Ctrl Pts',(1.12340266514511,4.61736025269291,5.2476384125661));
#10575=CARTESIAN_POINT('Ctrl Pts',(1.17808737194234,4.62127874361412,5.20631272915261));
#10576=CARTESIAN_POINT('Ctrl Pts',(1.23268985867502,4.62519134296901,5.1650491801192));
#10577=CARTESIAN_POINT('Ctrl Pts',(1.28520644730769,4.6291039423239,5.12084945702431));
#10578=CARTESIAN_POINT('Ctrl Pts',(1.33530666907632,4.63301654167879,5.07395400069754));
#10579=CARTESIAN_POINT('Ctrl Pts',(1.38534809989083,4.63692454972768,5.02711357463857));
#10580=CARTESIAN_POINT('Ctrl Pts',(1.43297843794734,4.64083255777657,4.97758403233599));
#10581=CARTESIAN_POINT('Ctrl Pts',(1.4778999945136,4.64474056582545,4.9256462456019));
#10582=CARTESIAN_POINT('Ctrl Pts',(1.52279346860112,4.64864613080332,4.87374092750655));
#10583=CARTESIAN_POINT('Ctrl Pts',(1.56498119938352,4.65255169578119,4.81943072256503));
#10584=CARTESIAN_POINT('Ctrl Pts',(1.60420321923423,4.65645726075905,4.76303241645457));
#10585=CARTESIAN_POINT('Ctrl Pts',(1.64341416458766,4.66036172298472,4.70665003463588));
#10586=CARTESIAN_POINT('Ctrl Pts',(1.6796607807379,4.66426618521039,4.64818112563726));
#10587=CARTESIAN_POINT('Ctrl Pts',(1.71272528491316,4.66817064743605,4.58797306596677));
#10588=CARTESIAN_POINT('Ctrl Pts',(1.74579178703228,4.67207534559135,4.52776136818568));
#10589=CARTESIAN_POINT('Ctrl Pts',(1.77567556097397,4.67598004374665,4.46581074337491));
#10590=CARTESIAN_POINT('Ctrl Pts',(1.80220470312597,4.67988474190195,4.40249327508376));
#10591=CARTESIAN_POINT('Ctrl Pts',(1.82876207354774,4.68379359484191,4.33910843399309));
#10592=CARTESIAN_POINT('Ctrl Pts',(1.85195749827294,4.68770244778187,4.27435430137876));
#10593=CARTESIAN_POINT('Ctrl Pts',(1.87166757980066,4.69161130072183,4.20862211436267));
#10594=CARTESIAN_POINT('Ctrl Pts',(1.89138947567435,4.69552249665266,4.14285052706313));
#10595=CARTESIAN_POINT('Ctrl Pts',(1.90762175436047,4.69943369258349,4.07610019650604));
#10596=CARTESIAN_POINT('Ctrl Pts',(1.92029187621526,4.70334488851431,4.00877392279351));
#10597=CARTESIAN_POINT('Ctrl Pts',(1.93298380762609,4.70726281693342,3.94133175784042));
#10598=CARTESIAN_POINT('Ctrl Pts',(1.94210127926275,4.71118074535253,3.87331215822697));
#10599=CARTESIAN_POINT('Ctrl Pts',(1.94762356115872,4.71509867377163,3.80512355253726));
#10600=CARTESIAN_POINT('Ctrl Pts',(1.95018513944006,4.71691605298828,3.77349343030518));
#10601=CARTESIAN_POINT('Ctrl Pts',(1.951973883556,4.71873343220493,3.74182694727277));
#10602=CARTESIAN_POINT('Ctrl Pts',(1.95299152617942,4.72055081142158,3.71016467356757));
#10603=CARTESIAN_POINT('Ctrl Pts',(1.95365963993518,4.72174397690631,3.68937741474616));
#10604=CARTESIAN_POINT('Ctrl Pts',(1.95399588157958,4.72293714239104,3.66857943228896));
#10605=CARTESIAN_POINT('Ctrl Pts',(1.95399996239942,4.72413030787577,3.64777779982394));
#10606=CARTESIAN_POINT('Origin',(0.,0.,3.64739446828387));
#10607=CARTESIAN_POINT('',(1.95399938884984,5.5258696920781,3.64893990493632));
#10608=CARTESIAN_POINT('',(1.95399943981962,5.42413030787577,3.64887405762317));
#10609=CARTESIAN_POINT('',(1.954,4.33875158023511E-16,3.64739446828387));
#10610=CARTESIAN_POINT('Ctrl Pts',(1.95399938884984,5.5258696920781,3.64893990493632));
#10611=CARTESIAN_POINT('Ctrl Pts',(1.9539356881594,5.5212902068915,3.72948096754413));
#10612=CARTESIAN_POINT('Ctrl Pts',(1.94888837279949,5.51671072170489,3.80981306186041));
#10613=CARTESIAN_POINT('Ctrl Pts',(1.9389580842007,5.51213123651829,3.88938113674468));
#10614=CARTESIAN_POINT('Ctrl Pts',(1.92891637635983,5.50750036886043,3.96984197667887));
#10615=CARTESIAN_POINT('Ctrl Pts',(1.91388160449032,5.50286950120256,4.04952144814088));
#10616=CARTESIAN_POINT('Ctrl Pts',(1.89400709304294,5.4982386335447,4.12786624841569));
#10617=CARTESIAN_POINT('Ctrl Pts',(1.88182705946909,5.49540062045954,4.17587961972344));
#10618=CARTESIAN_POINT('Ctrl Pts',(1.8678302625667,5.49256260737438,4.22339212396168));
#10619=CARTESIAN_POINT('Ctrl Pts',(1.85206076918552,5.48972459428922,4.27028041871456));
#10620=CARTESIAN_POINT('Ctrl Pts',(1.83028813032353,5.48580620372998,4.33501819334256));
#10621=CARTESIAN_POINT('Ctrl Pts',(1.80507401469036,5.48188781317074,4.39874111135267));
#10622=CARTESIAN_POINT('Ctrl Pts',(1.77653259424178,5.47796942261151,4.4610577534311));
#10623=CARTESIAN_POINT('Ctrl Pts',(1.74803409982399,5.47405692527522,4.52328067185963));
#10624=CARTESIAN_POINT('Ctrl Pts',(1.71621843544014,5.47014442793892,4.58410106841738));
#10625=CARTESIAN_POINT('Ctrl Pts',(1.68124898529418,5.46623193060263,4.64314436130283));
#10626=CARTESIAN_POINT('Ctrl Pts',(1.64632058913066,5.4623240265212,4.70211833761915));
#10627=CARTESIAN_POINT('Ctrl Pts',(1.60824600996504,5.45841612243977,4.75931893258246));
#10628=CARTESIAN_POINT('Ctrl Pts',(1.56723518853597,5.45450821835834,4.81439483838433));
#10629=CARTESIAN_POINT('Ctrl Pts',(1.52625001755183,5.45060275849711,4.86943629665652));
#10630=CARTESIAN_POINT('Ctrl Pts',(1.48233254040991,5.44669729863589,4.92235530833293));
#10631=CARTESIAN_POINT('Ctrl Pts',(1.43573591095886,5.44279183877466,4.97282963983438));
#10632=CARTESIAN_POINT('Ctrl Pts',(1.3891524504077,5.43888748265443,5.02328970653972));
#10633=CARTESIAN_POINT('Ctrl Pts',(1.33989167411641,5.43498312653419,5.07130610346387));
#10634=CARTESIAN_POINT('Ctrl Pts',(1.2882457154627,5.43107877041396,5.11659117961697));
#10635=CARTESIAN_POINT('Ctrl Pts',(1.23659664695655,5.4271741791936,5.16187898260307));
#10636=CARTESIAN_POINT('Ctrl Pts',(1.18256248241879,5.42326958797323,5.20443481600125));
#10637=CARTESIAN_POINT('Ctrl Pts',(1.12646938739104,5.41936499675287,5.24401048952093));
#10638=CARTESIAN_POINT('Ctrl Pts',(1.07031661254359,5.41545625127252,5.28362826927595));
#10639=CARTESIAN_POINT('Ctrl Pts',(1.01210093814373,5.41154750579218,5.3202592773975));
#10640=CARTESIAN_POINT('Ctrl Pts',(0.952177706509464,5.40763876031183,5.35369854881183));
#10641=CARTESIAN_POINT('Ctrl Pts',(0.892218562522306,5.40372767229682,5.38715786058251));
#10642=CARTESIAN_POINT('Ctrl Pts',(0.830550266194682,5.39981658428181,5.41742141207676));
#10643=CARTESIAN_POINT('Ctrl Pts',(0.767550432646793,5.39590549626681,5.44433139910357));
#10644=CARTESIAN_POINT('Ctrl Pts',(0.704442145284472,5.39198767533855,5.47128771150261));
#10645=CARTESIAN_POINT('Ctrl Pts',(0.639998207402256,5.3880698544103,5.49487876839399));
#10646=CARTESIAN_POINT('Ctrl Pts',(0.574612917820234,5.38415203348204,5.51499613745054));
#10647=CARTESIAN_POINT('Ctrl Pts',(0.544266505187708,5.38233370689407,5.52433294679058));
#10648=CARTESIAN_POINT('Ctrl Pts',(0.51371748425252,5.3805153803061,5.53292222715602));
#10649=CARTESIAN_POINT('Ctrl Pts',(0.483005906313117,5.37869705371813,5.54075689911074));
#10650=CARTESIAN_POINT('Ctrl Pts',(0.416821913118872,5.3747785277876,5.55764075562745));
#10651=CARTESIAN_POINT('Ctrl Pts',(0.349620703532056,5.37086000185707,5.57108354879797));
#10652=CARTESIAN_POINT('Ctrl Pts',(0.281792968696771,5.36694147592654,5.5809685482697));
#10653=CARTESIAN_POINT('Ctrl Pts',(0.214067207838018,5.36302884120956,5.59083868637673));
#10654=CARTESIAN_POINT('Ctrl Pts',(0.145717273873277,5.35911620649259,5.59716157616641));
#10655=CARTESIAN_POINT('Ctrl Pts',(0.0771464480080062,5.35520357177562,
5.5998709535609));
#10656=CARTESIAN_POINT('Ctrl Pts',(0.00865608095150007,5.35129552801879,
5.60257715185882));
#10657=CARTESIAN_POINT('Ctrl Pts',(-0.0600541741936425,5.34738748426196,
5.60167823916572));
#10658=CARTESIAN_POINT('Ctrl Pts',(-0.128575292284244,5.34347944050513,
5.59715968343518));
#10659=CARTESIAN_POINT('Ctrl Pts',(-0.19705357853462,5.33957383962592,5.59264395220695));
#10660=CARTESIAN_POINT('Ctrl Pts',(-0.265342472663803,5.33566823874671,
5.58451309856255));
#10661=CARTESIAN_POINT('Ctrl Pts',(-0.333033891360969,5.3317626378675,5.572804665412));
#10662=CARTESIAN_POINT('Ctrl Pts',(-0.400706199678621,5.32785813960242,
5.56109953774101));
#10663=CARTESIAN_POINT('Ctrl Pts',(-0.467780883087573,5.32395364133734,
5.54581891941343));
#10664=CARTESIAN_POINT('Ctrl Pts',(-0.533857724051586,5.32004914307227,
5.52705186538326));
#10665=CARTESIAN_POINT('Ctrl Pts',(-0.599938559117321,5.31614440879465,
5.50828367695379));
#10666=CARTESIAN_POINT('Ctrl Pts',(-0.665020959650626,5.31223967451703,
5.48602877125568));
#10667=CARTESIAN_POINT('Ctrl Pts',(-0.728719356347817,5.30833494023941,
5.46042621088631));
#10668=CARTESIAN_POINT('Ctrl Pts',(-0.792485528538388,5.30442605130004,
5.43479640923221));
#10669=CARTESIAN_POINT('Ctrl Pts',(-0.85486430094833,5.30051716236068,5.40581202823352));
#10670=CARTESIAN_POINT('Ctrl Pts',(-0.915490550093738,5.29660827342131,
5.37366010621132));
#10671=CARTESIAN_POINT('Ctrl Pts',(-0.976153138378129,5.29269704150905,
5.34148891245156));
#10672=CARTESIAN_POINT('Ctrl Pts',(-1.03506069105742,5.28878580959679,5.30614665209339));
#10673=CARTESIAN_POINT('Ctrl Pts',(-1.09187558439369,5.28487457768452,5.26786468035349));
#10674=CARTESIAN_POINT('Ctrl Pts',(-1.14878826855107,5.28095661368921,5.22951681699203));
#10675=CARTESIAN_POINT('Ctrl Pts',(-1.2036007120852,5.27703864969391,5.18821943943032));
#10676=CARTESIAN_POINT('Ctrl Pts',(-1.25600768300803,5.2731206856986,5.14424472807101));
#10677=CARTESIAN_POINT('Ctrl Pts',(-1.28031277631211,5.27130362818142,5.1238503140496));
#10678=CARTESIAN_POINT('Ctrl Pts',(-1.30410099538044,5.26948657066424,5.10288056396188));
#10679=CARTESIAN_POINT('Ctrl Pts',(-1.32734469991678,5.26766951314705,5.08136519588009));
#10680=CARTESIAN_POINT('Ctrl Pts',(-1.37746993607036,5.26375101396759,5.03496713121941));
#10681=CARTESIAN_POINT('Ctrl Pts',(-1.42525856221547,5.25983251478813,4.98584591761483));
#10682=CARTESIAN_POINT('Ctrl Pts',(-1.4704003566331,5.25591401560867,4.93426617564761));
#10683=CARTESIAN_POINT('Ctrl Pts',(-1.51547428213325,5.25200140773904,4.88276398179951));
#10684=CARTESIAN_POINT('Ctrl Pts',(-1.55790895241811,5.24808879986942,4.82881096259533));
#10685=CARTESIAN_POINT('Ctrl Pts',(-1.59742967920943,5.24417619199979,4.7727097218821));
#10686=CARTESIAN_POINT('Ctrl Pts',(-1.63690403325636,5.24026817509747,4.71667430912061));
#10687=CARTESIAN_POINT('Ctrl Pts',(-1.67347095248102,5.23636015819515,4.65849608111685));
#10688=CARTESIAN_POINT('Ctrl Pts',(-1.70689606355721,5.23245214129283,4.59851056435885));
#10689=CARTESIAN_POINT('Ctrl Pts',(-1.74030028090185,5.22854656725617,4.53856254399932));
#10690=CARTESIAN_POINT('Ctrl Pts',(-1.77056634709308,5.22464099321951,4.47680990453237));
#10691=CARTESIAN_POINT('Ctrl Pts',(-1.79750412333859,5.22073541918285,4.41361566779532));
#10692=CARTESIAN_POINT('Ctrl Pts',(-1.82443429493401,5.21683094770654,4.3504392710631));
#10693=CARTESIAN_POINT('Ctrl Pts',(-1.84803784911865,5.21292647623023,4.28582253714577));
#10694=CARTESIAN_POINT('Ctrl Pts',(-1.86817217000141,5.20902200475392,4.22014986392169));
#10695=CARTESIAN_POINT('Ctrl Pts',(-1.88830770843132,5.20511729716942,4.15447321939029));
#10696=CARTESIAN_POINT('Ctrl Pts',(-1.90497345537371,5.20121258958491,4.08774097969491));
#10697=CARTESIAN_POINT('Ctrl Pts',(-1.91807673883904,5.19730788200041,4.02035240683005));
#10698=CARTESIAN_POINT('Ctrl Pts',(-1.93119396548151,5.19339901942455,3.95289212592253));
#10699=CARTESIAN_POINT('Ctrl Pts',(-1.94074106941275,5.18949015684868,3.8847746017087));
#10700=CARTESIAN_POINT('Ctrl Pts',(-1.94667676563993,5.18558129427282,3.81640798880124));
#10701=CARTESIAN_POINT('Ctrl Pts',(-1.95261601995247,5.18167008857389,3.7480003943078));
#10702=CARTESIAN_POINT('Ctrl Pts',(-1.95493954153139,5.17775888287496,3.67934390549862));
#10703=CARTESIAN_POINT('Ctrl Pts',(-1.95365819189621,5.17384767717603,3.6108476594378));
#10704=CARTESIAN_POINT('Ctrl Pts',(-1.95237463659777,5.16992973888634,3.54223350671894));
#10705=CARTESIAN_POINT('Ctrl Pts',(-1.94747386063335,5.16601180059666,3.4737806374872));
#10706=CARTESIAN_POINT('Ctrl Pts',(-1.93901859753382,5.16209386230697,3.40589316721499));
#10707=CARTESIAN_POINT('Ctrl Pts',(-1.93509670812356,5.16027656572998,3.37440424160542));
#10708=CARTESIAN_POINT('Ctrl Pts',(-1.93041080123305,5.15845926915298,3.34303681436157));
#10709=CARTESIAN_POINT('Ctrl Pts',(-1.92497081948355,5.15664197257598,3.31183025067891));
#10710=CARTESIAN_POINT('Ctrl Pts',(-1.91324106259502,5.15272349490011,3.24454226660473));
#10711=CARTESIAN_POINT('Ctrl Pts',(-1.89795575006275,5.14880501722424,3.17773696910645));
#10712=CARTESIAN_POINT('Ctrl Pts',(-1.87916855139228,5.14488653954837,3.11181855820364));
#10713=CARTESIAN_POINT('Ctrl Pts',(-1.86040960103854,5.14097395367151,3.04599926181934));
#10714=CARTESIAN_POINT('Ctrl Pts',(-1.83815934832929,5.13706136779465,2.98106467459702));
#10715=CARTESIAN_POINT('Ctrl Pts',(-1.81252265527332,5.13314878191779,2.91740979438929));
#10716=CARTESIAN_POINT('Ctrl Pts',(-1.78691604795421,5.12924078762491,2.85382961585903));
#10717=CARTESIAN_POINT('Ctrl Pts',(-1.75793107587758,5.12533279333203,2.7915266157593));
#10718=CARTESIAN_POINT('Ctrl Pts',(-1.72572214182345,5.12142479903915,2.7308798261639));
#10719=CARTESIAN_POINT('Ctrl Pts',(-1.69353334444491,5.11751924798183,2.67027095228239));
#10720=CARTESIAN_POINT('Ctrl Pts',(-1.65812481356218,5.11361369692452,2.61131666823852));
#10721=CARTESIAN_POINT('Ctrl Pts',(-1.61969806496519,5.10970814586721,2.55437380134841));
#10722=CARTESIAN_POINT('Ctrl Pts',(-1.58128216776611,5.10580369770541,2.4974470146558));
#10723=CARTESIAN_POINT('Ctrl Pts',(-1.53985001983799,5.10189924954361,2.44253092495088));
#10724=CARTESIAN_POINT('Ctrl Pts',(-1.49564689828911,5.09799480138181,2.3899540698402));
#10725=CARTESIAN_POINT('Ctrl Pts',(-1.45144110711249,5.09409011741261,2.3373740393739));
#10726=CARTESIAN_POINT('Ctrl Pts',(-1.40446432849758,5.09018543344342,2.28713389874032));
#10727=CARTESIAN_POINT('Ctrl Pts',(-1.35500144837191,5.08628074947422,2.23952832588608));
#10728=CARTESIAN_POINT('Ctrl Pts',(-1.30548593831245,5.08237191080844,2.19187209932667));
#10729=CARTESIAN_POINT('Ctrl Pts',(-1.25347940263471,5.07846307214267,2.14685637657934));
#10730=CARTESIAN_POINT('Ctrl Pts',(-1.1993021061283,5.07455423347689,2.10473752060035));
#10731=CARTESIAN_POINT('Ctrl Pts',(-1.14509233627885,5.07064305189135,2.06259341898994));
#10732=CARTESIAN_POINT('Ctrl Pts',(-1.08870961977551,5.06673187030581,2.02334992078389));
#10733=CARTESIAN_POINT('Ctrl Pts',(-1.03050337127767,5.06282068872027,1.98722013955048));
#10734=CARTESIAN_POINT('Ctrl Pts',(-0.972196929213085,5.05890277460612,
1.95102816616862));
#10735=CARTESIAN_POINT('Ctrl Pts',(-0.912061121091908,5.05498486049197,
1.91796084372819));
#10736=CARTESIAN_POINT('Ctrl Pts',(-0.850469321204268,5.05106694637782,
1.88818500557332));
#10737=CARTESIAN_POINT('Ctrl Pts',(-0.821897129951727,5.04924944158685,
1.87437211255805));
#10738=CARTESIAN_POINT('Ctrl Pts',(-0.793011879616013,5.04743193679587,
1.8612668600447));
#10739=CARTESIAN_POINT('Ctrl Pts',(-0.7638520361295,5.0456144320049,1.84888228681252));
#10740=CARTESIAN_POINT('Ctrl Pts',(-0.700984107837436,5.04169593494841,
1.82218144178747));
#10741=CARTESIAN_POINT('Ctrl Pts',(-0.636590155551062,5.03777743789193,
1.79872813327963));
#10742=CARTESIAN_POINT('Ctrl Pts',(-0.571038710239946,5.03385894083544,
1.77869684924341));
#10743=CARTESIAN_POINT('Ctrl Pts',(-0.505585822135277,5.02994633527565,
1.75869568242865));
#10744=CARTESIAN_POINT('Ctrl Pts',(-0.438979361448358,5.02603372971586,
1.74210647146396));
#10745=CARTESIAN_POINT('Ctrl Pts',(-0.37160793886445,5.02212112415607,1.72905572349115));
#10746=CARTESIAN_POINT('Ctrl Pts',(-0.30431557304831,5.01821310983003,1.71602028987437));
#10747=CARTESIAN_POINT('Ctrl Pts',(-0.236260508593127,5.01430509550399,
1.70651516594548));
#10748=CARTESIAN_POINT('Ctrl Pts',(-0.167844859934866,5.01039708117795,
1.70061659112545));
#10749=CARTESIAN_POINT('Ctrl Pts',(-0.099471980176605,5.00649150988179,
1.69472170370094));
#10750=CARTESIAN_POINT('Ctrl Pts',(-0.0307394522219087,5.00258593858563,
1.69242893512387));
#10751=CARTESIAN_POINT('Ctrl Pts',(0.0379436627796952,4.99868036728946,
1.69376290669022));
#10752=CARTESIAN_POINT('Ctrl Pts',(0.106607385407991,4.99477589871406,1.6950965016156));
#10753=CARTESIAN_POINT('Ctrl Pts',(0.175221231337193,4.99087143013866,1.70005479430132));
#10754=CARTESIAN_POINT('Ctrl Pts',(0.243376122230749,4.98696696156325,1.70861029692082));
#10755=CARTESIAN_POINT('Ctrl Pts',(0.311535131800966,4.98306225703642,1.71716631655895));
#10756=CARTESIAN_POINT('Ctrl Pts',(0.379234643660844,4.97915755250959,1.72931991390676));
#10757=CARTESIAN_POINT('Ctrl Pts',(0.44607249438087,4.97525284798276,1.74499195310554));
#10758=CARTESIAN_POINT('Ctrl Pts',(0.512981463455144,4.971343988682,1.76068066802959));
#10759=CARTESIAN_POINT('Ctrl Pts',(0.57902646198267,4.96743512938124,1.7798951836522));
#10760=CARTESIAN_POINT('Ctrl Pts',(0.643818279759381,4.96352627008048,1.802505847622));
#10761=CARTESIAN_POINT('Ctrl Pts',(0.708648934144848,4.95961506778574,1.82513006456099));
#10762=CARTESIAN_POINT('Ctrl Pts',(0.772224457656997,4.95570386549099,1.85115429490052));
#10763=CARTESIAN_POINT('Ctrl Pts',(0.834176119683657,4.95179266319625,1.88040091952668));
#10764=CARTESIAN_POINT('Ctrl Pts',(0.89623442027662,4.9478747284751,1.90969788692037));
#10765=CARTESIAN_POINT('Ctrl Pts',(0.956662847974734,4.94395679375395,1.94222808592337));
#10766=CARTESIAN_POINT('Ctrl Pts',(1.01511851568101,4.9400388590328,1.9777686422014));
#10767=CARTESIAN_POINT('Ctrl Pts',(1.04223300575413,4.93822153649981,1.9942540250258));
#10768=CARTESIAN_POINT('Ctrl Pts',(1.06892347732324,4.93640421396681,2.01138649999389));
#10769=CARTESIAN_POINT('Ctrl Pts',(1.09515809873353,4.93458689143382,2.02914086060109));
#10770=CARTESIAN_POINT('Ctrl Pts',(1.15152628047914,4.93068215939184,2.06728820070681));
#10771=CARTESIAN_POINT('Ctrl Pts',(1.20601427441916,4.92677742734985,2.10846238665927));
#10772=CARTESIAN_POINT('Ctrl Pts',(1.25827678983222,4.92287269530786,2.15245115157601));
#10773=CARTESIAN_POINT('Ctrl Pts',(1.3123737685588,4.91883090350855,2.19798396340301));
#10774=CARTESIAN_POINT('Ctrl Pts',(1.36408562775225,4.91478911170923,2.24653241326189));
#10775=CARTESIAN_POINT('Ctrl Pts',(1.41306090869165,4.91074731990991,2.29781124805345));
#10776=CARTESIAN_POINT('Ctrl Pts',(1.46024774346122,4.90685312352861,2.34721751705432));
#10777=CARTESIAN_POINT('Ctrl Pts',(1.50489402519352,4.90295892714731,2.39915781793867));
#10778=CARTESIAN_POINT('Ctrl Pts',(1.54671985078529,4.89906473076601,2.45333680502522));
#10779=CARTESIAN_POINT('Ctrl Pts',(1.58852053660532,4.89517287502489,2.50748322736618));
#10780=CARTESIAN_POINT('Ctrl Pts',(1.62750382633125,4.89128101928378,2.56386527560244));
#10781=CARTESIAN_POINT('Ctrl Pts',(1.66342951017411,4.88738916354266,2.62215387960144));
#10782=CARTESIAN_POINT('Ctrl Pts',(1.69934614678611,4.88349828789472,2.68042780467435));
#10783=CARTESIAN_POINT('Ctrl Pts',(1.73220644619769,4.87960741224677,2.74060691051942));
#10784=CARTESIAN_POINT('Ctrl Pts',(1.7618140741169,4.87571653659883,2.80233401586428));
#10785=CARTESIAN_POINT('Ctrl Pts',(1.79142458548153,4.87182528202395,2.86406713272549));
#10786=CARTESIAN_POINT('Ctrl Pts',(1.81778158504737,4.86793402744908,2.92734810008913));
#10787=CARTESIAN_POINT('Ctrl Pts',(1.84073598285911,4.8640427728742,2.99179776191044));
#10788=CARTESIAN_POINT('Ctrl Pts',(1.86371507458946,4.86014733215929,3.05631675749151));
#10789=CARTESIAN_POINT('Ctrl Pts',(1.88328409647504,4.85625189144437,3.12200648773898));
#10790=CARTESIAN_POINT('Ctrl Pts',(1.89934352177934,4.85235645072946,3.18847161390109));
#10791=CARTESIAN_POINT('Ctrl Pts',(1.91541329890123,4.8484584990348,3.25497958311947));
#10792=CARTESIAN_POINT('Ctrl Pts',(1.92796888898634,4.84456054734014,3.32226345550801));
#10793=CARTESIAN_POINT('Ctrl Pts',(1.9369622120323,4.84066259564547,3.38991944200186));
#10794=CARTESIAN_POINT('Ctrl Pts',(1.9459703877051,4.83675820641692,3.4576871635146));
#10795=CARTESIAN_POINT('Ctrl Pts',(1.9514045239227,4.83285381718836,3.52582773192098));
#10796=CARTESIAN_POINT('Ctrl Pts',(1.95326856711042,4.8289494279598,3.59393509362967));
#10797=CARTESIAN_POINT('Ctrl Pts',(1.95375867881703,4.82792284934794,3.61184251954123));
#10798=CARTESIAN_POINT('Ctrl Pts',(1.95400226243369,4.82689627073609,3.62974767089841));
#10799=CARTESIAN_POINT('Ctrl Pts',(1.95399998416515,4.82586969212423,3.6476432303685));
#10800=CARTESIAN_POINT('Ctrl Pts',(1.95710318190607,4.72413079030316,3.64776998461591));
#10801=CARTESIAN_POINT('Ctrl Pts',(1.95541360145849,4.75994664419965,3.02236479651099));
#10802=CARTESIAN_POINT('Ctrl Pts',(1.29210840943673,4.83277167828651,1.74764265246944));
#10803=CARTESIAN_POINT('Ctrl Pts',(-0.878268351030347,4.94260589256373,
1.51220654580568));
#10804=CARTESIAN_POINT('Ctrl Pts',(-2.26979830067417,5.05363343313481,3.22502187308484));
#10805=CARTESIAN_POINT('Ctrl Pts',(-1.5875322833648,5.16466097370589,5.3237364314922));
#10806=CARTESIAN_POINT('Ctrl Pts',(0.545177970067398,5.27568851427696,5.89086615319871));
#10807=CARTESIAN_POINT('Ctrl Pts',(1.81852615233383,5.36217802636004,4.735922224886));
#10808=CARTESIAN_POINT('Ctrl Pts',(1.95368429139157,5.41165835825274,3.86808546352169));
#10809=CARTESIAN_POINT('Ctrl Pts',(1.95213885961564,5.42412950995508,3.64888667332462));
#10810=CARTESIAN_POINT('Origin',(0.,0.,3.64739446828387));
#10811=CARTESIAN_POINT('',(1.95353597714873,6.22586985342116,3.64632535240867));
#10812=CARTESIAN_POINT('',(1.95399955699052,6.12413030792733,3.64607868681972));
#10813=CARTESIAN_POINT('',(1.954,4.33875158023511E-16,3.64739446828387));
#10814=CARTESIAN_POINT('Ctrl Pts',(1.95399970893239,6.22586969212423,3.64632793551614));
#10815=CARTESIAN_POINT('Ctrl Pts',(1.95403757522787,6.22192922025797,3.71570295389059));
#10816=CARTESIAN_POINT('Ctrl Pts',(1.95037645685081,6.21798874839172,3.78509205096178));
#10817=CARTESIAN_POINT('Ctrl Pts',(1.94303829200873,6.21404827652546,3.8540782745866));
#10818=CARTESIAN_POINT('Ctrl Pts',(1.93569906479725,6.21010723418459,3.92307448556584));
#10819=CARTESIAN_POINT('Ctrl Pts',(1.92468178589055,6.20616619184372,3.99166723064893));
#10820=CARTESIAN_POINT('Ctrl Pts',(1.91006015343091,6.20222514950286,4.05944569116215));
#10821=CARTESIAN_POINT('Ctrl Pts',(1.89541999607838,6.19827911405418,4.12731002366842));
#10822=CARTESIAN_POINT('Ctrl Pts',(1.8771664669629,6.1943330786055,4.19435754146491));
#10823=CARTESIAN_POINT('Ctrl Pts',(1.85542408294095,6.19038704315682,4.26018927280064));
#10824=CARTESIAN_POINT('Ctrl Pts',(1.83366809728879,6.18643853914191,4.32606218724052));
#10825=CARTESIAN_POINT('Ctrl Pts',(1.80841908414587,6.182490035127,4.39071735315611));
#10826=CARTESIAN_POINT('Ctrl Pts',(1.77984999050241,6.17854153111209,4.45377527863874));
#10827=CARTESIAN_POINT('Ctrl Pts',(1.75122193840221,6.17458487851165,4.51696333768521));
#10828=CARTESIAN_POINT('Ctrl Pts',(1.71926033568422,6.17062822591121,4.57854714271363));
#10829=CARTESIAN_POINT('Ctrl Pts',(1.68418427929645,6.16667157331077,4.63817159426665));
#10830=CARTESIAN_POINT('Ctrl Pts',(1.65232394988155,6.16307766144574,4.69232975408544));
#10831=CARTESIAN_POINT('Ctrl Pts',(1.61789476739731,6.15948374958072,4.74487148430728));
#10832=CARTESIAN_POINT('Ctrl Pts',(1.58109015814158,6.15588983771569,4.79555382648631));
#10833=CARTESIAN_POINT('Ctrl Pts',(1.54101347268038,6.15197641278597,4.85074203054611));
#10834=CARTESIAN_POINT('Ctrl Pts',(1.49796252247796,6.14806298785625,4.90394126259874));
#10835=CARTESIAN_POINT('Ctrl Pts',(1.45216195437618,6.14414956292653,4.95481240385855));
#10836=CARTESIAN_POINT('Ctrl Pts',(1.40643121462749,6.14024210447341,5.00560598608009));
#10837=CARTESIAN_POINT('Ctrl Pts',(1.35795950337589,6.13633464602028,5.05407815776852));
#10838=CARTESIAN_POINT('Ctrl Pts',(1.30701347514832,6.13242718756716,5.09992046659878));
#10839=CARTESIAN_POINT('Ctrl Pts',(1.2561284283943,6.12852440627108,5.1457079030152));
#10840=CARTESIAN_POINT('Ctrl Pts',(1.20277531117035,6.12462162497499,5.18887139966879));
#10841=CARTESIAN_POINT('Ctrl Pts',(1.14725832432907,6.12071884367891,5.22913854911921));
#10842=CARTESIAN_POINT('Ctrl Pts',(1.09177680681312,6.11681855583622,5.26937997223424));
#10843=CARTESIAN_POINT('Ctrl Pts',(1.03413456015336,6.11291826799353,5.30672842959029));
#10844=CARTESIAN_POINT('Ctrl Pts',(0.974668408497103,6.10901798015085,5.34095211226229));
#10845=CARTESIAN_POINT('Ctrl Pts',(0.915219717759489,6.10511883754132,5.3751657459077));
#10846=CARTESIAN_POINT('Ctrl Pts',(0.853948612355341,6.10121969493179,5.40625618021199));
#10847=CARTESIAN_POINT('Ctrl Pts',(0.791218844617371,6.09732055232226,5.4340362174665));
#10848=CARTESIAN_POINT('Ctrl Pts',(0.728485838336562,6.09342120841212,5.46181768891794));
#10849=CARTESIAN_POINT('Ctrl Pts',(0.664294472261032,6.08952186450199,5.48628822667285));
#10850=CARTESIAN_POINT('Ctrl Pts',(0.599029234793864,6.08562252059185,5.5073084383003));
#10851=CARTESIAN_POINT('Ctrl Pts',(0.533694725717585,6.08171903797269,5.52835096048602));
#10852=CARTESIAN_POINT('Ctrl Pts',(0.467284540993296,6.07781555535353,5.54593569663892));
#10853=CARTESIAN_POINT('Ctrl Pts',(0.400198132892293,6.07391207273437,5.55997321291885));
#10854=CARTESIAN_POINT('Ctrl Pts',(0.333071752208107,6.07000626427473,5.57401909327436));
#10855=CARTESIAN_POINT('Ctrl Pts',(0.265268833825228,6.06610045581509,5.58451347230028));
#10856=CARTESIAN_POINT('Ctrl Pts',(0.197196009186804,6.06219464735545,5.59141857666339));
#10857=CARTESIAN_POINT('Ctrl Pts',(0.129005325724356,6.05828207652045,5.5983356362742));
#10858=CARTESIAN_POINT('Ctrl Pts',(0.0605442957417832,6.05436950568546,
5.60165099501346));
#10859=CARTESIAN_POINT('Ctrl Pts',(-0.00777927282300132,6.05045693485046,
5.60137898278606));
#10860=CARTESIAN_POINT('Ctrl Pts',(-0.0403448696313994,6.04859205561518,
5.60124933147084));
#10861=CARTESIAN_POINT('Ctrl Pts',(-0.0728792977296982,6.04672717637989,
5.60030545174067));
#10862=CARTESIAN_POINT('Ctrl Pts',(-0.105338970147305,6.04486229714461,
5.59855302190485));
#10863=CARTESIAN_POINT('Ctrl Pts',(-0.173561813075235,6.04094274547719,
5.59486981327928));
#10864=CARTESIAN_POINT('Ctrl Pts',(-0.241725674141963,6.03702319380978,
5.58759689429551));
#10865=CARTESIAN_POINT('Ctrl Pts',(-0.309422647205287,6.03310364214236,
5.57673985607644));
#10866=CARTESIAN_POINT('Ctrl Pts',(-0.377017944907859,6.02918997732352,
5.56589912424787));
#10867=CARTESIAN_POINT('Ctrl Pts',(-0.44414726494164,6.02527631250469,5.55148503414066));
#10868=CARTESIAN_POINT('Ctrl Pts',(-0.510405798910999,6.02136264768585,
5.53355509782687));
#10869=CARTESIAN_POINT('Ctrl Pts',(-0.576586629003742,6.01745357256905,
5.51564618862423));
#10870=CARTESIAN_POINT('Ctrl Pts',(-0.641898229039365,6.01354449745225,
5.49422974987089));
#10871=CARTESIAN_POINT('Ctrl Pts',(-0.705945795963749,6.00963542233545,
5.46941437299433));
#10872=CARTESIAN_POINT('Ctrl Pts',(-0.769953340349426,6.00572878995172,
5.4446145029423));
#10873=CARTESIAN_POINT('Ctrl Pts',(-0.832697961298485,6.001822157568,5.41642008531667));
#10874=CARTESIAN_POINT('Ctrl Pts',(-0.893801338936124,5.99791552518427,
5.38498911794069));
#10875=CARTESIAN_POINT('Ctrl Pts',(-0.954887447690772,5.99400999688317,
5.3535670335057));
#10876=CARTESIAN_POINT('Ctrl Pts',(-1.01433279715199,5.99010446858207,5.31891043993488));
#10877=CARTESIAN_POINT('Ctrl Pts',(-1.07178198514885,5.98619894028097,5.28122413391931));
#10878=CARTESIAN_POINT('Ctrl Pts',(-1.12923459948064,5.98229317904972,5.24353558024957));
#10879=CARTESIAN_POINT('Ctrl Pts',(-1.18469040646407,5.97838741781847,5.20281722710281));
#10880=CARTESIAN_POINT('Ctrl Pts',(-1.23782293994499,5.97448165658721,5.15931720749575));
#10881=CARTESIAN_POINT('Ctrl Pts',(-1.29101183163741,5.97057175247583,5.11577104698133));
#10882=CARTESIAN_POINT('Ctrl Pts',(-1.34187215084897,5.96666184836444,5.06943764360133));
#10883=CARTESIAN_POINT('Ctrl Pts',(-1.39011129021989,5.96275194425305,5.02060479478276));
#10884=CARTESIAN_POINT('Ctrl Pts',(-1.4383792714137,5.95883970243906,4.97174274916685));
#10885=CARTESIAN_POINT('Ctrl Pts',(-1.48402262717635,5.95492746062506,4.920378651296));
#10886=CARTESIAN_POINT('Ctrl Pts',(-1.52678824140386,5.95101521881107,4.86683436672533));
#10887=CARTESIAN_POINT('Ctrl Pts',(-1.56962724054416,5.94709626367074,4.81319820126567));
#10888=CARTESIAN_POINT('Ctrl Pts',(-1.60957835661129,5.94317730853041,4.75737478184416));
#10889=CARTESIAN_POINT('Ctrl Pts',(-1.64643158878374,5.93925835339007,4.69971524801554));
#10890=CARTESIAN_POINT('Ctrl Pts',(-1.66343247001633,5.93745048778456,4.67311614588089));
#10891=CARTESIAN_POINT('Ctrl Pts',(-1.67977473443788,5.93564262217904,4.64612664650909));
#10892=CARTESIAN_POINT('Ctrl Pts',(-1.69544115163435,5.93383475657353,4.61878280532771));
#10893=CARTESIAN_POINT('Ctrl Pts',(-1.72940432509507,5.9299154907718,4.55950418345271));
#10894=CARTESIAN_POINT('Ctrl Pts',(-1.76032172067742,5.92599622497007,4.49832553361439));
#10895=CARTESIAN_POINT('Ctrl Pts',(-1.78797652885598,5.92207695916834,4.43559236999391));
#10896=CARTESIAN_POINT('Ctrl Pts',(-1.81558989213884,5.91816356697678,4.37295322146865));
#10897=CARTESIAN_POINT('Ctrl Pts',(-1.83995017544407,5.91425017478521,4.30876462905162));
#10898=CARTESIAN_POINT('Ctrl Pts',(-1.86088584978545,5.91033678259365,4.24339770155386));
#10899=CARTESIAN_POINT('Ctrl Pts',(-1.88179708321254,5.90642795900979,4.17810708530581));
#10900=CARTESIAN_POINT('Ctrl Pts',(-1.8992914986264,5.90251913542594,4.11164133195107));
#10901=CARTESIAN_POINT('Ctrl Pts',(-1.91324589168175,5.89861031184208,4.04439088887596));
#10902=CARTESIAN_POINT('Ctrl Pts',(-1.9271916116718,5.89470391770693,3.97718224392716));
#10903=CARTESIAN_POINT('Ctrl Pts',(-1.93760157433051,5.89079752357178,3.90919035696625));
#10904=CARTESIAN_POINT('Ctrl Pts',(-1.94440301405618,5.88689112943662,3.84081866255448));
#10905=CARTESIAN_POINT('Ctrl Pts',(-1.9512025553041,5.8829858256886,3.77246605265214));
#10906=CARTESIAN_POINT('Ctrl Pts',(-1.95439552460935,5.87908052194059,3.7037343346659));
#10907=CARTESIAN_POINT('Ctrl Pts',(-1.95396089951249,5.87517521819256,3.6350331100915));
#10908=CARTESIAN_POINT('Ctrl Pts',(-1.95352624692107,5.87126966739347,3.5663275394502));
#10909=CARTESIAN_POINT('Ctrl Pts',(-1.94946355000495,5.86736411659438,3.49765295755817));
#10910=CARTESIAN_POINT('Ctrl Pts',(-1.94180388956302,5.86345856579528,3.42941819783696));
#10911=CARTESIAN_POINT('Ctrl Pts',(-1.93413605902316,5.85954884918065,3.36111065621202));
#10912=CARTESIAN_POINT('Ctrl Pts',(-1.92286366321737,5.85563913256602,3.29324436238369));
#10913=CARTESIAN_POINT('Ctrl Pts',(-1.90806947589916,5.85172941595138,3.2262212555294));
#10914=CARTESIAN_POINT('Ctrl Pts',(-1.89326639420659,5.84781734878633,3.15915785388972));
#10915=CARTESIAN_POINT('Ctrl Pts',(-1.87493743823184,5.84390528162128,3.09293912189492));
#10916=CARTESIAN_POINT('Ctrl Pts',(-1.85321543256441,5.83999321445623,3.0279523317569));
#10917=CARTESIAN_POINT('Ctrl Pts',(-1.83145603003673,5.83607441223037,2.96285365959719));
#10918=CARTESIAN_POINT('Ctrl Pts',(-1.80629209935227,5.83215561000451,2.8989916193083));
#10919=CARTESIAN_POINT('Ctrl Pts',(-1.77790445793065,5.82823680777865,2.83673317127362));
#10920=CARTESIAN_POINT('Ctrl Pts',(-1.76479387842829,5.82642694385325,2.80797966123279));
#10921=CARTESIAN_POINT('Ctrl Pts',(-1.75099633135699,5.82461707992785,2.77956783987734));
#10922=CARTESIAN_POINT('Ctrl Pts',(-1.73653280861798,5.82280721600245,2.75153186464793));
#10923=CARTESIAN_POINT('Ctrl Pts',(-1.7052239763555,5.81888944803674,2.69084307799399));
#10924=CARTESIAN_POINT('Ctrl Pts',(-1.67066771919403,5.81497168007103,2.63167709240382));
#10925=CARTESIAN_POINT('Ctrl Pts',(-1.63303593841815,5.81105391210532,2.57440349728982));
#10926=CARTESIAN_POINT('Ctrl Pts',(-1.59546085757294,5.80714204705379,2.51721619649422));
#10927=CARTESIAN_POINT('Ctrl Pts',(-1.55481971769915,5.80323018200225,2.46191603529419));
#10928=CARTESIAN_POINT('Ctrl Pts',(-1.51133052729588,5.79931831695071,2.40884853160507));
#10929=CARTESIAN_POINT('Ctrl Pts',(-1.46789252609841,5.7954110563828,2.3558434913314));
#10930=CARTESIAN_POINT('Ctrl Pts',(-1.42161344246657,5.79150379581489,2.30506626812456));
#10931=CARTESIAN_POINT('Ctrl Pts',(-1.37275379361176,5.78759653524699,2.25683234377287));
#10932=CARTESIAN_POINT('Ctrl Pts',(-1.32392479182163,5.78369172549627,2.2086286740021));
#10933=CARTESIAN_POINT('Ctrl Pts',(-1.27251878501446,5.77978691574555,2.16296548343151));
#10934=CARTESIAN_POINT('Ctrl Pts',(-1.2188346174519,5.77588210599483,2.12012298773404));
#10935=CARTESIAN_POINT('Ctrl Pts',(-1.16516570144289,5.77197840559195,2.07729266349505));
#10936=CARTESIAN_POINT('Ctrl Pts',(-1.10922029387599,5.76807470518906,2.03728175003944));
#10937=CARTESIAN_POINT('Ctrl Pts',(-1.05133054742944,5.76417100478618,2.00033038937203));
#10938=CARTESIAN_POINT('Ctrl Pts',(-0.993437383134554,5.76026707390628,
1.96337684707222));
#10939=CARTESIAN_POINT('Ctrl Pts',(-0.933600068135027,5.75636314302639,
1.92948347871644));
#10940=CARTESIAN_POINT('Ctrl Pts',(-0.872178434039136,5.75245921214649,
1.89884627644098));
#10941=CARTESIAN_POINT('Ctrl Pts',(-0.810691478933431,5.74855112949318,
1.86817649194885));
#10942=CARTESIAN_POINT('Ctrl Pts',(-0.747617283319028,5.74464304683987,
1.8407700043208));
#10943=CARTESIAN_POINT('Ctrl Pts',(-0.683337987343935,5.74073496418656,
1.8167756671533));
#10944=CARTESIAN_POINT('Ctrl Pts',(-0.619020201144726,5.73682454138663,
1.79276696225819));
#10945=CARTESIAN_POINT('Ctrl Pts',(-0.553496347862654,5.7329141185867,1.7721746216137));
#10946=CARTESIAN_POINT('Ctrl Pts',(-0.487163454161461,5.72900369578677,
1.75509751248399));
#10947=CARTESIAN_POINT('Ctrl Pts',(-0.420716293815641,5.72508653679809,
1.73799098591369));
#10948=CARTESIAN_POINT('Ctrl Pts',(-0.353457793522332,5.72116937780941,
1.7244118735935));
#10949=CARTESIAN_POINT('Ctrl Pts',(-0.285794006257928,5.71725221882073,
1.71440771561663));
#10950=CARTESIAN_POINT('Ctrl Pts',(-0.254283668215943,5.71542803769094,
1.70974888092201));
#10951=CARTESIAN_POINT('Ctrl Pts',(-0.222685489647666,5.71360385656116,
1.70586459717763));
#10952=CARTESIAN_POINT('Ctrl Pts',(-0.191040535300942,5.71177967543137,
1.70275580933668));
#10953=CARTESIAN_POINT('Ctrl Pts',(-0.1230611042813,5.70786098451083,1.69607753683001));
#10954=CARTESIAN_POINT('Ctrl Pts',(-0.0545967376771535,5.70394229359028,
1.69295492978579));
#10955=CARTESIAN_POINT('Ctrl Pts',(0.0139486777056309,5.70002360266974,
1.69344425540989));
#10956=CARTESIAN_POINT('Ctrl Pts',(0.0823910661357122,5.69611080172421,
1.69393284555478));
#10957=CARTESIAN_POINT('Ctrl Pts',(0.150913773809587,5.69219800077868,1.69802259030236));
#10958=CARTESIAN_POINT('Ctrl Pts',(0.219108106246929,5.68828519983315,1.70571796644921));
#10959=CARTESIAN_POINT('Ctrl Pts',(0.287222442472813,5.68437698884753,1.71340431543918));
#10960=CARTESIAN_POINT('Ctrl Pts',(0.355008682185071,5.68046877786191,1.72468784075316));
#10961=CARTESIAN_POINT('Ctrl Pts',(0.42206028141137,5.67656056687629,1.73952101366091));
#10962=CARTESIAN_POINT('Ctrl Pts',(0.489069978092514,5.67265479824833,1.75434491687629));
#10963=CARTESIAN_POINT('Ctrl Pts',(0.555345465977129,5.66874902962038,1.77271396128303));
#10964=CARTESIAN_POINT('Ctrl Pts',(0.620489011696533,5.66484326099242,1.79452928528651));
#10965=CARTESIAN_POINT('Ctrl Pts',(0.685614171468399,5.6609385947186,1.81633845218879));
#10966=CARTESIAN_POINT('Ctrl Pts',(0.749607557262514,5.65703392844478,1.84159181166391));
#10967=CARTESIAN_POINT('Ctrl Pts',(0.812087004737327,5.65312926217096,1.87014077318664));
#10968=CARTESIAN_POINT('Ctrl Pts',(0.874570228709034,5.64922435988417,1.89869146031786));
#10969=CARTESIAN_POINT('Ctrl Pts',(0.93553888652736,5.64531945759738,1.93053793828093));
#10970=CARTESIAN_POINT('Ctrl Pts',(0.99463285904909,5.64141455531059,1.96548440062275));
#10971=CARTESIAN_POINT('Ctrl Pts',(1.05378968769378,5.63750549952036,2.00046803425363));
#10972=CARTESIAN_POINT('Ctrl Pts',(1.11106742756554,5.63359644373013,2.03855798189388));
#10973=CARTESIAN_POINT('Ctrl Pts',(1.16613342782562,5.62968738793989,2.07951410661476));
#10974=CARTESIAN_POINT('Ctrl Pts',(1.22123242710567,5.62577598959692,2.12049477482838));
#10975=CARTESIAN_POINT('Ctrl Pts',(1.27411667037651,5.62186459125394,2.16434472458715));
#10976=CARTESIAN_POINT('Ctrl Pts',(1.32448739361204,5.61795319291096,2.21078417173063));
#10977=CARTESIAN_POINT('Ctrl Pts',(1.37494478129112,5.61403506488178,2.25730351943117));
#10978=CARTESIAN_POINT('Ctrl Pts',(1.42287967463537,5.61011693685261,2.30642090478317));
#10979=CARTESIAN_POINT('Ctrl Pts',(1.46803150387258,5.60619880882343,2.35782108780581));
#10980=CARTESIAN_POINT('Ctrl Pts',(1.4889536798763,5.60438325083572,2.38163858742855));
#10981=CARTESIAN_POINT('Ctrl Pts',(1.50927887683722,5.602567692848,2.4059457964163));
#10982=CARTESIAN_POINT('Ctrl Pts',(1.5289843240469,5.60075213486029,2.43070924324872));
#10983=CARTESIAN_POINT('Ctrl Pts',(1.571427375016,5.59684165166293,2.48404658824245));
#10984=CARTESIAN_POINT('Ctrl Pts',(1.61116405275229,5.59293116846557,2.5397180074941));
#10985=CARTESIAN_POINT('Ctrl Pts',(1.6479272127628,5.58902068526822,2.59741737261186));
#10986=CARTESIAN_POINT('Ctrl Pts',(1.68463680664051,5.58511589987981,2.65503266628818));
#10987=CARTESIAN_POINT('Ctrl Pts',(1.71838121312421,5.58121111449141,2.71466963328221));
#10988=CARTESIAN_POINT('Ctrl Pts',(1.74893386808947,5.577306329103,2.7759896685211));
#10989=CARTESIAN_POINT('Ctrl Pts',(1.77945257014948,5.57340588306934,2.83724155932709));
#10990=CARTESIAN_POINT('Ctrl Pts',(1.80678633979274,5.56950543703568,2.90017236789852));
#10991=CARTESIAN_POINT('Ctrl Pts',(1.83075322221469,5.56560499100202,2.9644166945968));
#10992=CARTESIAN_POINT('Ctrl Pts',(1.85470355842854,5.56170723775045,3.028616668426));
#10993=CARTESIAN_POINT('Ctrl Pts',(1.87529144678653,5.55780948449888,3.09412790017339));
#10994=CARTESIAN_POINT('Ctrl Pts',(1.89238272508226,5.55391173124731,3.160564290696));
#10995=CARTESIAN_POINT('Ctrl Pts',(1.90946718207926,5.55001553362773,3.22697416579603));
#10996=CARTESIAN_POINT('Ctrl Pts',(1.92305768028705,5.54611933600815,3.29430798817317));
#10997=CARTESIAN_POINT('Ctrl Pts',(1.93307022193307,5.54222313838858,3.3621655828679));
#10998=CARTESIAN_POINT('Ctrl Pts',(1.94308489345346,5.53832611196731,3.43003761227433));
#10999=CARTESIAN_POINT('Ctrl Pts',(1.94952001575387,5.53442908554603,3.49843314825239));
#11000=CARTESIAN_POINT('Ctrl Pts',(1.95234315435092,5.53053205912476,3.56694443621978));
#11001=CARTESIAN_POINT('Ctrl Pts',(1.95346901347271,5.52897793679125,3.59426653035457));
#11002=CARTESIAN_POINT('Ctrl Pts',(1.95402100669827,5.52742381445774,3.62160699244058));
#11003=CARTESIAN_POINT('Ctrl Pts',(1.95399938885048,5.52586969212423,3.64893990412503));
#11004=CARTESIAN_POINT('Ctrl Pts',(1.95399943981962,5.42413030787577,3.64887405762317));
#11005=CARTESIAN_POINT('Ctrl Pts',(1.9540514551376,5.42803486416929,3.58018073880955));
#11006=CARTESIAN_POINT('Ctrl Pts',(1.95047675797586,5.4319394204628,3.51144725141444));
#11007=CARTESIAN_POINT('Ctrl Pts',(1.94328925495969,5.43584397675632,3.44308374522165));
#11008=CARTESIAN_POINT('Ctrl Pts',(1.93610276751857,5.43974798134642,3.37472989861037));
#11009=CARTESIAN_POINT('Ctrl Pts',(1.92530453973603,5.44365198593652,3.30674641766519));
#11010=CARTESIAN_POINT('Ctrl Pts',(1.91096035466864,5.44755599052662,3.23953846074605));
#11011=CARTESIAN_POINT('Ctrl Pts',(1.89661329756237,5.45146077678908,3.17231704723357));
#11012=CARTESIAN_POINT('Ctrl Pts',(1.87871897897927,5.45536556305154,3.10587194559488));
#11013=CARTESIAN_POINT('Ctrl Pts',(1.85739392663886,5.459270349314,3.04059647777544));
#11014=CARTESIAN_POINT('Ctrl Pts',(1.83604304214031,5.46317986564955,2.97524193834669));
#11015=CARTESIAN_POINT('Ctrl Pts',(1.81125328691822,5.46708938198511,2.91106032641277));
#11016=CARTESIAN_POINT('Ctrl Pts',(1.78319022584856,5.47099889832066,2.84842724840677));
#11017=CARTESIAN_POINT('Ctrl Pts',(1.7551069686539,5.4749112282153,2.78574909529402));
#11018=CARTESIAN_POINT('Ctrl Pts',(1.72374594392167,5.47882355810995,2.72462212920007));
#11019=CARTESIAN_POINT('Ctrl Pts',(1.68931847990919,5.48273588800459,2.66539697672022));
#11020=CARTESIAN_POINT('Ctrl Pts',(1.65483066125898,5.48665507658779,2.60606799688262));
#11021=CARTESIAN_POINT('Ctrl Pts',(1.61726594887417,5.490574265171,2.54864789067694));
#11022=CARTESIAN_POINT('Ctrl Pts',(1.57687814704101,5.4944934537542,2.49345716089473));
#11023=CARTESIAN_POINT('Ctrl Pts',(1.56571375465843,5.49557683430917,2.47820079795339));
#11024=CARTESIAN_POINT('Ctrl Pts',(1.55433386759307,5.49666021486415,2.46311458302517));
#11025=CARTESIAN_POINT('Ctrl Pts',(1.54274435158161,5.49774359541912,2.44820479785512));
#11026=CARTESIAN_POINT('Ctrl Pts',(1.50082572987124,5.5016621214048,2.39427695102281));
#11027=CARTESIAN_POINT('Ctrl Pts',(1.45599318072079,5.50558064739048,2.34244306268919));
#11028=CARTESIAN_POINT('Ctrl Pts',(1.40848368839703,5.50949917337616,2.29303495193694));
#11029=CARTESIAN_POINT('Ctrl Pts',(1.36104562422435,5.51341180805355,2.24370112381383));
#11030=CARTESIAN_POINT('Ctrl Pts',(1.31093894257671,5.51732444273093,2.19678618675944));
#11031=CARTESIAN_POINT('Ctrl Pts',(1.25844152415245,5.52123707740832,2.15258982208797));
#11032=CARTESIAN_POINT('Ctrl Pts',(1.20600570638572,5.52514512098626,2.10844531758802));
#11033=CARTESIAN_POINT('Ctrl Pts',(1.1511850976712,5.5290531645642,2.06701336528422));
#11034=CARTESIAN_POINT('Ctrl Pts',(1.09429384419979,5.53296120814213,2.02855631005234));
#11035=CARTESIAN_POINT('Ctrl Pts',(1.03743815411931,5.53686680875612,1.9901232947775));
#11036=CARTESIAN_POINT('Ctrl Pts',(0.978514793457789,5.5407724093701,1.95466176237224));
#11037=CARTESIAN_POINT('Ctrl Pts',(0.917869103633709,5.54467800998409,1.92239234985194));
#11038=CARTESIAN_POINT('Ctrl Pts',(0.857240536397379,5.54858250789828,1.89013204821568));
#11039=CARTESIAN_POINT('Ctrl Pts',(0.794891039285684,5.55248700581248,1.86106230817246));
#11040=CARTESIAN_POINT('Ctrl Pts',(0.731191334976556,5.55639150372668,1.83535825682031));
#11041=CARTESIAN_POINT('Ctrl Pts',(0.667487781642525,5.56029623756834,1.80965265231286));
#11042=CARTESIAN_POINT('Ctrl Pts',(0.602434316124245,5.56420097141,1.78731332188365));
#11043=CARTESIAN_POINT('Ctrl Pts',(0.536420762696227,5.56810570525167,1.76846691104586));
#11044=CARTESIAN_POINT('Ctrl Pts',(0.47033697254014,5.57201459363001,1.74960044811022));
#11045=CARTESIAN_POINT('Ctrl Pts',(0.403291529646144,5.57592348200835,1.73423445667258));
#11046=CARTESIAN_POINT('Ctrl Pts',(0.335687534544171,5.57983237038669,1.72244514969087));
#11047=CARTESIAN_POINT('Ctrl Pts',(0.268043019113123,5.58374360166567,1.71064877646112));
#11048=CARTESIAN_POINT('Ctrl Pts',(0.199839773474815,5.58765483294465,1.70243341304384));
#11049=CARTESIAN_POINT('Ctrl Pts',(0.131486358980064,5.59156606422363,1.69782340330517));
#11050=CARTESIAN_POINT('Ctrl Pts',(0.0630152951561597,5.5954840274814,1.69320545885605));
#11051=CARTESIAN_POINT('Ctrl Pts',(-0.00560596196028167,5.59940199073916,
1.69220526025078));
#11052=CARTESIAN_POINT('Ctrl Pts',(-0.0739693956144667,5.60331995399692,
1.69479503969837));
#11053=CARTESIAN_POINT('Ctrl Pts',(-0.105674773640132,5.60513701466135,
1.69599611945695));
#11054=CARTESIAN_POINT('Ctrl Pts',(-0.137324779937373,5.60695407532578,
1.69796863240154));
#11055=CARTESIAN_POINT('Ctrl Pts',(-0.168879356249839,5.6087711359902,1.70070605895056));
#11056=CARTESIAN_POINT('Ctrl Pts',(-0.236924946485957,5.6126895205751,1.70660915850138));
#11057=CARTESIAN_POINT('Ctrl Pts',(-0.304795263666282,5.61660790515999,
1.71609598339349));
#11058=CARTESIAN_POINT('Ctrl Pts',(-0.37208300607575,5.62052628974489,1.72914781141473));
#11059=CARTESIAN_POINT('Ctrl Pts',(-0.439269574640891,5.62443878264702,
1.74218001470835));
#11060=CARTESIAN_POINT('Ctrl Pts',(-0.505874827988365,5.62835127554915,
1.7587664897847));
#11061=CARTESIAN_POINT('Ctrl Pts',(-0.571496231559392,5.63226376845129,
1.77883672036345));
#11062=CARTESIAN_POINT('Ctrl Pts',(-0.637040634203744,5.63617167038824,
1.79888340029762));
#11063=CARTESIAN_POINT('Ctrl Pts',(-0.701603011786067,5.64007957232519,
1.82240557394209));
#11064=CARTESIAN_POINT('Ctrl Pts',(-0.764792477692609,5.64398747426214,
1.84928199514299));
#11065=CARTESIAN_POINT('Ctrl Pts',(-0.827942444368853,5.64789293340081,
1.87614161610773));
#11066=CARTESIAN_POINT('Ctrl Pts',(-0.889720750222587,5.65179839253948,
1.90635113331962));
#11067=CARTESIAN_POINT('Ctrl Pts',(-0.949754581589428,5.65570385167816,
1.93974045334118));
#11068=CARTESIAN_POINT('Ctrl Pts',(-1.00977146830455,5.6596082084943,1.97312034916998));
#11069=CARTESIAN_POINT('Ctrl Pts',(-1.06804442841452,5.66351256531044,2.00967802715169));
#11070=CARTESIAN_POINT('Ctrl Pts',(-1.12422507203602,5.66741692212658,2.04919736297877));
#11071=CARTESIAN_POINT('Ctrl Pts',(-1.18040911894683,5.67132151545933,2.08871909279289));
#11072=CARTESIAN_POINT('Ctrl Pts',(-1.23450019697194,5.67522610879209,2.13120255158595));
#11073=CARTESIAN_POINT('Ctrl Pts',(-1.28618024652872,5.67913070212485,2.17638924278692));
#11074=CARTESIAN_POINT('Ctrl Pts',(-1.33791530868143,5.6830394518355,2.22162403450649));
#11075=CARTESIAN_POINT('Ctrl Pts',(-1.38723384954957,5.68694820154615,2.26956747692651));
#11076=CARTESIAN_POINT('Ctrl Pts',(-1.43385294230865,5.6908569512568,2.31992253267362));
#11077=CARTESIAN_POINT('Ctrl Pts',(-1.48049998864117,5.69476804471795,2.37030778213891));
#11078=CARTESIAN_POINT('Ctrl Pts',(-1.52444405084831,5.6986791381791,2.42310714477325));
#11079=CARTESIAN_POINT('Ctrl Pts',(-1.56544278673989,5.70259023164025,2.47799082477833));
#11080=CARTESIAN_POINT('Ctrl Pts',(-1.60651212056007,5.7065080598236,2.53296901194412));
#11081=CARTESIAN_POINT('Ctrl Pts',(-1.64462573292539,5.71042588800695,2.59003827088932));
#11082=CARTESIAN_POINT('Ctrl Pts',(-1.67958533188183,5.71434371619031,2.6488409579864));
#11083=CARTESIAN_POINT('Ctrl Pts',(-1.69581058202618,5.71616203631396,2.67613212652923));
#11084=CARTESIAN_POINT('Ctrl Pts',(-1.71135711117398,5.71798035643762,2.70379635134295));
#11085=CARTESIAN_POINT('Ctrl Pts',(-1.72620860178437,5.71979867656128,2.73179637789395));
#11086=CARTESIAN_POINT('Ctrl Pts',(-1.75821443653912,5.7237172632497,2.79213808004562));
#11087=CARTESIAN_POINT('Ctrl Pts',(-1.78711577385684,5.72763584993812,2.85427932151719));
#11088=CARTESIAN_POINT('Ctrl Pts',(-1.8127070947079,5.73155443662653,2.91786791715934));
#11089=CARTESIAN_POINT('Ctrl Pts',(-1.83825993473054,5.73546713106488,2.98136089671926));
#11090=CARTESIAN_POINT('Ctrl Pts',(-1.86051245417097,5.73937982550323,3.04629645861358));
#11091=CARTESIAN_POINT('Ctrl Pts',(-1.87930521175737,5.74329251994158,3.11229828902111));
#11092=CARTESIAN_POINT('Ctrl Pts',(-1.89807591022528,5.7472006216218,3.17822264584923));
#11093=CARTESIAN_POINT('Ctrl Pts',(-1.91339477829516,5.75110872330202,3.24521031476371));
#11094=CARTESIAN_POINT('Ctrl Pts',(-1.92515129595695,5.75501682498224,3.31286720829557));
#11095=CARTESIAN_POINT('Ctrl Pts',(-1.93690046140127,5.75892248263828,3.38048179098259));
#11096=CARTESIAN_POINT('Ctrl Pts',(-1.94509161174385,5.76282814029432,3.44876428467494));
#11097=CARTESIAN_POINT('Ctrl Pts',(-1.94966505701588,5.76673379795036,3.51730924448326));
#11098=CARTESIAN_POINT('Ctrl Pts',(-1.95423720971819,5.7706383517701,3.58583483177583));
#11099=CARTESIAN_POINT('Ctrl Pts',(-1.95519365441088,5.77454290558984,3.65462224750134));
#11100=CARTESIAN_POINT('Ctrl Pts',(-1.95252661590114,5.77844745940959,3.72326155072172));
#11101=CARTESIAN_POINT('Ctrl Pts',(-1.94985941706836,5.78235224794284,3.79190498004009));
#11102=CARTESIAN_POINT('Ctrl Pts',(-1.94356832425462,5.78625703647609,3.8603997879099));
#11103=CARTESIAN_POINT('Ctrl Pts',(-1.93369761352118,5.79016182500934,3.92833848310264));
#11104=CARTESIAN_POINT('Ctrl Pts',(-1.9238164062701,5.79407076589625,3.99634942433036));
#11105=CARTESIAN_POINT('Ctrl Pts',(-1.91034805528997,5.79797970678315,4.06380258514305));
#11106=CARTESIAN_POINT('Ctrl Pts',(-1.89338827958256,5.80188864767005,4.13029903726142));
#11107=CARTESIAN_POINT('Ctrl Pts',(-1.87641834377479,5.8057999302879,4.19683532543889));
#11108=CARTESIAN_POINT('Ctrl Pts',(-1.85595296703681,5.80971121290576,4.26241329479919));
#11109=CARTESIAN_POINT('Ctrl Pts',(-1.83213741818948,5.81362249552361,4.32665029701853));
#11110=CARTESIAN_POINT('Ctrl Pts',(-1.80828089286891,5.81754050780235,4.3909978239131));
#11111=CARTESIAN_POINT('Ctrl Pts',(-1.78106288604198,5.82145852008109,4.4539993277038));
#11112=CARTESIAN_POINT('Ctrl Pts',(-1.75067597596649,5.82537653235982,4.51529401729503));
#11113=CARTESIAN_POINT('Ctrl Pts',(-1.73658727746823,5.82719309395067,4.54371291211027));
#11114=CARTESIAN_POINT('Ctrl Pts',(-1.7218180070701,5.82900965554151,4.57176527645755));
#11115=CARTESIAN_POINT('Ctrl Pts',(-1.70639051229435,5.83082621713236,4.59941727239722));
#11116=CARTESIAN_POINT('Ctrl Pts',(-1.67311031083597,5.8347449049416,4.6590681754748));
#11117=CARTESIAN_POINT('Ctrl Pts',(-1.63663272637617,5.83866359275084,4.71708976633959));
#11118=CARTESIAN_POINT('Ctrl Pts',(-1.59714186055193,5.84258228056009,4.77311818095618));
#11119=CARTESIAN_POINT('Ctrl Pts',(-1.55771034837625,5.84649507869296,4.82906238645856));
#11120=CARTESIAN_POINT('Ctrl Pts',(-1.51527482417665,5.85040787682584,4.88301896247169));
#11121=CARTESIAN_POINT('Ctrl Pts',(-1.47006467497902,5.85432067495872,4.93464963000545));
#11122=CARTESIAN_POINT('Ctrl Pts',(-1.42490755490916,5.85822888358513,4.98621973748103));
#11123=CARTESIAN_POINT('Ctrl Pts',(-1.37698259577513,5.86213709221154,5.03546898652687));
#11124=CARTESIAN_POINT('Ctrl Pts',(-1.32656067870836,5.86604530083795,5.08209052170593));
#11125=CARTESIAN_POINT('Ctrl Pts',(-1.27617026817339,5.86995106738943,5.12868292505172));
#11126=CARTESIAN_POINT('Ctrl Pts',(-1.22328635500603,5.87385683394092,5.1726505386083));
#11127=CARTESIAN_POINT('Ctrl Pts',(-1.16821696380806,5.8777626004924,5.21372301794103));
#11128=CARTESIAN_POINT('Ctrl Pts',(-1.11316311124442,5.88166726497472,5.25478390807286));
#11129=CARTESIAN_POINT('Ctrl Pts',(-1.05592539883184,5.88557192945703,5.29295099187465));
#11130=CARTESIAN_POINT('Ctrl Pts',(-0.996843822961217,5.88947659393935,
5.32799507301543));
#11131=CARTESIAN_POINT('Ctrl Pts',(-0.937758671622232,5.89338149472214,
5.36304127493584));
#11132=CARTESIAN_POINT('Ctrl Pts',(-0.876829859508176,5.89728639550492,
5.39496385033971));
#11133=CARTESIAN_POINT('Ctrl Pts',(-0.814423597313302,5.90119129628771,
5.42357863782803));
#11134=CARTESIAN_POINT('Ctrl Pts',(-0.751950948727575,5.90510035101692,
5.45222386508953));
#11135=CARTESIAN_POINT('Ctrl Pts',(-0.68799816132685,5.90900940574613,5.47755407684457));
#11136=CARTESIAN_POINT('Ctrl Pts',(-0.622952197243925,5.91291846047534,
5.49943295599112));
#11137=CARTESIAN_POINT('Ctrl Pts',(-0.557867249321767,5.9168298580088,5.52132494775303));
#11138=CARTESIAN_POINT('Ctrl Pts',(-0.49168829452493,5.92074125554226,5.53976135825024));
#11139=CARTESIAN_POINT('Ctrl Pts',(-0.424815539001397,5.92465265307572,
5.55465631654251));
#11140=CARTESIAN_POINT('Ctrl Pts',(-0.357827719992853,5.92857078068973,
5.5695769035949));
#11141=CARTESIAN_POINT('Ctrl Pts',(-0.290144202343355,5.93248890830375,
5.58094379549636));
#11142=CARTESIAN_POINT('Ctrl Pts',(-0.222172536782913,5.93640703591776,
5.58872271561853));
#11143=CARTESIAN_POINT('Ctrl Pts',(-0.190675965964007,5.93822260984632,
5.59232729565202));
#11144=CARTESIAN_POINT('Ctrl Pts',(-0.159117552570487,5.94003818377488,
5.5951622042778));
#11145=CARTESIAN_POINT('Ctrl Pts',(-0.127537778503509,5.94185375770344,
5.59722782399774));
#11146=CARTESIAN_POINT('Ctrl Pts',(-0.0593934976570972,5.94577148616542,
5.60168511270469));
#11147=CARTESIAN_POINT('Ctrl Pts',(0.00911979872288664,5.9496892146274,
5.60257459642064));
#11148=CARTESIAN_POINT('Ctrl Pts',(0.0775967852891967,5.95360694308939,
5.59985310777224));
#11149=CARTESIAN_POINT('Ctrl Pts',(0.145970770506179,5.95751877860341,5.59713571271816));
#11150=CARTESIAN_POINT('Ctrl Pts',(0.214308066663938,5.96143061411744,5.59081814430954));
#11151=CARTESIAN_POINT('Ctrl Pts',(0.282200215529573,5.96534244963147,5.58090915360567));
#11152=CARTESIAN_POINT('Ctrl Pts',(0.350012708166729,5.96924969548279,5.57101178888272));
#11153=CARTESIAN_POINT('Ctrl Pts',(0.417380606241897,5.97315694133412,5.55753144105258));
#11154=CARTESIAN_POINT('Ctrl Pts',(0.483899283144623,5.97706418718544,5.54052876985154));
#11155=CARTESIAN_POINT('Ctrl Pts',(0.550376392945058,5.98096899142344,5.52353672351266));
#11156=CARTESIAN_POINT('Ctrl Pts',(0.616004858668005,5.98487379566144,5.5030268415894));
#11157=CARTESIAN_POINT('Ctrl Pts',(0.68039052408249,5.98877859989944,5.47911080405717));
#11158=CARTESIAN_POINT('Ctrl Pts',(0.744758049056729,5.99268230397225,5.45520150478642));
#11159=CARTESIAN_POINT('Ctrl Pts',(0.807883007867177,5.99658600804505,5.42788812625661));
#11160=CARTESIAN_POINT('Ctrl Pts',(0.869388420972534,6.00048971211786,5.39733154528946));
#11161=CARTESIAN_POINT('Ctrl Pts',(0.930897609891899,6.00439365583885,5.36677308845545));
#11162=CARTESIAN_POINT('Ctrl Pts',(0.990786616269292,6.00829759955984,5.33297125510818));
#11163=CARTESIAN_POINT('Ctrl Pts',(1.0487020315943,6.01220154328083,5.29613339513978));
#11164=CARTESIAN_POINT('Ctrl Pts',(1.10667924245568,6.01610965249549,5.2592562293095));
#11165=CARTESIAN_POINT('Ctrl Pts',(1.16267824386813,6.02001776171016,5.21933683660997));
#11166=CARTESIAN_POINT('Ctrl Pts',(1.21637452603494,6.02392587092482,5.17662597868813));
#11167=CARTESIAN_POINT('Ctrl Pts',(1.27010306932354,6.02783632816028,5.13388945976828));
#11168=CARTESIAN_POINT('Ctrl Pts',(1.3215257716477,6.03174678539575,5.08835846407014));
#11169=CARTESIAN_POINT('Ctrl Pts',(1.37035328888146,6.03565724263121,5.0403222710259));
#11170=CARTESIAN_POINT('Ctrl Pts',(1.41926506327743,6.03957444778359,4.99220318633494));
#11171=CARTESIAN_POINT('Ctrl Pts',(1.46557238303436,6.04349165293597,4.94157063931928));
#11172=CARTESIAN_POINT('Ctrl Pts',(1.50902523794478,6.04740885808835,4.88874809688681));
#11173=CARTESIAN_POINT('Ctrl Pts',(1.52926017077446,6.04923300481707,4.86414992951168));
#11174=CARTESIAN_POINT('Ctrl Pts',(1.54887670810714,6.05105715154579,4.83907727941792));
#11175=CARTESIAN_POINT('Ctrl Pts',(1.56785287850624,6.05288129827452,4.81356484664189));
#11176=CARTESIAN_POINT('Ctrl Pts',(1.6088093661754,6.05681837522051,4.75850106841765));
#11177=CARTESIAN_POINT('Ctrl Pts',(1.64694295803684,6.06075545216651,4.70116771866654));
#11178=CARTESIAN_POINT('Ctrl Pts',(1.68199473772208,6.06469252911251,4.64188413754908));
#11179=CARTESIAN_POINT('Ctrl Pts',(1.71699327098076,6.06862362532714,4.58269061288171));
#11180=CARTESIAN_POINT('Ctrl Pts',(1.74891903684479,6.07255472154176,4.52155314947093));
#11181=CARTESIAN_POINT('Ctrl Pts',(1.77755484817185,6.07648581775638,4.45882207549275));
#11182=CARTESIAN_POINT('Ctrl Pts',(1.80647677722473,6.080456191933,4.39546421737987));
#11183=CARTESIAN_POINT('Ctrl Pts',(1.83204232976779,6.08442656610961,4.33048112322196));
#11184=CARTESIAN_POINT('Ctrl Pts',(1.85407425987923,6.08839694028623,4.2642612601063));
#11185=CARTESIAN_POINT('Ctrl Pts',(1.87584314099761,6.09231991040319,4.1988320253298));
#11186=CARTESIAN_POINT('Ctrl Pts',(1.89416217128954,6.09624288052016,4.13219586906019));
#11187=CARTESIAN_POINT('Ctrl Pts',(1.9089086849859,6.10016585063712,4.06474759500681));
#11188=CARTESIAN_POINT('Ctrl Pts',(1.92392248772374,6.10415992684356,3.99607678219664));
#11189=CARTESIAN_POINT('Ctrl Pts',(1.9352327965442,6.10815400305,3.92656460262292));
#11190=CARTESIAN_POINT('Ctrl Pts',(1.94276391462493,6.11214807925644,3.85664162365573));
#11191=CARTESIAN_POINT('Ctrl Pts',(1.95029503270565,6.11614215546288,3.78671864468854));
#11192=CARTESIAN_POINT('Ctrl Pts',(1.95404689998987,6.12013623166932,3.71638539512167));
#11193=CARTESIAN_POINT('Ctrl Pts',(1.95399955699113,6.12413030787576,3.64607868772759));
#11194=CARTESIAN_POINT('Origin',(0.,0.,3.64739446828387));
#11195=CARTESIAN_POINT('',(-0.834037993952278,6.59995882699137,5.41445321791391));
#11196=CARTESIAN_POINT('Ctrl Pts',(1.95399955699052,6.12413030792734,3.64607868681973));
#11197=CARTESIAN_POINT('Ctrl Pts',(1.95394681966027,6.12857947203199,3.56776118292628));
#11198=CARTESIAN_POINT('Ctrl Pts',(1.9491815174852,6.13302863613665,3.48962762197157));
#11199=CARTESIAN_POINT('Ctrl Pts',(1.93979384649706,6.13747780024131,3.41220128578885));
#11200=CARTESIAN_POINT('Ctrl Pts',(1.93032535002667,6.14196527052806,3.334108328357));
#11201=CARTESIAN_POINT('Ctrl Pts',(1.9161546596225,6.14645274081481,3.25673503473416));
#11202=CARTESIAN_POINT('Ctrl Pts',(1.89742413111215,6.15094021110156,3.18059936690288));
#11203=CARTESIAN_POINT('Ctrl Pts',(1.87938061318503,6.15526308701624,3.10725625292463));
#11204=CARTESIAN_POINT('Ctrl Pts',(1.85710603049997,6.15958596293091,3.03506166685624));
#11205=CARTESIAN_POINT('Ctrl Pts',(1.83076925289313,6.16390883884559,2.96445966710506));
#11206=CARTESIAN_POINT('Ctrl Pts',(1.80688998876339,6.16782834248827,2.90044561704498));
#11207=CARTESIAN_POINT('Ctrl Pts',(1.77960225082737,6.17174784613095,2.83755952478635));
#11208=CARTESIAN_POINT('Ctrl Pts',(1.74903318078107,6.17566734977363,2.77618902034013));
#11209=CARTESIAN_POINT('Ctrl Pts',(1.71850995347514,6.1795809755539,2.7149105498386));
#11210=CARTESIAN_POINT('Ctrl Pts',(1.68471537782719,6.18349460133417,2.65514359264585));
#11211=CARTESIAN_POINT('Ctrl Pts',(1.64782522231823,6.18740822711444,2.59725731691178));
#11212=CARTESIAN_POINT('Ctrl Pts',(1.61097820320366,6.19131727661405,2.53943872875413));
#11213=CARTESIAN_POINT('Ctrl Pts',(1.57104305610025,6.19522632611366,2.48349686699577));
#11214=CARTESIAN_POINT('Ctrl Pts',(1.52824131094056,6.19913537561327,2.42977609804849));
#11215=CARTESIAN_POINT('Ctrl Pts',(1.485466220882,6.20304199072359,2.37608878410457));
#11216=CARTESIAN_POINT('Ctrl Pts',(1.43982837971589,6.20694860583392,2.32462020257675));
#11217=CARTESIAN_POINT('Ctrl Pts',(1.39159154689848,6.21085522094425,2.2756842340869));
#11218=CARTESIAN_POINT('Ctrl Pts',(1.34336824369791,6.21476074031502,2.22676199130964));
#11219=CARTESIAN_POINT('Ctrl Pts',(1.29254774089051,6.2186662596858,2.18037130118323));
#11220=CARTESIAN_POINT('Ctrl Pts',(1.239431617202,6.22257177905657,2.1367901963847));
#11221=CARTESIAN_POINT('Ctrl Pts',(1.18631221202198,6.22647753970867,2.09320639916406));
#11222=CARTESIAN_POINT('Ctrl Pts',(1.13089728596076,6.23038330036077,2.05243284162792));
#11223=CARTESIAN_POINT('Ctrl Pts',(1.07352113506544,6.23428906101287,2.01470699893531));
#11224=CARTESIAN_POINT('Ctrl Pts',(1.01608394002085,6.23819897711689,1.97694101862565));
#11225=CARTESIAN_POINT('Ctrl Pts',(0.956681767401087,6.2421088932209,1.94222949473817));
#11226=CARTESIAN_POINT('Ctrl Pts',(0.895676657146016,6.24601880932492,1.91076574404724));
#11227=CARTESIAN_POINT('Ctrl Pts',(0.834634960160548,6.24993107033162,1.87928312353116));
#11228=CARTESIAN_POINT('Ctrl Pts',(0.771988860386681,6.25384333133831,1.8510523547138));
#11229=CARTESIAN_POINT('Ctrl Pts',(0.708121117161774,6.257755592345,1.82621889096312));
#11230=CARTESIAN_POINT('Ctrl Pts',(0.644143601749468,6.2616745775199,1.80134274488958));
#11231=CARTESIAN_POINT('Ctrl Pts',(0.578940718830332,6.2655935626948,1.77987571125726));
#11232=CARTESIAN_POINT('Ctrl Pts',(0.512910290448957,6.2695125478697,1.76191335356764));
#11233=CARTESIAN_POINT('Ctrl Pts',(0.482448499574328,6.2713204917187,1.75362678634447));
#11234=CARTESIAN_POINT('Ctrl Pts',(0.451810724361782,6.27312843556769,1.7460853844003));
#11235=CARTESIAN_POINT('Ctrl Pts',(0.421036523795813,6.27493637941668,1.73929482580449));
#11236=CARTESIAN_POINT('Ctrl Pts',(0.354427834596093,6.27884955238994,1.72459711802713));
#11237=CARTESIAN_POINT('Ctrl Pts',(0.286914720102416,6.28276272536319,1.71336187894293));
#11238=CARTESIAN_POINT('Ctrl Pts',(0.218890401956769,6.28667589833644,1.70569341201099));
#11239=CARTESIAN_POINT('Ctrl Pts',(0.150968725339446,6.29058316674401,1.69803651598763));
#11240=CARTESIAN_POINT('Ctrl Pts',(0.0825378619267655,6.29449043515158,
1.69393576663677));
#11241=CARTESIAN_POINT('Ctrl Pts',(0.0140020575316699,6.29839770355914,
1.693444637202));
#11242=CARTESIAN_POINT('Ctrl Pts',(-0.05445332293134,6.30230038694882,1.6929540840873));
#11243=CARTESIAN_POINT('Ctrl Pts',(-0.123012908974516,6.30620307033851,
1.69606474292708));
#11244=CARTESIAN_POINT('Ctrl Pts',(-0.191268328643992,6.31010575372819,
1.70277820113558));
#11245=CARTESIAN_POINT('Ctrl Pts',(-0.259481139672085,6.31400600085657,
1.70948746844856));
#11246=CARTESIAN_POINT('Ctrl Pts',(-0.327389671181108,6.31790624798496,
1.71979502595738));
#11247=CARTESIAN_POINT('Ctrl Pts',(-0.39458814071355,6.32180649511335,1.73365044172018));
#11248=CARTESIAN_POINT('Ctrl Pts',(-0.461767861968078,6.32570565407831,
1.74750199184158));
#11249=CARTESIAN_POINT('Ctrl Pts',(-0.528237431631303,6.32960481304326,
1.7648993357988));
#11250=CARTESIAN_POINT('Ctrl Pts',(-0.593600579199147,6.33350397200822,
1.78574080759012));
#11251=CARTESIAN_POINT('Ctrl Pts',(-0.658968056903733,6.33740338928221,
1.80658366007417));
#11252=CARTESIAN_POINT('Ctrl Pts',(-0.723228497863437,6.3413028065562,1.83087094102833));
#11253=CARTESIAN_POINT('Ctrl Pts',(-0.786001893430877,6.34520222383019,
1.85845147771009));
#11254=CARTESIAN_POINT('Ctrl Pts',(-0.848843289649065,6.34910586523305,
1.88606189161014));
#11255=CARTESIAN_POINT('Ctrl Pts',(-0.910193973351151,6.35300950663591,
1.9169724817724));
#11256=CARTESIAN_POINT('Ctrl Pts',(-0.969695934475925,6.35691314803876,
1.95098479056423));
#11257=CARTESIAN_POINT('Ctrl Pts',(-1.0292340940101,6.36081916424754,1.9850177909678));
#11258=CARTESIAN_POINT('Ctrl Pts',(-1.08692087827315,6.36472518045632,2.02215599775597));
#11259=CARTESIAN_POINT('Ctrl Pts',(-1.14242723508615,6.3686311966651,2.06215757351596));
#11260=CARTESIAN_POINT('Ctrl Pts',(-1.19803072837799,6.37254404842718,2.10222915228894));
#11261=CARTESIAN_POINT('Ctrl Pts',(-1.2514457948728,6.37645690018927,2.14517379158583));
#11262=CARTESIAN_POINT('Ctrl Pts',(-1.30237711460561,6.38036975195135,2.19070992750246));
#11263=CARTESIAN_POINT('Ctrl Pts',(-1.32664912712783,6.38223447463015,2.21241079186215));
#11264=CARTESIAN_POINT('Ctrl Pts',(-1.35035760118794,6.38409919730895,2.23469968813218));
#11265=CARTESIAN_POINT('Ctrl Pts',(-1.37347374173203,6.38596391998775,2.25754344001767));
#11266=CARTESIAN_POINT('Ctrl Pts',(-1.42214152323476,6.38988983122374,2.30563774552445));
#11267=CARTESIAN_POINT('Ctrl Pts',(-1.46837481356246,6.39381574245974,2.35638495257543));
#11268=CARTESIAN_POINT('Ctrl Pts',(-1.51187169559919,6.39774165369573,2.40950918440413));
#11269=CARTESIAN_POINT('Ctrl Pts',(-1.55530304717379,6.40166165032899,2.46255338163496));
#11270=CARTESIAN_POINT('Ctrl Pts',(-1.59600586540521,6.40558164696225,2.51796711955861));
#11271=CARTESIAN_POINT('Ctrl Pts',(-1.6337150448608,6.40950164359551,2.5754377750376));
#11272=CARTESIAN_POINT('Ctrl Pts',(-1.67137938712491,6.4134169792512,2.63284009641807));
#11273=CARTESIAN_POINT('Ctrl Pts',(-1.70605689353571,6.41733231490688,2.6922940697625));
#11274=CARTESIAN_POINT('Ctrl Pts',(-1.73752386585787,6.42124765056257,2.75345553548459));
#11275=CARTESIAN_POINT('Ctrl Pts',(-1.768970819619,6.42516049537214,2.81457809169476));
#11276=CARTESIAN_POINT('Ctrl Pts',(-1.79721106794491,6.42907334018171,2.87740555063099));
#11277=CARTESIAN_POINT('Ctrl Pts',(-1.82206603382122,6.43298618499128,2.94156774139191));
#11278=CARTESIAN_POINT('Ctrl Pts',(-1.84691362236179,6.4368978684084,3.00571088782885));
#11279=CARTESIAN_POINT('Ctrl Pts',(-1.86837774659705,6.44080955182552,3.07118752306012));
#11280=CARTESIAN_POINT('Ctrl Pts',(-1.88632802424344,6.44472123524263,3.13760766485144));
#11281=CARTESIAN_POINT('Ctrl Pts',(-1.90427906532718,6.44863308502627,3.20403063153597));
#11282=CARTESIAN_POINT('Ctrl Pts',(-1.91871583776213,6.45254493480991,3.27139671099792));
#11283=CARTESIAN_POINT('Ctrl Pts',(-1.92955835474803,6.45645678459355,3.33930267088887));
#11284=CARTESIAN_POINT('Ctrl Pts',(-1.94041196353363,6.46037263616518,3.40727809798073));
#11285=CARTESIAN_POINT('Ctrl Pts',(-1.94766390122193,6.46428848773681,3.47579402321349));
#11286=CARTESIAN_POINT('Ctrl Pts',(-1.95128582531457,6.46820433930844,3.54443997383869));
#11287=CARTESIAN_POINT('Ctrl Pts',(-1.95490984473786,6.47212245625163,3.61312563704788));
#11288=CARTESIAN_POINT('Ctrl Pts',(-1.95489967004011,6.47604057319483,3.68194098549075));
#11289=CARTESIAN_POINT('Ctrl Pts',(-1.95127910870616,6.47995869013802,3.75047618308775));
#11290=CARTESIAN_POINT('Ctrl Pts',(-1.94765250212591,6.48388334915571,3.81912581381036));
#11291=CARTESIAN_POINT('Ctrl Pts',(-1.94040352839182,6.4878080081734,3.88749387319111));
#11292=CARTESIAN_POINT('Ctrl Pts',(-1.92960768452086,6.49173266719108,3.95517715759252));
#11293=CARTESIAN_POINT('Ctrl Pts',(-1.92478576989575,6.49348559831367,3.98540758912072));
#11294=CARTESIAN_POINT('Ctrl Pts',(-1.91925696002774,6.49523852943625,4.01550157306799));
#11295=CARTESIAN_POINT('Ctrl Pts',(-1.91303120504268,6.49699146055883,4.04542412613984));
#11296=CARTESIAN_POINT('Ctrl Pts',(-1.89924643361079,6.50087271751781,4.11167722407641));
#11297=CARTESIAN_POINT('Ctrl Pts',(-1.88198628894891,6.50475397447679,4.17735458711253));
#11298=CARTESIAN_POINT('Ctrl Pts',(-1.86131381314334,6.50863523143576,4.24205982712176));
#11299=CARTESIAN_POINT('Ctrl Pts',(-1.84067596241916,6.51250998753633,4.30665668997177));
#11300=CARTESIAN_POINT('Ctrl Pts',(-1.81663727951453,6.5163847436369,4.370284188447));
#11301=CARTESIAN_POINT('Ctrl Pts',(-1.78931167938921,6.52025949973747,4.43255668973964));
#11302=CARTESIAN_POINT('Ctrl Pts',(-1.76201162445679,6.52413063354278,4.49477097591349));
#11303=CARTESIAN_POINT('Ctrl Pts',(-1.7314309429528,6.52800176734808,4.55563231808264));
#11304=CARTESIAN_POINT('Ctrl Pts',(-1.69773268329178,6.53187290115338,4.61477223114742));
#11305=CARTESIAN_POINT('Ctrl Pts',(-1.66405383217142,6.53574180537595,4.67387808253014));
#11306=CARTESIAN_POINT('Ctrl Pts',(-1.62726121136195,6.53961070959853,4.73126403542487));
#11307=CARTESIAN_POINT('Ctrl Pts',(-1.58756426082807,6.5434796138211,4.78658528537354));
#11308=CARTESIAN_POINT('Ctrl Pts',(-1.54787592827796,6.54734767812641,4.84189452539128));
#11309=CARTESIAN_POINT('Ctrl Pts',(-1.50528481066995,6.55121574243173,4.89513954481632));
#11310=CARTESIAN_POINT('Ctrl Pts',(-1.46004311123215,6.55508380673704,4.9460053081214));
#11311=CARTESIAN_POINT('Ctrl Pts',(-1.41476494890701,6.55895498853782,4.99691206707033));
#11312=CARTESIAN_POINT('Ctrl Pts',(-1.36683226981971,6.56282617033861,5.04543536161551));
#11313=CARTESIAN_POINT('Ctrl Pts',(-1.3165361887834,6.56669735213939,5.09129490239409));
#11314=CARTESIAN_POINT('Ctrl Pts',(-1.26622087358059,6.57057001435284,5.13717198072281));
#11315=CARTESIAN_POINT('Ctrl Pts',(-1.21354074412195,6.57444267656628,5.18038295628708));
#11316=CARTESIAN_POINT('Ctrl Pts',(-1.15882003527184,6.57831533877973,5.22068786935456));
#11317=CARTESIAN_POINT('Ctrl Pts',(-1.10400413035419,6.58219473815396,5.26106289973789));
#11318=CARTESIAN_POINT('Ctrl Pts',(-1.04714097458841,6.58607413752819,5.29852149120498));
#11319=CARTESIAN_POINT('Ctrl Pts',(-0.988583156110888,6.58995353690241,
5.33286750083403));
#11320=CARTESIAN_POINT('Ctrl Pts',(-0.938241345921017,6.59328863359873,
5.36239456216384));
#11321=CARTESIAN_POINT('Ctrl Pts',(-0.886647658348861,6.59662373029505,
5.38962186526928));
#11322=CARTESIAN_POINT('Ctrl Pts',(-0.834037993952278,6.59995882699137,
5.41445321791391));
#11323=CARTESIAN_POINT('',(-1.90834530359594,6.6,4.06731613031539));
#11324=CARTESIAN_POINT('Origin',(-1.46549439250521E-15,6.6,3.64739446828387));
#11325=CARTESIAN_POINT('Ctrl Pts',(-1.90834530359594,6.6,4.06731613031539));
#11326=CARTESIAN_POINT('Ctrl Pts',(-2.04784060254395,6.56299081980964,3.43337598697229));
#11327=CARTESIAN_POINT('Ctrl Pts',(-1.64305422583223,6.48897245942892,2.02647090284422));
#11328=CARTESIAN_POINT('Ctrl Pts',(0.47254091610022,6.37794491885784,1.38598473075092));
#11329=CARTESIAN_POINT('Ctrl Pts',(1.80025717638367,6.29024427840894,2.51599492455184));
#11330=CARTESIAN_POINT('Ctrl Pts',(1.9529603584434,6.23955281815039,3.40572641983012));
#11331=CARTESIAN_POINT('Ctrl Pts',(1.95156756343269,6.22587053808222,3.64631438782882));
#11332=CARTESIAN_POINT('Origin',(-2.67773308947627E-16,1.2059437743963,
3.64739446828387));
#11333=CARTESIAN_POINT('',(0.426542481555679,6.599956144719,2.15151955324975));
#11334=CARTESIAN_POINT('Ctrl Pts',(1.5554997682929,6.4559437743963,3.6465454448856));
#11335=CARTESIAN_POINT('Ctrl Pts',(1.55546406369716,6.46061116422838,3.58113088679472));
#11336=CARTESIAN_POINT('Ctrl Pts',(1.55129786300922,6.46527855406046,3.51586849460407));
#11337=CARTESIAN_POINT('Ctrl Pts',(1.54308295192937,6.46994594389254,3.45124336972736));
#11338=CARTESIAN_POINT('Ctrl Pts',(1.53480401511366,6.47464971063311,3.38611456670539));
#11339=CARTESIAN_POINT('Ctrl Pts',(1.52241313274287,6.47935347737368,3.32163325345467));
#11340=CARTESIAN_POINT('Ctrl Pts',(1.50604397351761,6.48405724411425,3.25827777649169));
#11341=CARTESIAN_POINT('Ctrl Pts',(1.4910402357253,6.48836864959578,3.20020705025716));
#11342=CARTESIAN_POINT('Ctrl Pts',(1.47269489336211,6.49268005507731,3.14308208717692));
#11343=CARTESIAN_POINT('Ctrl Pts',(1.45114591966537,6.49699146055883,3.0872554053374));
#11344=CARTESIAN_POINT('Ctrl Pts',(1.42970295788867,6.50128165573217,3.03170336737719));
#11345=CARTESIAN_POINT('Ctrl Pts',(1.40501473944521,6.50557185090551,2.97725350914402));
#11346=CARTESIAN_POINT('Ctrl Pts',(1.37722024457808,6.50986204607885,2.92431449488931));
#11347=CARTESIAN_POINT('Ctrl Pts',(1.35064705115635,6.51396372832576,2.87370164252155));
#11348=CARTESIAN_POINT('Ctrl Pts',(1.32123511808883,6.51806541057266,2.8244701800106));
#11349=CARTESIAN_POINT('Ctrl Pts',(1.28915582586842,6.52216709281957,2.77695922851613));
#11350=CARTESIAN_POINT('Ctrl Pts',(1.25710663774667,6.52626492593395,2.72949286261793));
#11351=CARTESIAN_POINT('Ctrl Pts',(1.22239534318046,6.53036275904833,2.68374424903125));
#11352=CARTESIAN_POINT('Ctrl Pts',(1.18523844654547,6.53446059216271,2.64002657380317));
#11353=CARTESIAN_POINT('Ctrl Pts',(1.14810147323584,6.53855622804132,2.59633233975415));
#11354=CARTESIAN_POINT('Ctrl Pts',(1.10852184009623,6.54265186391993,2.55466729042924));
#11355=CARTESIAN_POINT('Ctrl Pts',(1.06675701342171,6.54674749979854,2.51531243754776));
#11356=CARTESIAN_POINT('Ctrl Pts',(1.02499778330378,6.55084258685509,2.47596285828235));
#11357=CARTESIAN_POINT('Ctrl Pts',(0.981054328890205,6.55493767391165,2.4389232239911));
#11358=CARTESIAN_POINT('Ctrl Pts',(0.93522003928002,6.55903276096821,2.40443681489053));
#11359=CARTESIAN_POINT('Ctrl Pts',(0.889344673355693,6.56313151800817,2.36991949935319));
#11360=CARTESIAN_POINT('Ctrl Pts',(0.841575516606039,6.56723027504813,2.33796029461034));
#11361=CARTESIAN_POINT('Ctrl Pts',(0.792236695122553,6.57132903208809,2.30876036259954));
#11362=CARTESIAN_POINT('Ctrl Pts',(0.742871689082678,6.57542996437529,2.27954493392215));
#11363=CARTESIAN_POINT('Ctrl Pts',(0.691935833065454,6.57953089666248,2.25309193575008));
#11364=CARTESIAN_POINT('Ctrl Pts',(0.639776841899524,6.58363182894968,2.22955602806261));
#11365=CARTESIAN_POINT('Ctrl Pts',(0.58753186031973,6.58773952212041,2.20598131858089));
#11366=CARTESIAN_POINT('Ctrl Pts',(0.534060217488818,6.59184721529114,2.18533348088132));
#11367=CARTESIAN_POINT('Ctrl Pts',(0.47972703809965,6.59595490846187,2.16771807835392));
#11368=CARTESIAN_POINT('Ctrl Pts',(0.462085353070969,6.59728865388091,2.1619984538715));
#11369=CARTESIAN_POINT('Ctrl Pts',(0.444352929777355,6.59862239929996,2.15659812813977));
#11370=CARTESIAN_POINT('Ctrl Pts',(0.426542481555679,6.599956144719,2.15151955324975));
#11371=CARTESIAN_POINT('',(1.55328677638795,6.6,3.5644460487792));
#11372=CARTESIAN_POINT('Origin',(-1.46549439250521E-15,6.6,3.64739446828387));
#11373=CARTESIAN_POINT('Ctrl Pts',(1.55549999987963,6.59414638614667,3.64737511703584));
#11374=CARTESIAN_POINT('Ctrl Pts',(1.55549982783689,6.59510874546272,3.63354590681206));
#11375=CARTESIAN_POINT('Ctrl Pts',(1.55531523240308,6.59607695453386,3.61971776272614));
#11376=CARTESIAN_POINT('Ctrl Pts',(1.5545773647494,6.59802745792116,3.59207096791368));
#11377=CARTESIAN_POINT('Ctrl Pts',(1.55402412717384,6.59900966026662,3.57825363224026));
#11378=CARTESIAN_POINT('Ctrl Pts',(1.55328677638795,6.6,3.5644460487792));
#11379=CARTESIAN_POINT('Ctrl Pts',(0.684651324693825,2.26863408412604,5.04165517356951));
#11380=CARTESIAN_POINT('Ctrl Pts',(1.14788625211098,2.30564859368349,4.81419027525137));
#11381=CARTESIAN_POINT('Ctrl Pts',(1.82177976417329,2.3796722834313,3.86524735393602));
#11382=CARTESIAN_POINT('Ctrl Pts',(1.17126252580745,2.49070515336946,2.23289142025749));
#11383=CARTESIAN_POINT('Ctrl Pts',(-0.550929011373164,2.60173269394054,
1.8972621249236));
#11384=CARTESIAN_POINT('Ctrl Pts',(-1.76895437683424,2.71276023451162,3.15850697088285));
#11385=CARTESIAN_POINT('Ctrl Pts',(-1.37119925940374,2.8237877750827,4.86751886652752));
#11386=CARTESIAN_POINT('Ctrl Pts',(0.279566957660274,2.93481531565378,5.46119858728686));
#11387=CARTESIAN_POINT('Ctrl Pts',(1.67479408727594,3.04584285622485,4.3979960058981));
#11388=CARTESIAN_POINT('Ctrl Pts',(1.53990869075139,3.15687039679593,2.648854714652));
#11389=CARTESIAN_POINT('Ctrl Pts',(-0.00194110293598168,3.26789793736701,
1.81210655462338));
#11390=CARTESIAN_POINT('Ctrl Pts',(-1.5420014927779,3.37892547793809,2.65212320530051));
#11391=CARTESIAN_POINT('Ctrl Pts',(-1.67322430909778,3.48995301850917,4.40148852237912));
#11392=CARTESIAN_POINT('Ctrl Pts',(-0.275705577370856,3.60098055908025,
5.46186647902077));
#11393=CARTESIAN_POINT('Ctrl Pts',(1.37370863799142,3.71200809965133,4.86446239222593));
#11394=CARTESIAN_POINT('Ctrl Pts',(1.76803851820382,3.8230356402224,3.15508418544703));
#11395=CARTESIAN_POINT('Ctrl Pts',(0.547003778353852,3.93406318079349,1.89550562214907));
#11396=CARTESIAN_POINT('Ctrl Pts',(-1.17379929443624,4.04509072136456,2.23653514832174));
#11397=CARTESIAN_POINT('Ctrl Pts',(-1.8221637133016,4.15611826193564,3.86659322783984));
#11398=CARTESIAN_POINT('Ctrl Pts',(-0.805712675430428,4.26714580250672,
5.29638067585463));
#11399=CARTESIAN_POINT('Ctrl Pts',(0.946875698946843,4.3781733430778,5.2195760848642));
#11400=CARTESIAN_POINT('Ctrl Pts',(1.83435347884445,4.48920088364888,3.70635156641869));
#11401=CARTESIAN_POINT('Ctrl Pts',(1.04587869061767,4.60022842421995,2.13926112118895));
#11402=CARTESIAN_POINT('Ctrl Pts',(-0.698160489741093,4.71125596479103,
1.95007286504292));
#11403=CARTESIAN_POINT('Ctrl Pts',(-1.80432722111991,4.82228350536211,3.31163848029748));
#11404=CARTESIAN_POINT('Ctrl Pts',(-1.26197456066073,4.93331104593319,4.97996636915454));
#11405=CARTESIAN_POINT('Ctrl Pts',(0.433377472991916,5.04433858650427,5.43079391382108));
#11406=CARTESIAN_POINT('Ctrl Pts',(1.73277632833419,5.15536612707534,4.25222167463752));
#11407=CARTESIAN_POINT('Ctrl Pts',(1.44902630832145,5.26639366764643,2.521053045387));
#11408=CARTESIAN_POINT('Ctrl Pts',(-0.158619024761313,5.3774212082175,1.81895867888319));
#11409=CARTESIAN_POINT('Ctrl Pts',(-1.6213501498084,5.48844874878859,2.7874193626174));
#11410=CARTESIAN_POINT('Ctrl Pts',(-1.60272396252789,5.59947628935966,4.54157643737503));
#11411=CARTESIAN_POINT('Ctrl Pts',(-0.119801397977274,5.71050382993074,
5.47880049657949));
#11412=CARTESIAN_POINT('Ctrl Pts',(1.47263207300637,5.82153137050182,4.74269930283736));
#11413=CARTESIAN_POINT('Ctrl Pts',(1.71949372363033,5.9325589110729,3.00600192052272));
#11414=CARTESIAN_POINT('Ctrl Pts',(0.395546584890944,6.04358645164398,1.8550680874704));
#11415=CARTESIAN_POINT('Ctrl Pts',(-1.29018035693896,6.15461399221506,2.34215685811287));
#11416=CARTESIAN_POINT('Ctrl Pts',(-1.79638565259649,6.26564153278613,4.02087081558556));
#11417=CARTESIAN_POINT('Ctrl Pts',(-0.662790583736326,6.37666907335722,
5.36010676734267));
#11418=CARTESIAN_POINT('Ctrl Pts',(1.07933315373079,6.48769661392829,5.13104989888334));
#11419=CARTESIAN_POINT('Ctrl Pts',(1.57859588144957,6.56171497430901,4.07982280745058));
#11420=CARTESIAN_POINT('Ctrl Pts',(1.55108009138598,6.59872415449937,3.56456388988623));
#11421=CARTESIAN_POINT('Ctrl Pts',(0.743896982560042,2.34623717873851,5.1623062111741));
#11422=CARTESIAN_POINT('Ctrl Pts',(1.24721750834176,2.38325168829595,4.91515785201061));
#11423=CARTESIAN_POINT('Ctrl Pts',(1.9794257610814,2.45727537804376,3.88409904831387));
#11424=CARTESIAN_POINT('Ctrl Pts',(1.27261662587663,2.56830824798192,2.11048873057953));
#11425=CARTESIAN_POINT('Ctrl Pts',(-0.598603134739513,2.679335788553,1.74581607012819));
#11426=CARTESIAN_POINT('Ctrl Pts',(-1.92202917857765,2.79036332912407,3.11620155152352));
#11427=CARTESIAN_POINT('Ctrl Pts',(-1.48985469649849,2.90139086969515,4.97310118273044));
#11428=CARTESIAN_POINT('Ctrl Pts',(0.30375902116303,3.01241841026623,5.61815441924826));
#11429=CARTESIAN_POINT('Ctrl Pts',(1.81972081700291,3.12344595083731,4.46294860335526));
#11430=CARTESIAN_POINT('Ctrl Pts',(1.67316323966835,3.23447349140838,2.56244701707551));
#11431=CARTESIAN_POINT('Ctrl Pts',(-0.00210907445123478,3.34550103197947,
1.6532916427157));
#11432=CARTESIAN_POINT('Ctrl Pts',(-1.6754371403481,3.45652857255054,2.5659983434854));
#11433=CARTESIAN_POINT('Ctrl Pts',(-1.81801519954786,3.56755611312163,4.46674334146218));
#11434=CARTESIAN_POINT('Ctrl Pts',(-0.29956349996529,3.6785836536927,5.61888010636462));
#11435=CARTESIAN_POINT('Ctrl Pts',(1.49258122179998,3.78961119426379,4.96978021930246));
#11436=CARTESIAN_POINT('Ctrl Pts',(1.92103406698283,3.90063873483486,3.11248257857215));
#11437=CARTESIAN_POINT('Ctrl Pts',(0.594338235376008,4.01166627540594,1.7439075700396));
#11438=CARTESIAN_POINT('Ctrl Pts',(-1.27537291139066,4.12269381597701,2.11444776522171));
#11439=CARTESIAN_POINT('Ctrl Pts',(-1.97984293488608,4.2337213565481,3.88556138614897));
#11440=CARTESIAN_POINT('Ctrl Pts',(-0.875434263318064,4.34474889711917,
5.43907414500631));
#11441=CARTESIAN_POINT('Ctrl Pts',(1.02881269618661,4.45577643769026,5.35562334103673));
#11442=CARTESIAN_POINT('Ctrl Pts',(1.99308753031499,4.56680397826132,3.71145336340483));
#11443=CARTESIAN_POINT('Ctrl Pts',(1.13638281854237,4.67783151883242,2.00875622172268));
#11444=CARTESIAN_POINT('Ctrl Pts',(-0.758575150487437,4.78885905940348,
1.80319673792884));
#11445=CARTESIAN_POINT('Ctrl Pts',(-1.96046297864434,4.89988659997457,3.28258415195061));
#11446=CARTESIAN_POINT('Ctrl Pts',(-1.37117834127157,5.01091414054565,5.0952792241416));
#11447=CARTESIAN_POINT('Ctrl Pts',(0.470879384644959,5.12194168111673,5.58511870598642));
#11448=CARTESIAN_POINT('Ctrl Pts',(1.88272049670789,5.2329692216878,4.30455982756789));
#11449=CARTESIAN_POINT('Ctrl Pts',(1.57441643582957,5.34399676225888,2.42358615067044));
#11450=CARTESIAN_POINT('Ctrl Pts',(-0.172344972748464,5.45502430282995,
1.66073670909787));
#11451=CARTESIAN_POINT('Ctrl Pts',(-1.7616521587176,5.56605184340105,2.7130022264108));
#11452=CARTESIAN_POINT('Ctrl Pts',(-1.74141417185507,5.67707938397211,4.61895363230649));
#11453=CARTESIAN_POINT('Ctrl Pts',(-0.130168299172757,5.78810692454321,
5.63727949319146));
#11454=CARTESIAN_POINT('Ctrl Pts',(1.60006490313954,5.89913446511426,4.83748047559882));
#11455=CARTESIAN_POINT('Ctrl Pts',(1.86828849430994,6.01016200568537,2.95049962019548));
#11456=CARTESIAN_POINT('Ctrl Pts',(0.429774836255361,6.12118954625642,1.69997081136455));
#11457=CARTESIAN_POINT('Ctrl Pts',(-1.40182489957839,6.23221708682751,2.22920935023958));
#11458=CARTESIAN_POINT('Ctrl Pts',(-1.95183419396478,6.34324462739859,4.05318923971664));
#11459=CARTESIAN_POINT('Ctrl Pts',(-0.720144542963022,6.45427216796968,
5.50831471383087));
#11460=CARTESIAN_POINT('Ctrl Pts',(1.17273223212766,6.56529970854074,5.25943662488868));
#11461=CARTESIAN_POINT('Ctrl Pts',(1.7151981899943,6.63931806892147,4.11724258670156));
#11462=CARTESIAN_POINT('Ctrl Pts',(1.68530134694034,6.67632724911183,3.55739622375953));
#11463=CARTESIAN_POINT('Ctrl Pts',(0.803142640426261,2.42384027335096,5.28295724877869));
#11464=CARTESIAN_POINT('Ctrl Pts',(1.34654876457254,2.46085478290841,5.01612542876985));
#11465=CARTESIAN_POINT('Ctrl Pts',(2.1370717579895,2.53487847265622,3.90295074269172));
#11466=CARTESIAN_POINT('Ctrl Pts',(1.3739707259458,2.64591134259438,1.98808604090159));
#11467=CARTESIAN_POINT('Ctrl Pts',(-0.646277258105862,2.75693888316546,
1.59437001533278));
#11468=CARTESIAN_POINT('Ctrl Pts',(-2.07510398032106,2.86796642373654,3.07389613216417));
#11469=CARTESIAN_POINT('Ctrl Pts',(-1.60851013359324,2.97899396430762,5.07868349893336));
#11470=CARTESIAN_POINT('Ctrl Pts',(0.327951084665787,3.09002150487869,5.77511025120965));
#11471=CARTESIAN_POINT('Ctrl Pts',(1.96464754672989,3.20104904544978,4.52790120081243));
#11472=CARTESIAN_POINT('Ctrl Pts',(1.80641778858531,3.31207658602085,2.47603931949901));
#11473=CARTESIAN_POINT('Ctrl Pts',(-0.00227704596648566,3.42310412659194,
1.494476730808));
#11474=CARTESIAN_POINT('Ctrl Pts',(-1.8088727879183,3.53413166716301,2.47987348167028));
#11475=CARTESIAN_POINT('Ctrl Pts',(-1.96280608999794,3.64515920773409,4.53199816054525));
#11476=CARTESIAN_POINT('Ctrl Pts',(-0.323421422559725,3.75618674830517,
5.77589373370848));
#11477=CARTESIAN_POINT('Ctrl Pts',(1.61145380560854,3.86721428887625,5.07509804637899));
#11478=CARTESIAN_POINT('Ctrl Pts',(2.07402961576183,3.97824182944732,3.06988097169728));
#11479=CARTESIAN_POINT('Ctrl Pts',(0.641672692398164,4.08926937001841,1.59230951793014));
#11480=CARTESIAN_POINT('Ctrl Pts',(-1.37694652834506,4.20029691058948,1.99236038212167));
#11481=CARTESIAN_POINT('Ctrl Pts',(-2.13752215647056,4.31132445116056,3.90452954445811));
#11482=CARTESIAN_POINT('Ctrl Pts',(-0.945155851205701,4.42235199173164,
5.58176761415798));
#11483=CARTESIAN_POINT('Ctrl Pts',(1.11074969342638,4.53337953230272,5.49167059720925));
#11484=CARTESIAN_POINT('Ctrl Pts',(2.15182158178555,4.64440707287379,3.71655516039097));
#11485=CARTESIAN_POINT('Ctrl Pts',(1.22688694646707,4.75543461344488,1.8782513222564));
#11486=CARTESIAN_POINT('Ctrl Pts',(-0.81898981123378,4.86646215401595,1.65632061081476));
#11487=CARTESIAN_POINT('Ctrl Pts',(-2.11659873616878,4.97748969458703,3.25352982360373));
#11488=CARTESIAN_POINT('Ctrl Pts',(-1.4803821218824,5.08851723515811,5.21059207912866));
#11489=CARTESIAN_POINT('Ctrl Pts',(0.508381296297998,5.19954477572919,5.73944349815177));
#11490=CARTESIAN_POINT('Ctrl Pts',(2.0326646650816,5.31057231630027,4.35689798049827));
#11491=CARTESIAN_POINT('Ctrl Pts',(1.69980656333768,5.42159985687135,2.32611925595385));
#11492=CARTESIAN_POINT('Ctrl Pts',(-0.186070920735614,5.53262739744242,
1.50251473931255));
#11493=CARTESIAN_POINT('Ctrl Pts',(-1.90195416762681,5.64365493801351,2.63858509020417));
#11494=CARTESIAN_POINT('Ctrl Pts',(-1.88010438118225,5.75468247858458,4.69633082723795));
#11495=CARTESIAN_POINT('Ctrl Pts',(-0.140535200368238,5.86571001915566,
5.79575848980343));
#11496=CARTESIAN_POINT('Ctrl Pts',(1.72749773327271,5.97673755972674,4.9322616483603));
#11497=CARTESIAN_POINT('Ctrl Pts',(2.01708326498956,6.08776510029782,2.89499731986824));
#11498=CARTESIAN_POINT('Ctrl Pts',(0.464003087619777,6.19879264086889,1.54487353525871));
#11499=CARTESIAN_POINT('Ctrl Pts',(-1.51346944221782,6.30982018143997,2.1162618423663));
#11500=CARTESIAN_POINT('Ctrl Pts',(-2.10728273533306,6.42084772201105,4.08550766384771));
#11501=CARTESIAN_POINT('Ctrl Pts',(-0.777498502189718,6.53187526258214,
5.65652266031908));
#11502=CARTESIAN_POINT('Ctrl Pts',(1.26613131052453,6.64290280315321,5.38782335089402));
#11503=CARTESIAN_POINT('Ctrl Pts',(1.85180049853903,6.71692116353393,4.15466236595253));
#11504=CARTESIAN_POINT('Ctrl Pts',(1.81952260249468,6.75393034372429,3.55022855763283));
#11505=CARTESIAN_POINT('Ctrl Pts',(0.862388298292479,2.50144336796343,5.40360828638328));
#11506=CARTESIAN_POINT('Ctrl Pts',(1.44588002080332,2.53845787752087,5.11709300552908));
#11507=CARTESIAN_POINT('Ctrl Pts',(2.29471775489761,2.61248156726868,3.92180243706957));
#11508=CARTESIAN_POINT('Ctrl Pts',(1.47532482601497,2.72351443720684,1.86568335122363));
#11509=CARTESIAN_POINT('Ctrl Pts',(-0.693951381472212,2.83454197777791,
1.44292396053739));
#11510=CARTESIAN_POINT('Ctrl Pts',(-2.22817878206447,2.945569518349,3.03159071280484));
#11511=CARTESIAN_POINT('Ctrl Pts',(-1.72716557068799,3.05659705892007,5.18426581513628));
#11512=CARTESIAN_POINT('Ctrl Pts',(0.352143148168543,3.16762459949115,5.93206608317104));
#11513=CARTESIAN_POINT('Ctrl Pts',(2.10957427645686,3.27865214006223,4.5928537982696));
#11514=CARTESIAN_POINT('Ctrl Pts',(1.93967233750227,3.38967968063331,2.38963162192252));
#11515=CARTESIAN_POINT('Ctrl Pts',(-0.00244501748173502,3.50070722120439,
1.33566181890031));
#11516=CARTESIAN_POINT('Ctrl Pts',(-1.94230843548851,3.61173476177546,2.39374861985516));
#11517=CARTESIAN_POINT('Ctrl Pts',(-2.10759698044802,3.72276230234655,4.59725297962832));
#11518=CARTESIAN_POINT('Ctrl Pts',(-0.347279345154162,3.83378984291762,
5.93290736105231));
#11519=CARTESIAN_POINT('Ctrl Pts',(1.73032638941711,3.9448173834887,5.18041587345552));
#11520=CARTESIAN_POINT('Ctrl Pts',(2.22702516454082,4.05584492405978,3.0272793648224));
#11521=CARTESIAN_POINT('Ctrl Pts',(0.689007149420318,4.16687246463086,1.44071146582068));
#11522=CARTESIAN_POINT('Ctrl Pts',(-1.47852014529947,4.27790000520195,1.87027299902164));
#11523=CARTESIAN_POINT('Ctrl Pts',(-2.29520137805504,4.38892754577301,3.92349770276724));
#11524=CARTESIAN_POINT('Ctrl Pts',(-1.01487743909333,4.4999550863441,5.72446108330965));
#11525=CARTESIAN_POINT('Ctrl Pts',(1.19268669066615,4.61098262691517,5.62771785338177));
#11526=CARTESIAN_POINT('Ctrl Pts',(2.31055563325609,4.72201016748625,3.72165695737712));
#11527=CARTESIAN_POINT('Ctrl Pts',(1.31739107439176,4.83303770805733,1.74774642279012));
#11528=CARTESIAN_POINT('Ctrl Pts',(-0.879404471980124,4.94406524862841,
1.50944448370067));
#11529=CARTESIAN_POINT('Ctrl Pts',(-2.2727344936932,5.05509278919948,3.22447549525686));
#11530=CARTESIAN_POINT('Ctrl Pts',(-1.58958590249323,5.16612032977057,5.32590493411573));
#11531=CARTESIAN_POINT('Ctrl Pts',(0.545883207951039,5.27714787034165,5.8937682903171));
#11532=CARTESIAN_POINT('Ctrl Pts',(2.1826088334553,5.38817541091274,4.40923613342865));
#11533=CARTESIAN_POINT('Ctrl Pts',(1.8251966908458,5.49920295148381,2.22865236123728));
#11534=CARTESIAN_POINT('Ctrl Pts',(-0.199796868722764,5.61023049205489,
1.34429276952724));
#11535=CARTESIAN_POINT('Ctrl Pts',(-2.04225617653602,5.72125803262598,2.56416795399757));
#11536=CARTESIAN_POINT('Ctrl Pts',(-2.01879459050944,5.83228557319703,4.77370802216941));
#11537=CARTESIAN_POINT('Ctrl Pts',(-0.15090210156372,5.94331311376812,5.95423748641541));
#11538=CARTESIAN_POINT('Ctrl Pts',(1.85493056340587,6.0543406543392,5.02704282112175));
#11539=CARTESIAN_POINT('Ctrl Pts',(2.16587803566918,6.16536819491026,2.83949501954101));
#11540=CARTESIAN_POINT('Ctrl Pts',(0.498231338984191,6.27639573548136,1.38977625915286));
#11541=CARTESIAN_POINT('Ctrl Pts',(-1.62511398485724,6.38742327605242,2.00331433449301));
#11542=CARTESIAN_POINT('Ctrl Pts',(-2.26273127670134,6.49845081662351,4.1178260879788));
#11543=CARTESIAN_POINT('Ctrl Pts',(-0.834852461416417,6.60947835719459,
5.80473060680729));
#11544=CARTESIAN_POINT('Ctrl Pts',(1.3595303889214,6.72050589776568,5.51621007689934));
#11545=CARTESIAN_POINT('Ctrl Pts',(1.98840280708377,6.79452425814639,4.1920821452035));
#11546=CARTESIAN_POINT('Ctrl Pts',(1.95374385804904,6.83153343833676,3.54306089150614));
#11547=CARTESIAN_POINT('Ctrl Pts',(-0.83475068776765,6.6,5.41764852956582));
#11548=CARTESIAN_POINT('Ctrl Pts',(-0.7907192463387,6.6,5.43356975418934));
#11549=CARTESIAN_POINT('Ctrl Pts',(-0.746172855022355,6.6,5.44776191297247));
#11550=CARTESIAN_POINT('Ctrl Pts',(-0.701168580024064,6.6,5.46015373566206));
#11551=CARTESIAN_POINT('Ctrl Pts',(-0.632780325123476,6.6,5.47898428295588));
#11552=CARTESIAN_POINT('Ctrl Pts',(-0.563334570914971,6.6,5.49366007719785));
#11553=CARTESIAN_POINT('Ctrl Pts',(-0.49318299999272,6.6,5.50428783506038));
#11554=CARTESIAN_POINT('Ctrl Pts',(-0.422101207184304,6.6,5.51505651881859));
#11555=CARTESIAN_POINT('Ctrl Pts',(-0.350293636793303,6.6,5.52166884246449));
#11556=CARTESIAN_POINT('Ctrl Pts',(-0.278132525181492,6.6,5.52418340588826));
#11557=CARTESIAN_POINT('Ctrl Pts',(-0.245886653883812,6.6,5.52530706220011));
#11558=CARTESIAN_POINT('Ctrl Pts',(-0.213570373240598,6.6,5.52561179547267));
#11559=CARTESIAN_POINT('Ctrl Pts',(-0.181218209318684,6.6,5.52509972733527));
#11560=CARTESIAN_POINT('Ctrl Pts',(-0.160635756765334,6.6,5.5247739494934));
#11561=CARTESIAN_POINT('Ctrl Pts',(-0.140038799820486,6.6,5.52411753323216));
#11562=CARTESIAN_POINT('Ctrl Pts',(-0.119436477969568,6.6,5.52313064631106));
#11563=CARTESIAN_POINT('Ctrl Pts',(-0.107012385205877,6.6,5.52253551073635));
#11564=CARTESIAN_POINT('Ctrl Pts',(-0.0945852684134668,6.6,5.52182002861019));
#11565=CARTESIAN_POINT('Ctrl Pts',(-0.0821742362766652,6.6,5.52098560168541));
#11566=CARTESIAN_POINT('Ctrl Pts',(-0.0118828483446975,6.6,5.51625972344871));
#11567=CARTESIAN_POINT('Ctrl Pts',(0.0580208766311918,6.6,5.50771766688765));
#11568=CARTESIAN_POINT('Ctrl Pts',(0.127194914653329,6.6,5.49545172311723));
#11569=CARTESIAN_POINT('Ctrl Pts',(0.195407928457269,6.6,5.4833561882077));
#11570=CARTESIAN_POINT('Ctrl Pts',(0.262912350191099,6.6,5.46763903161575));
#11571=CARTESIAN_POINT('Ctrl Pts',(0.329361205535183,6.6,5.44834294016202));
#11572=CARTESIAN_POINT('Ctrl Pts',(0.394438685628238,6.6,5.42944508253977));
#11573=CARTESIAN_POINT('Ctrl Pts',(0.458504499769621,6.6,5.40711402878233));
#11574=CARTESIAN_POINT('Ctrl Pts',(0.521201674006322,6.6,5.38135263368176));
#11575=CARTESIAN_POINT('Ctrl Pts',(0.536341223462779,6.6,5.37513200380584));
#11576=CARTESIAN_POINT('Ctrl Pts',(0.551400795453242,6.6,5.3687112007047));
#11577=CARTESIAN_POINT('Ctrl Pts',(0.566375007947456,6.6,5.3620899749367));
#11578=CARTESIAN_POINT('Ctrl Pts',(0.580397210890301,6.6,5.3558897042056));
#11579=CARTESIAN_POINT('Ctrl Pts',(0.594348562080344,6.6,5.34951165292926));
#11580=CARTESIAN_POINT('Ctrl Pts',(0.608198751045081,6.6,5.34296812914597));
#11581=CARTESIAN_POINT('Ctrl Pts',(0.668835467698714,6.6,5.31432030357665));
#11582=CARTESIAN_POINT('Ctrl Pts',(0.727626283796037,6.6,5.28246636804899));
#11583=CARTESIAN_POINT('Ctrl Pts',(0.784252300197534,6.6,5.24745318934579));
#11584=CARTESIAN_POINT('Ctrl Pts',(0.839181586975068,6.6,5.21348913790441));
#11585=CARTESIAN_POINT('Ctrl Pts',(0.892074481299448,6.6,5.17655181654566));
#11586=CARTESIAN_POINT('Ctrl Pts',(0.942605638187179,6.6,5.13664980587656));
#11587=CARTESIAN_POINT('Ctrl Pts',(0.971967892807195,6.6,5.11346385350029));
#11588=CARTESIAN_POINT('Ctrl Pts',(1.00053202791341,6.6,5.08927628734268));
#11589=CARTESIAN_POINT('Ctrl Pts',(1.0282274369325,6.6,5.06408422531173));
#11590=CARTESIAN_POINT('Ctrl Pts',(1.05360839269705,6.6,5.0409974165347));
#11591=CARTESIAN_POINT('Ctrl Pts',(1.0782596465578,6.6,5.01706684049449));
#11592=CARTESIAN_POINT('Ctrl Pts',(1.10215906011826,6.6,4.99233467734654));
#11593=CARTESIAN_POINT('Ctrl Pts',(1.11213104592551,6.6,4.9820152283245));
#11594=CARTESIAN_POINT('Ctrl Pts',(1.12197209809735,6.6,4.97155621627406));
#11595=CARTESIAN_POINT('Ctrl Pts',(1.13168042859955,6.6,4.96096067325043));
#11596=CARTESIAN_POINT('Ctrl Pts',(1.13846377674299,6.6,4.95355741714148));
#11597=CARTESIAN_POINT('Ctrl Pts',(1.14518055018692,6.6,4.94608936910646));
#11598=CARTESIAN_POINT('Ctrl Pts',(1.15182470138071,6.6,4.93856413487155));
#11599=CARTESIAN_POINT('Ctrl Pts',(1.1947391474218,6.6,4.8899587902457));
#11600=CARTESIAN_POINT('Ctrl Pts',(1.23469798287611,6.6,4.8388936680893));
#11601=CARTESIAN_POINT('Ctrl Pts',(1.27161691603853,6.6,4.78569376463853));
#11602=CARTESIAN_POINT('Ctrl Pts',(1.30884832136374,6.6,4.73204359116456));
#11603=CARTESIAN_POINT('Ctrl Pts',(1.3429884558849,6.6,4.67622123940713));
#11604=CARTESIAN_POINT('Ctrl Pts',(1.37390225448353,6.6,4.61854045655832));
#11605=CARTESIAN_POINT('Ctrl Pts',(1.39543358779238,6.6,4.57836602904272));
#11606=CARTESIAN_POINT('Ctrl Pts',(1.41539879061861,6.6,4.53728964580654));
#11607=CARTESIAN_POINT('Ctrl Pts',(1.4337373029043,6.6,4.49541608766621));
#11608=CARTESIAN_POINT('Ctrl Pts',(1.44483372946547,6.6,4.47007887080145));
#11609=CARTESIAN_POINT('Ctrl Pts',(1.45533433091002,6.6,4.44444978212132));
#11610=CARTESIAN_POINT('Ctrl Pts',(1.46522340816155,6.6,4.41855234498481));
#11611=CARTESIAN_POINT('Ctrl Pts',(1.47071187773358,6.6,4.4041791843651));
#11612=CARTESIAN_POINT('Ctrl Pts',(1.47601290065572,6.6,4.3897202501464));
#11613=CARTESIAN_POINT('Ctrl Pts',(1.48111560166178,6.6,4.37520350423181));
#11614=CARTESIAN_POINT('Ctrl Pts',(1.50212938442664,6.6,4.31542109786712));
#11615=CARTESIAN_POINT('Ctrl Pts',(1.51981558387626,6.6,4.25457930080361));
#11616=CARTESIAN_POINT('Ctrl Pts',(1.53403760689704,6.6,4.19297054210301));
#11617=CARTESIAN_POINT('Ctrl Pts',(1.54599109479687,6.6,4.14118891085586));
#11618=CARTESIAN_POINT('Ctrl Pts',(1.55549659766993,6.6,4.08886504394274));
#11619=CARTESIAN_POINT('Ctrl Pts',(1.562444707927,6.6,4.03617640078462));
#11620=CARTESIAN_POINT('Ctrl Pts',(1.56482594200129,6.6,4.01811911790135));
#11621=CARTESIAN_POINT('Ctrl Pts',(1.56690656933101,6.6,4.00001905247287));
#11622=CARTESIAN_POINT('Ctrl Pts',(1.56868146279202,6.6,3.98188358852107));
#11623=CARTESIAN_POINT('Ctrl Pts',(1.56996504112484,6.6,3.96876827253417));
#11624=CARTESIAN_POINT('Ctrl Pts',(1.57108783615978,6.6,3.95564316680129));
#11625=CARTESIAN_POINT('Ctrl Pts',(1.57204829872014,6.6,3.94251393050095));
#11626=CARTESIAN_POINT('Ctrl Pts',(1.57651492193268,6.6,3.8814565254104));
#11627=CARTESIAN_POINT('Ctrl Pts',(1.5774768860156,6.6,3.82028786924348));
#11628=CARTESIAN_POINT('Ctrl Pts',(1.57477701172009,6.6,3.75928439561325));
#11629=CARTESIAN_POINT('Ctrl Pts',(1.57207713742458,6.6,3.69828092198303));
#11630=CARTESIAN_POINT('Ctrl Pts',(1.5657155359986,6.6,3.63744172301404));
#11631=CARTESIAN_POINT('Ctrl Pts',(1.55548296576947,6.6,3.57706412384393));
#11632=CARTESIAN_POINT('Ctrl Pts',(1.55476975631434,6.6,3.57285580925216));
#11633=CARTESIAN_POINT('Ctrl Pts',(1.55403772001654,6.6,3.56864974882339));
#11634=CARTESIAN_POINT('Ctrl Pts',(1.55328677638795,6.6,3.5644460487792));
#11635=CARTESIAN_POINT('Ctrl Pts',(0.905551381329051,2.5,2.37953274318763));
#11636=CARTESIAN_POINT('Ctrl Pts',(0.93880750735117,2.5,2.39730741392822));
#11637=CARTESIAN_POINT('Ctrl Pts',(0.971294169096419,2.5,2.41632950410138));
#11638=CARTESIAN_POINT('Ctrl Pts',(1.00293325234873,2.5,2.43657864884141));
#11639=CARTESIAN_POINT('Ctrl Pts',(1.05261738259362,2.5,2.46837669863281));
#11640=CARTESIAN_POINT('Ctrl Pts',(1.10021262907751,2.5,2.50319771185004));
#11641=CARTESIAN_POINT('Ctrl Pts',(1.14565012573383,2.5,2.54071161219957));
#11642=CARTESIAN_POINT('Ctrl Pts',(1.19258297319328,2.5,2.57946009731157));
#11643=CARTESIAN_POINT('Ctrl Pts',(1.23721436530706,2.5,2.62108203509865));
#11644=CARTESIAN_POINT('Ctrl Pts',(1.27944920585672,2.5,2.66526593419356));
#11645=CARTESIAN_POINT('Ctrl Pts',(1.29885420450408,2.5,2.68556643707253));
#11646=CARTESIAN_POINT('Ctrl Pts',(1.3177529711192,2.5,2.70640843912578));
#11647=CARTESIAN_POINT('Ctrl Pts',(1.33613438528024,2.5,2.7277648485129));
#11648=CARTESIAN_POINT('Ctrl Pts',(1.34511395963642,2.5,2.73819774907173));
#11649=CARTESIAN_POINT('Ctrl Pts',(1.35397004983125,2.5,2.7487534378361));
#11650=CARTESIAN_POINT('Ctrl Pts',(1.36270123656557,2.5,2.75942890284171));
#11651=CARTESIAN_POINT('Ctrl Pts',(1.37087012055007,2.5,2.76941685038711));
#11652=CARTESIAN_POINT('Ctrl Pts',(1.37893068791712,2.5,2.77951115669149));
#11653=CARTESIAN_POINT('Ctrl Pts',(1.38686853165449,2.5,2.78969190446717));
#11654=CARTESIAN_POINT('Ctrl Pts',(1.42575294049156,2.5,2.83956342775162));
#11655=CARTESIAN_POINT('Ctrl Pts',(1.4617682837703,2.5,2.89159377975069));
#11656=CARTESIAN_POINT('Ctrl Pts',(1.49483280836886,2.5,2.94542719131568));
#11657=CARTESIAN_POINT('Ctrl Pts',(1.52879779254209,2.5,3.00072666995616));
#11658=CARTESIAN_POINT('Ctrl Pts',(1.55964980037441,2.5,3.05792940973309));
#11659=CARTESIAN_POINT('Ctrl Pts',(1.58727136569837,2.5,3.11669729836776));
#11660=CARTESIAN_POINT('Ctrl Pts',(1.61427745983468,2.5,3.17415570501651));
#11661=CARTESIAN_POINT('Ctrl Pts',(1.63819595312473,2.5,3.2331112717908));
#11662=CARTESIAN_POINT('Ctrl Pts',(1.65888103081932,2.5,3.29327996688395));
#11663=CARTESIAN_POINT('Ctrl Pts',(1.66330526486009,2.5,3.30614916626286));
#11664=CARTESIAN_POINT('Ctrl Pts',(1.66758143128018,2.5,3.3190739507735));
#11665=CARTESIAN_POINT('Ctrl Pts',(1.67170785004731,2.5,3.3320516709478));
#11666=CARTESIAN_POINT('Ctrl Pts',(1.67470502407642,2.5,3.34147787998246));
#11667=CARTESIAN_POINT('Ctrl Pts',(1.67762270870614,2.5,3.3509306725004));
#11668=CARTESIAN_POINT('Ctrl Pts',(1.68045765017757,2.5,3.36039960222491));
#11669=CARTESIAN_POINT('Ctrl Pts',(1.69969107442491,2.5,3.42464076712906));
#11670=CARTESIAN_POINT('Ctrl Pts',(1.71515655755157,2.5,3.48973852400943));
#11671=CARTESIAN_POINT('Ctrl Pts',(1.72674329034789,2.5,3.5553343327368));
#11672=CARTESIAN_POINT('Ctrl Pts',(1.73830533427205,2.5,3.62079037069669));
#11673=CARTESIAN_POINT('Ctrl Pts',(1.74600577016182,2.5,3.68674333666893));
#11674=CARTESIAN_POINT('Ctrl Pts',(1.74969313315442,2.5,3.75286685206911));
#11675=CARTESIAN_POINT('Ctrl Pts',(1.75158782641231,2.5,3.78684337650342));
#11676=CARTESIAN_POINT('Ctrl Pts',(1.75242223721543,2.5,3.82086532261504));
#11677=CARTESIAN_POINT('Ctrl Pts',(1.75217071705448,2.5,3.85489016933049));
#11678=CARTESIAN_POINT('Ctrl Pts',(1.75188640575889,2.5,3.89335089635671));
#11679=CARTESIAN_POINT('Ctrl Pts',(1.75021469129045,2.5,3.93181536987594));
#11680=CARTESIAN_POINT('Ctrl Pts',(1.74719268051567,2.5,3.97023541010561));
#11681=CARTESIAN_POINT('Ctrl Pts',(1.74626233628355,2.5,3.98206325106621));
#11682=CARTESIAN_POINT('Ctrl Pts',(1.74520379369109,2.5,3.99388863698127));
#11683=CARTESIAN_POINT('Ctrl Pts',(1.74401857389663,2.5,4.00570464319947));
#11684=CARTESIAN_POINT('Ctrl Pts',(1.73748874453672,2.5,4.07080354272976));
#11685=CARTESIAN_POINT('Ctrl Pts',(1.72714356193382,2.5,4.13537383510635));
#11686=CARTESIAN_POINT('Ctrl Pts',(1.71324196470453,2.5,4.19917345782921));
#11687=CARTESIAN_POINT('Ctrl Pts',(1.69886014349002,2.5,4.26517700781126));
#11688=CARTESIAN_POINT('Ctrl Pts',(1.68067195249187,2.5,4.33035647617853));
#11689=CARTESIAN_POINT('Ctrl Pts',(1.65890851542243,2.5,4.39445447707118));
#11690=CARTESIAN_POINT('Ctrl Pts',(1.64157193770915,2.5,4.44551442546975));
#11691=CARTESIAN_POINT('Ctrl Pts',(1.62196549958368,2.5,4.49588849772744));
#11692=CARTESIAN_POINT('Ctrl Pts',(1.60018245343868,2.5,4.54544604562494));
#11693=CARTESIAN_POINT('Ctrl Pts',(1.58725007186591,2.5,4.57486787739977));
#11694=CARTESIAN_POINT('Ctrl Pts',(1.57355011774653,2.5,4.60400187538072));
#11695=CARTESIAN_POINT('Ctrl Pts',(1.55909887661838,2.5,4.63281994275618));
#11696=CARTESIAN_POINT('Ctrl Pts',(1.55322527455423,2.5,4.64453283706888));
#11697=CARTESIAN_POINT('Ctrl Pts',(1.54722753643038,2.5,4.65619353196182));
#11698=CARTESIAN_POINT('Ctrl Pts',(1.54110664803519,2.5,4.66780009865119));
#11699=CARTESIAN_POINT('Ctrl Pts',(1.53534542548472,2.5,4.67872465885014));
#11700=CARTESIAN_POINT('Ctrl Pts',(1.52947966959677,2.5,4.68959258354897));
#11701=CARTESIAN_POINT('Ctrl Pts',(1.52351124624247,2.5,4.70040147770194));
#11702=CARTESIAN_POINT('Ctrl Pts',(1.48912287727678,2.5,4.7626792717152));
#11703=CARTESIAN_POINT('Ctrl Pts',(1.45132521312236,2.5,4.82300799805288));
#11704=CARTESIAN_POINT('Ctrl Pts',(1.41034991342183,2.5,4.88110430170117));
#11705=CARTESIAN_POINT('Ctrl Pts',(1.37394992446206,2.5,4.93271355964086));
#11706=CARTESIAN_POINT('Ctrl Pts',(1.33504133707781,2.5,4.98256157219523));
#11707=CARTESIAN_POINT('Ctrl Pts',(1.29375331928111,2.5,5.03044054308138));
#11708=CARTESIAN_POINT('Ctrl Pts',(1.28165188884384,2.5,5.04447376788862));
#11709=CARTESIAN_POINT('Ctrl Pts',(1.26934585903873,2.5,5.05833775129039));
#11710=CARTESIAN_POINT('Ctrl Pts',(1.25683802025374,2.5,5.0720270093414));
#11711=CARTESIAN_POINT('Ctrl Pts',(1.24131610083745,2.5,5.08901504092617));
#11712=CARTESIAN_POINT('Ctrl Pts',(1.22549768695784,2.5,5.10571818778577));
#11713=CARTESIAN_POINT('Ctrl Pts',(1.2093967828829,2.5,5.12212019708054));
#11714=CARTESIAN_POINT('Ctrl Pts',(1.15862553679579,2.5,5.17384092321813));
#11715=CARTESIAN_POINT('Ctrl Pts',(1.1050280730408,2.5,5.2225917566086));
#11716=CARTESIAN_POINT('Ctrl Pts',(1.04880818331837,2.5,5.26807455143759));
#11717=CARTESIAN_POINT('Ctrl Pts',(0.999177416468837,2.5,5.30822663990606));
#11718=CARTESIAN_POINT('Ctrl Pts',(0.947501993564268,2.5,5.34583208873346));
#11719=CARTESIAN_POINT('Ctrl Pts',(0.893894163889863,2.5,5.38066677880411));
#11720=CARTESIAN_POINT('Ctrl Pts',(0.883181709025403,2.5,5.38762779638989));
#11721=CARTESIAN_POINT('Ctrl Pts',(0.872392012801787,2.5,5.39447809859823));
#11722=CARTESIAN_POINT('Ctrl Pts',(0.86152585967053,2.5,5.40121577991141));
#11723=CARTESIAN_POINT('Ctrl Pts',(-1.13599383904839,2.2684956023837,2.05457297837212));
#11724=CARTESIAN_POINT('Ctrl Pts',(-1.66530114882627,2.30551665559472,2.43205274651924));
#11725=CARTESIAN_POINT('Ctrl Pts',(-2.30874613777931,2.37954688899609,3.74944295559739));
#11726=CARTESIAN_POINT('Ctrl Pts',(-1.16608200062918,2.49058630258783,5.64507475471972));
#11727=CARTESIAN_POINT('Ctrl Pts',(1.04293058450782,2.60161384315891,5.70965731572961));
#11728=CARTESIAN_POINT('Ctrl Pts',(2.2985040575111,2.71264138372999,3.89288000979708));
#11729=CARTESIAN_POINT('Ctrl Pts',(1.45435102275404,2.82366892430106,1.85036189287024));
#11730=CARTESIAN_POINT('Ctrl Pts',(-0.718720235097675,2.93469646487215,
1.4504525726535));
#11731=CARTESIAN_POINT('Ctrl Pts',(-2.23505443062616,3.04572400544322,3.05738160024003));
#11732=CARTESIAN_POINT('Ctrl Pts',(-1.70937833319428,3.15675154601431,5.20357835530822));
#11733=CARTESIAN_POINT('Ctrl Pts',(0.378088709672631,3.26777908658538,5.92786550335696));
#11734=CARTESIAN_POINT('Ctrl Pts',(2.12010467341403,3.37880662715646,4.56866108547329));
#11735=CARTESIAN_POINT('Ctrl Pts',(1.92509810864168,3.48983416772754,2.36771502264023));
#11736=CARTESIAN_POINT('Ctrl Pts',(-0.0287726246970399,3.60086170829862,
1.3359598329503));
#11737=CARTESIAN_POINT('Ctrl Pts',(-1.95635373610663,3.71188924886969,2.41603341962473));
#11738=CARTESIAN_POINT('Ctrl Pts',(-2.0965179233959,3.82291678944078,4.62114101481739));
#11739=CARTESIAN_POINT('Ctrl Pts',(-0.321203270128677,3.93394433001185,
5.93658538901197));
#11740=CARTESIAN_POINT('Ctrl Pts',(1.74757773142461,4.04497187058293,5.16051723839122));
#11741=CARTESIAN_POINT('Ctrl Pts',(2.2196887832987,4.15599941115401,3.00198764182795));
#11742=CARTESIAN_POINT('Ctrl Pts',(0.663786606567354,4.26702695172509,1.43313269957975));
#11743=CARTESIAN_POINT('Ctrl Pts',(-1.49858251767498,4.37805449229617,1.88733236901576));
#11744=CARTESIAN_POINT('Ctrl Pts',(-2.29177547185453,4.48908203286725,3.949608535076));
#11745=CARTESIAN_POINT('Ctrl Pts',(-0.991093389100879,4.60010957343832,
5.73576745544));
#11746=CARTESIAN_POINT('Ctrl Pts',(1.21509863142361,4.7111371140094,5.61388972183788));
#11747=CARTESIAN_POINT('Ctrl Pts',(2.31111895030389,4.82216465458049,3.69532819685544));
#11748=CARTESIAN_POINT('Ctrl Pts',(1.29559086556015,4.93319219515156,1.73297264398224));
#11749=CARTESIAN_POINT('Ctrl Pts',(-0.903650040337952,5.04421973572264,
1.51972289010189));
#11750=CARTESIAN_POINT('Ctrl Pts',(-2.27727441159882,5.15524727629372,3.25041685278073));
#11751=CARTESIAN_POINT('Ctrl Pts',(-1.57027056200704,5.26627481686479,5.34380488426395));
#11752=CARTESIAN_POINT('Ctrl Pts',(0.571403078011824,5.37730235743588,5.88727855768163));
#11753=CARTESIAN_POINT('Ctrl Pts',(2.19102344350068,5.48832989800695,4.38427456450717));
#11754=CARTESIAN_POINT('Ctrl Pts',(1.80880579267535,5.59935743857804,2.20804710973091));
#11755=CARTESIAN_POINT('Ctrl Pts',(-0.225994198385466,5.71038497914911,
1.34682732113855));
#11756=CARTESIAN_POINT('Ctrl Pts',(-2.05437013573578,5.82141251972019,2.5876082456352));
#11757=CARTESIAN_POINT('Ctrl Pts',(-2.00567014672563,5.93244006029126,4.79648094529437));
#11758=CARTESIAN_POINT('Ctrl Pts',(-0.124697940094913,6.04346760086235,
5.95583840267334));
#11759=CARTESIAN_POINT('Ctrl Pts',(1.87059546628155,6.15449514143342,5.00542858236713));
#11760=CARTESIAN_POINT('Ctrl Pts',(2.15606965103839,6.2655226820045,2.81553154933147));
#11761=CARTESIAN_POINT('Ctrl Pts',(0.473125107460961,6.37655022257559,1.3831890024094));
#11762=CARTESIAN_POINT('Ctrl Pts',(-1.64508549561477,6.48757776314665,2.02446699268324));
#11763=CARTESIAN_POINT('Ctrl Pts',(-2.0503723003236,6.56159612352738,3.43311140089402));
#11764=CARTESIAN_POINT('Ctrl Pts',(-1.91070454657702,6.59860530371774,4.06783526971427));
#11765=CARTESIAN_POINT('Ctrl Pts',(-1.05786062916686,2.34618472182287,2.16412661457789));
#11766=CARTESIAN_POINT('Ctrl Pts',(-1.55076239015994,2.38320577503389,2.51564347259569));
#11767=CARTESIAN_POINT('Ctrl Pts',(-2.14995148560286,2.45723600843527,3.74242410073808));
#11768=CARTESIAN_POINT('Ctrl Pts',(-1.08587933881672,2.568275422027,5.50767508957099));
#11769=CARTESIAN_POINT('Ctrl Pts',(0.971198228706071,2.67930296259808,5.56781568741114));
#11770=CARTESIAN_POINT('Ctrl Pts',(2.14041385159104,2.79033050316915,3.87599561071092));
#11771=CARTESIAN_POINT('Ctrl Pts',(1.35432133086994,2.90135804374023,1.97396108729576));
#11772=CARTESIAN_POINT('Ctrl Pts',(-0.669286939735767,3.01238558431131,
1.60155737298641));
#11773=CARTESIAN_POINT('Ctrl Pts',(-2.08132826511188,3.12341312488239,3.0979624534692));
#11774=CARTESIAN_POINT('Ctrl Pts',(-1.59180796310647,3.23444066545347,5.09654463903298));
#11775=CARTESIAN_POINT('Ctrl Pts',(0.352083916784465,3.34546820602455,5.77101560163446));
#11776=CARTESIAN_POINT('Ctrl Pts',(1.97428470703338,3.45649574659562,4.50529672953804));
#11777=CARTESIAN_POINT('Ctrl Pts',(1.79269061716177,3.56752328716671,2.45573087208473));
#11778=CARTESIAN_POINT('Ctrl Pts',(-0.0267936548760603,3.67855082773777,
1.49493939893213));
#11779=CARTESIAN_POINT('Ctrl Pts',(-1.82179649485102,3.78957836830887,2.50072594871048));
#11780=CARTESIAN_POINT('Ctrl Pts',(-1.9523202444135,3.90060590887993,4.55416710996289));
#11781=CARTESIAN_POINT('Ctrl Pts',(-0.299111035420236,4.01163344945102,
5.77913573698044));
#11782=CARTESIAN_POINT('Ctrl Pts',(1.62738002173627,4.12266099002209,5.05644524881745));
#11783=CARTESIAN_POINT('Ctrl Pts',(2.06701946096995,4.23368853059318,3.04637846975065));
#11784=CARTESIAN_POINT('Ctrl Pts',(0.618131624590583,4.34471607116425,1.58542875397713));
#11785=CARTESIAN_POINT('Ctrl Pts',(-1.39551060095016,4.45574361173534,2.00838874861888));
#11786=CARTESIAN_POINT('Ctrl Pts',(-2.13414805541208,4.56677115230641,3.92882237031159));
#11787=CARTESIAN_POINT('Ctrl Pts',(-0.922926375230729,4.67779869287749,
5.59212998197178));
#11788=CARTESIAN_POINT('Ctrl Pts',(1.13152462500531,4.78882623344857,5.47863495099715));
#11789=CARTESIAN_POINT('Ctrl Pts',(2.15216109701436,4.89985377401965,3.69203133383899));
#11790=CARTESIAN_POINT('Ctrl Pts',(1.20648063490589,5.01088131459073,1.86464582482029));
#11791=CARTESIAN_POINT('Ctrl Pts',(-0.841497345636436,5.1219088551618,1.66606330521921));
#11792=CARTESIAN_POINT('Ctrl Pts',(-2.12064437238283,5.23293639573289,3.27772081718985));
#11793=CARTESIAN_POINT('Ctrl Pts',(-1.46226796976159,5.34396393630395,5.22712644242662));
#11794=CARTESIAN_POINT('Ctrl Pts',(0.532102198828668,5.45499147687504,5.73322021013476));
#11795=CARTESIAN_POINT('Ctrl Pts',(2.04032571197971,5.56601901744612,4.33359224103263));
#11796=CARTESIAN_POINT('Ctrl Pts',(1.68439684099264,5.6770465580172,2.30704485548669));
#11797=CARTESIAN_POINT('Ctrl Pts',(-0.210450406220845,5.78807409858828,
1.50505942555297));
#11798=CARTESIAN_POINT('Ctrl Pts',(-1.91307136502743,5.89910163915935,2.66049992560517));
#11799=CARTESIAN_POINT('Ctrl Pts',(-1.86772094212563,6.01012917973043,4.71744722891832));
#11800=CARTESIAN_POINT('Ctrl Pts',(-0.116121264772982,6.12115672030151,
5.79706453592731));
#11801=CARTESIAN_POINT('Ctrl Pts',(1.74193664512734,6.23218426087259,4.9120235296154));
#11802=CARTESIAN_POINT('Ctrl Pts',(2.00777602762851,6.34321180144366,2.87274675403155));
#11803=CARTESIAN_POINT('Ctrl Pts',(0.440583748475743,6.45423934201476,1.53892016467367));
#11804=CARTESIAN_POINT('Ctrl Pts',(-1.53193716163296,6.56526688258582,2.13609130675508));
#11805=CARTESIAN_POINT('Ctrl Pts',(-1.90934849916403,6.63928524296654,3.44784970607045));
#11806=CARTESIAN_POINT('Ctrl Pts',(-1.77928703864022,6.6762944231569,4.03891751659649));
#11807=CARTESIAN_POINT('Ctrl Pts',(-0.979727419285334,2.42387384126203,
2.27368025078364));
#11808=CARTESIAN_POINT('Ctrl Pts',(-1.43622363149362,2.46089489447305,2.59923419867212));
#11809=CARTESIAN_POINT('Ctrl Pts',(-1.99115683342641,2.53492512787443,3.73540524587877));
#11810=CARTESIAN_POINT('Ctrl Pts',(-1.00567667700427,2.64596454146616,5.37027542442224));
#11811=CARTESIAN_POINT('Ctrl Pts',(0.89946587290432,2.75699208203724,5.42597405909269));
#11812=CARTESIAN_POINT('Ctrl Pts',(1.98232364567101,2.86801962260832,3.85911121162473));
#11813=CARTESIAN_POINT('Ctrl Pts',(1.25429163898582,2.9790471631794,2.09756028172128));
#11814=CARTESIAN_POINT('Ctrl Pts',(-0.619853644373857,3.09007470375048,
1.75266217331931));
#11815=CARTESIAN_POINT('Ctrl Pts',(-1.9276020995976,3.20110224432155,3.13854330669838));
#11816=CARTESIAN_POINT('Ctrl Pts',(-1.47423759301864,3.31212978489263,4.98951092275774));
#11817=CARTESIAN_POINT('Ctrl Pts',(0.326079123896297,3.42315732546372,5.61416569991195));
#11818=CARTESIAN_POINT('Ctrl Pts',(1.82846474065272,3.53418486603478,4.44193237360281));
#11819=CARTESIAN_POINT('Ctrl Pts',(1.66028312568185,3.64521240660588,2.54374672152922));
#11820=CARTESIAN_POINT('Ctrl Pts',(-0.0248146850550805,3.75623994717694,
1.65391896491398));
#11821=CARTESIAN_POINT('Ctrl Pts',(-1.6872392535954,3.86726748774803,2.58541847779621));
#11822=CARTESIAN_POINT('Ctrl Pts',(-1.8081225654311,3.97829502831911,4.4871932051084));
#11823=CARTESIAN_POINT('Ctrl Pts',(-0.277018800711798,4.08932256889018,
5.6216860849489));
#11824=CARTESIAN_POINT('Ctrl Pts',(1.50718231204793,4.20035010946126,4.95237325924368));
#11825=CARTESIAN_POINT('Ctrl Pts',(1.91435013864119,4.31137765003234,3.09076929767337));
#11826=CARTESIAN_POINT('Ctrl Pts',(0.572476642613815,4.42240519060342,1.73772480837452));
#11827=CARTESIAN_POINT('Ctrl Pts',(-1.29243868422536,4.5334327311745,2.12944512822198));
#11828=CARTESIAN_POINT('Ctrl Pts',(-1.97652063896961,4.64446027174557,3.90803620554718));
#11829=CARTESIAN_POINT('Ctrl Pts',(-0.854759361360582,4.75548781231666,
5.44849250850354));
#11830=CARTESIAN_POINT('Ctrl Pts',(1.04795061858702,4.86651535288773,5.34338018015644));
#11831=CARTESIAN_POINT('Ctrl Pts',(1.99320324372482,4.97754289345882,3.68873447082252));
#11832=CARTESIAN_POINT('Ctrl Pts',(1.11737040425166,5.08857043402988,1.99631900565835));
#11833=CARTESIAN_POINT('Ctrl Pts',(-0.779344650934924,5.19959797460099,
1.81240372033652));
#11834=CARTESIAN_POINT('Ctrl Pts',(-1.96401433316682,5.31062551517205,3.305024781599));
#11835=CARTESIAN_POINT('Ctrl Pts',(-1.35426537751614,5.42165305574312,5.11044800058928));
#11836=CARTESIAN_POINT('Ctrl Pts',(0.492801319645515,5.53268059631421,5.5791618625879));
#11837=CARTESIAN_POINT('Ctrl Pts',(1.88962798045874,5.64370813688528,4.2829099175581));
#11838=CARTESIAN_POINT('Ctrl Pts',(1.55998788930993,5.75473567745637,2.40604260124246));
#11839=CARTESIAN_POINT('Ctrl Pts',(-0.194906614056223,5.86576321802745,
1.66329152996741));
#11840=CARTESIAN_POINT('Ctrl Pts',(-1.77177259431909,5.97679075859852,2.73339160557513));
#11841=CARTESIAN_POINT('Ctrl Pts',(-1.72977173752561,6.08781829916961,4.63841351254227));
#11842=CARTESIAN_POINT('Ctrl Pts',(-0.107544589451053,6.19884583974067,
5.63829066918126));
#11843=CARTESIAN_POINT('Ctrl Pts',(1.61327782397313,6.30987338031176,4.81861847686368));
#11844=CARTESIAN_POINT('Ctrl Pts',(1.85948240421865,6.42090092088282,2.92996195873161));
#11845=CARTESIAN_POINT('Ctrl Pts',(0.408042389490524,6.53192846145393,1.69465132693797));
#11846=CARTESIAN_POINT('Ctrl Pts',(-1.41878882765114,6.64295600202498,2.2477156208269));
#11847=CARTESIAN_POINT('Ctrl Pts',(-1.76832469800446,6.71697436240571,3.46258801124687));
#11848=CARTESIAN_POINT('Ctrl Pts',(-1.64786953070343,6.75398354259608,4.00999976347872));
#11849=CARTESIAN_POINT('Ctrl Pts',(-0.901594209403805,2.5015629607012,2.38323388698939));
#11850=CARTESIAN_POINT('Ctrl Pts',(-1.3216848728273,2.53858401391222,2.68282492474856));
#11851=CARTESIAN_POINT('Ctrl Pts',(-1.83236218124995,2.6126142473136,3.72838639101944));
#11852=CARTESIAN_POINT('Ctrl Pts',(-0.925474015191809,2.72365366090533,
5.23287575927349));
#11853=CARTESIAN_POINT('Ctrl Pts',(0.827733517102571,2.8346812014764,5.28413243077424));
#11854=CARTESIAN_POINT('Ctrl Pts',(1.82423343975097,2.94570874204748,3.84222681253854));
#11855=CARTESIAN_POINT('Ctrl Pts',(1.15426194710171,3.05673628261856,2.22115947614681));
#11856=CARTESIAN_POINT('Ctrl Pts',(-0.57042034901195,3.16776382318964,1.9037669736522));
#11857=CARTESIAN_POINT('Ctrl Pts',(-1.77387593408332,3.27879136376072,3.17912415992756));
#11858=CARTESIAN_POINT('Ctrl Pts',(-1.35666722293081,3.3898189043318,4.8824772064825));
#11859=CARTESIAN_POINT('Ctrl Pts',(0.30007433100813,3.50084644490287,5.45731579818944));
#11860=CARTESIAN_POINT('Ctrl Pts',(1.68264477427207,3.61187398547397,4.37856801766755));
#11861=CARTESIAN_POINT('Ctrl Pts',(1.52787563420194,3.72290152604503,2.6317625709737));
#11862=CARTESIAN_POINT('Ctrl Pts',(-0.0228357152341017,3.83392906661613,
1.81289853089582));
#11863=CARTESIAN_POINT('Ctrl Pts',(-1.55268201233978,3.94495660718718,2.67011100688194));
#11864=CARTESIAN_POINT('Ctrl Pts',(-1.66392488644871,4.05598414775829,4.42021930025391));
#11865=CARTESIAN_POINT('Ctrl Pts',(-0.254926566003359,4.16701168832935,
5.46423643291735));
#11866=CARTESIAN_POINT('Ctrl Pts',(1.38698460235958,4.27803922890044,4.84830126966989));
#11867=CARTESIAN_POINT('Ctrl Pts',(1.76168081631245,4.3890667694715,3.13516012559607));
#11868=CARTESIAN_POINT('Ctrl Pts',(0.526821660637044,4.5000943100426,1.8900208627719));
#11869=CARTESIAN_POINT('Ctrl Pts',(-1.18936676750056,4.61112185061366,2.25050150782511));
#11870=CARTESIAN_POINT('Ctrl Pts',(-1.81889322252715,4.72214939118475,3.88725004078275));
#11871=CARTESIAN_POINT('Ctrl Pts',(-0.786592347490432,4.83317693175582,
5.30485503503531));
#11872=CARTESIAN_POINT('Ctrl Pts',(0.964376612168716,4.9442044723269,5.2081254093157));
#11873=CARTESIAN_POINT('Ctrl Pts',(1.83424539043528,5.05523201289798,3.68543760780607));
#11874=CARTESIAN_POINT('Ctrl Pts',(1.02826017359741,5.16625955346907,2.12799218649641));
#11875=CARTESIAN_POINT('Ctrl Pts',(-0.717191956233407,5.27728709404013,
1.95874413545384));
#11876=CARTESIAN_POINT('Ctrl Pts',(-1.80738429395082,5.38831463461122,3.33232874600814));
#11877=CARTESIAN_POINT('Ctrl Pts',(-1.2462627852707,5.49934217518229,4.99376955875193));
#11878=CARTESIAN_POINT('Ctrl Pts',(0.453500440462359,5.61036971575338,5.42510351504104));
#11879=CARTESIAN_POINT('Ctrl Pts',(1.73893024893777,5.72139725632445,4.23222759408355));
#11880=CARTESIAN_POINT('Ctrl Pts',(1.43557893762722,5.83242479689554,2.50504034699825));
#11881=CARTESIAN_POINT('Ctrl Pts',(-0.179362821891601,5.9434523374666,1.82152363438183));
#11882=CARTESIAN_POINT('Ctrl Pts',(-1.63047382361075,6.0544798780377,2.80628328554509));
#11883=CARTESIAN_POINT('Ctrl Pts',(-1.59182253292561,6.16550741860876,4.55937979616623));
#11884=CARTESIAN_POINT('Ctrl Pts',(-0.0989679141291225,6.27653495917986,
5.47951680243522));
#11885=CARTESIAN_POINT('Ctrl Pts',(1.48461900281892,6.38756249975091,4.72521342411197));
#11886=CARTESIAN_POINT('Ctrl Pts',(1.71118878080877,6.49859004032201,2.98717716343168));
#11887=CARTESIAN_POINT('Ctrl Pts',(0.375501030505306,6.60961758089308,1.85038248920226));
#11888=CARTESIAN_POINT('Ctrl Pts',(-1.30564049366934,6.72064512146416,2.35933993489874));
#11889=CARTESIAN_POINT('Ctrl Pts',(-1.62730089684488,6.79466348184489,3.47732631642329));
#11890=CARTESIAN_POINT('Ctrl Pts',(-1.51645202276663,6.83167266203525,3.98108201036094));
#11891=CARTESIAN_POINT('Ctrl Pts',(0.426653165344753,6.6,2.14890699090199));
#11892=CARTESIAN_POINT('Ctrl Pts',(0.392021497824992,6.6,2.13398863376564));
#11893=CARTESIAN_POINT('Ctrl Pts',(0.356894299772026,6.6,2.12044962477061));
#11894=CARTESIAN_POINT('Ctrl Pts',(0.321336195052727,6.6,2.10833833927896));
#11895=CARTESIAN_POINT('Ctrl Pts',(0.265498001512556,6.6,2.08931954430544));
#11896=CARTESIAN_POINT('Ctrl Pts',(0.208598730014752,6.6,2.07381868408178));
#11897=CARTESIAN_POINT('Ctrl Pts',(0.1509393876911,6.6,2.06168379971155));
#11898=CARTESIAN_POINT('Ctrl Pts',(0.0913824050528511,6.6,2.04914954127866));
#11899=CARTESIAN_POINT('Ctrl Pts',(0.0310137753734779,6.6,2.04020620057528));
#11900=CARTESIAN_POINT('Ctrl Pts',(-0.0298636689844298,6.6,2.03473391296962));
#11901=CARTESIAN_POINT('Ctrl Pts',(-0.0578342380330448,6.6,2.03221963202464));
#11902=CARTESIAN_POINT('Ctrl Pts',(-0.0859125425645439,6.60000000000001,
2.03043876497219));
#11903=CARTESIAN_POINT('Ctrl Pts',(-0.114070466778639,6.60000000000001,
2.02938311428739));
#11904=CARTESIAN_POINT('Ctrl Pts',(-0.127825777649119,6.60000000000001,
2.02886742274601));
#11905=CARTESIAN_POINT('Ctrl Pts',(-0.14160009738174,6.6,2.02852482806012));
#11906=CARTESIAN_POINT('Ctrl Pts',(-0.155390186243194,6.6,2.02835456195388));
#11907=CARTESIAN_POINT('Ctrl Pts',(-0.168292536222095,6.6,2.02819525675183));
#11908=CARTESIAN_POINT('Ctrl Pts',(-0.181210508050245,6.6,2.02818695541747));
#11909=CARTESIAN_POINT('Ctrl Pts',(-0.194119545885251,6.6,2.02832850350773));
#11910=CARTESIAN_POINT('Ctrl Pts',(-0.257354814991631,6.6,2.02902188063574));
#11911=CARTESIAN_POINT('Ctrl Pts',(-0.320489102810685,6.6,2.03330438410903));
#11912=CARTESIAN_POINT('Ctrl Pts',(-0.383193278303246,6.6,2.04101811062465));
#11913=CARTESIAN_POINT('Ctrl Pts',(-0.447605187296912,6.6,2.0489419186713));
#11914=CARTESIAN_POINT('Ctrl Pts',(-0.511564220105741,6.6,2.06048621346354));
#11915=CARTESIAN_POINT('Ctrl Pts',(-0.574732782053451,6.6,2.07553202136673));
#11916=CARTESIAN_POINT('Ctrl Pts',(-0.63649384373375,6.6,2.09024258373015));
#11917=CARTESIAN_POINT('Ctrl Pts',(-0.69750033846162,6.6,2.10830059514023));
#11918=CARTESIAN_POINT('Ctrl Pts',(-0.757439278427627,6.6,2.12964296447379));
#11919=CARTESIAN_POINT('Ctrl Pts',(-0.770258979238349,6.6,2.13420765630189));
#11920=CARTESIAN_POINT('Ctrl Pts',(-0.783029821639415,6.6,2.13892276037541));
#11921=CARTESIAN_POINT('Ctrl Pts',(-0.795748686884653,6.6,2.14378793828041));
#11922=CARTESIAN_POINT('Ctrl Pts',(-0.804987038335825,6.6,2.14732176165949));
#11923=CARTESIAN_POINT('Ctrl Pts',(-0.814196614102969,6.6,2.15093430558212));
#11924=CARTESIAN_POINT('Ctrl Pts',(-0.823367217132576,6.6,2.15462160038541));
#11925=CARTESIAN_POINT('Ctrl Pts',(-0.885585027870816,6.6,2.1796379934695));
#11926=CARTESIAN_POINT('Ctrl Pts',(-0.946123259636302,6.6,2.208134350996));
#11927=CARTESIAN_POINT('Ctrl Pts',(-1.00463249706853,6.6,2.23997375780666));
#11928=CARTESIAN_POINT('Ctrl Pts',(-1.06301708457837,6.6,2.27174533294216));
#11929=CARTESIAN_POINT('Ctrl Pts',(-1.11938248584106,6.6,2.3068458567018));
#11930=CARTESIAN_POINT('Ctrl Pts',(-1.17337908184492,6.6,2.34519025207806));
#11931=CARTESIAN_POINT('Ctrl Pts',(-1.2011248982945,6.6,2.36489328217099));
#11932=CARTESIAN_POINT('Ctrl Pts',(-1.22824511864328,6.6,2.38545362353557));
#11933=CARTESIAN_POINT('Ctrl Pts',(-1.25469050295844,6.6,2.40686481674483));
#11934=CARTESIAN_POINT('Ctrl Pts',(-1.28458305880662,6.6,2.43106697169013));
#11935=CARTESIAN_POINT('Ctrl Pts',(-1.31361349719727,6.6,2.45635617344964));
#11936=CARTESIAN_POINT('Ctrl Pts',(-1.34176728722323,6.6,2.48267337167381));
#11937=CARTESIAN_POINT('Ctrl Pts',(-1.3504346031965,6.6,2.49077528165927));
#11938=CARTESIAN_POINT('Ctrl Pts',(-1.35902006809447,6.6,2.49897589013228));
#11939=CARTESIAN_POINT('Ctrl Pts',(-1.36751921647731,6.6,2.50726969035999));
#11940=CARTESIAN_POINT('Ctrl Pts',(-1.41452515694303,6.6,2.55313991902021));
#11941=CARTESIAN_POINT('Ctrl Pts',(-1.45871734531156,6.59999999999999,2.60168402751855));
#11942=CARTESIAN_POINT('Ctrl Pts',(-1.50006762008885,6.6,2.65254463268113));
#11943=CARTESIAN_POINT('Ctrl Pts',(-1.54232945728785,6.6,2.70452645449005));
#11944=CARTESIAN_POINT('Ctrl Pts',(-1.58162322286118,6.6,2.75892858938386));
#11945=CARTESIAN_POINT('Ctrl Pts',(-1.61789321674135,6.6,2.81541824090764));
#11946=CARTESIAN_POINT('Ctrl Pts',(-1.65493748507655,6.6,2.87311380645206));
#11947=CARTESIAN_POINT('Ctrl Pts',(-1.68882811749007,6.6,2.93298765877334));
#11948=CARTESIAN_POINT('Ctrl Pts',(-1.71947060296554,6.6,2.99472594037275));
#11949=CARTESIAN_POINT('Ctrl Pts',(-1.72737084986519,6.6,3.01064330674259));
#11950=CARTESIAN_POINT('Ctrl Pts',(-1.73505498274876,6.6,3.02668477919227));
#11951=CARTESIAN_POINT('Ctrl Pts',(-1.74252093472838,6.6,3.04284531382503));
#11952=CARTESIAN_POINT('Ctrl Pts',(-1.74801629841351,6.6,3.05474038298642));
#11953=CARTESIAN_POINT('Ctrl Pts',(-1.75339345226814,6.6,3.06669996022911));
#11954=CARTESIAN_POINT('Ctrl Pts',(-1.75865150299272,6.6,3.07872207225469));
#11955=CARTESIAN_POINT('Ctrl Pts',(-1.76360055617396,6.6,3.09003768613558));
#11956=CARTESIAN_POINT('Ctrl Pts',(-1.76844015488379,6.6,3.10139971532666));
#11957=CARTESIAN_POINT('Ctrl Pts',(-1.7731695901327,6.6,3.11280520805519));
#11958=CARTESIAN_POINT('Ctrl Pts',(-1.80041932407603,6.6,3.17852058969964));
#11959=CARTESIAN_POINT('Ctrl Pts',(-1.82401955599936,6.6,3.24568623985345));
#11960=CARTESIAN_POINT('Ctrl Pts',(-1.84389319792571,6.6,3.31394437456818));
#11961=CARTESIAN_POINT('Ctrl Pts',(-1.86154775130874,6.6,3.37458081390891));
#11962=CARTESIAN_POINT('Ctrl Pts',(-1.87626122909509,6.6,3.43608043801735));
#11963=CARTESIAN_POINT('Ctrl Pts',(-1.88795171174053,6.6,3.49821270276066));
#11964=CARTESIAN_POINT('Ctrl Pts',(-1.89137817487387,6.6,3.51642357745171));
#11965=CARTESIAN_POINT('Ctrl Pts',(-1.89454475421827,6.6,3.53468889469712));
#11966=CARTESIAN_POINT('Ctrl Pts',(-1.89744890219664,6.6,3.55300305372269));
#11967=CARTESIAN_POINT('Ctrl Pts',(-1.89980101601846,6.6,3.56783597095006));
#11968=CARTESIAN_POINT('Ctrl Pts',(-1.90197972571919,6.6,3.58269332806818));
#11969=CARTESIAN_POINT('Ctrl Pts',(-1.90398341147039,6.6,3.597565901918));
#11970=CARTESIAN_POINT('Ctrl Pts',(-1.91367106629463,6.6,3.6694735659412));
#11971=CARTESIAN_POINT('Ctrl Pts',(-1.91927795233211,6.6,3.74177918256837));
#11972=CARTESIAN_POINT('Ctrl Pts',(-1.920702872003,6.6,3.81413426671844));
#11973=CARTESIAN_POINT('Ctrl Pts',(-1.92211579885034,6.6,3.88588037495561));
#11974=CARTESIAN_POINT('Ctrl Pts',(-1.91941728760775,6.6,3.95767611430931));
#11975=CARTESIAN_POINT('Ctrl Pts',(-1.91246071929416,6.6,4.02919789216754));
#11976=CARTESIAN_POINT('Ctrl Pts',(-1.91122396329351,6.6,4.04191321155429));
#11977=CARTESIAN_POINT('Ctrl Pts',(-1.90985249159563,6.6,4.05461989137107));
#11978=CARTESIAN_POINT('Ctrl Pts',(-1.90834530359594,6.6,4.06731613031539));
#11979=CARTESIAN_POINT('Ctrl Pts',(-0.863580915426621,2.5,5.40376507534353));
#11980=CARTESIAN_POINT('Ctrl Pts',(-0.903481800679317,2.5,5.37926660921982));
#11981=CARTESIAN_POINT('Ctrl Pts',(-0.942351921741605,2.5,5.35328747129858));
#11982=CARTESIAN_POINT('Ctrl Pts',(-0.98009997800088,2.5,5.32582783981609));
#11983=CARTESIAN_POINT('Ctrl Pts',(-1.03746171315656,2.5,5.28410033740505));
#11984=CARTESIAN_POINT('Ctrl Pts',(-1.09223449276709,2.5,5.23895557017225));
#11985=CARTESIAN_POINT('Ctrl Pts',(-1.14428247580057,2.5,5.19073503960552));
#11986=CARTESIAN_POINT('Ctrl Pts',(-1.19702062674331,2.5,5.14187509400626));
#11987=CARTESIAN_POINT('Ctrl Pts',(-1.2469617357595,2.5,5.08985623930448));
#11988=CARTESIAN_POINT('Ctrl Pts',(-1.2939195274248,2.5,5.03500604649739));
#11989=CARTESIAN_POINT('Ctrl Pts',(-1.31490326590717,2.5,5.01049547943804));
#11990=CARTESIAN_POINT('Ctrl Pts',(-1.33529063452927,2.5,4.98541925943203));
#11991=CARTESIAN_POINT('Ctrl Pts',(-1.35506176433983,2.5,4.95980570446106));
#11992=CARTESIAN_POINT('Ctrl Pts',(-1.36763974825088,2.5,4.94351089048651));
#11993=CARTESIAN_POINT('Ctrl Pts',(-1.37996828403753,2.5,4.92699859586587));
#11994=CARTESIAN_POINT('Ctrl Pts',(-1.39204180474552,2.5,4.91027607043345));
#11995=CARTESIAN_POINT('Ctrl Pts',(-1.39932292816931,2.5,4.90019129279686));
#11996=CARTESIAN_POINT('Ctrl Pts',(-1.40651184411551,2.5,4.89002911341411));
#11997=CARTESIAN_POINT('Ctrl Pts',(-1.41359773398804,2.5,4.87980534670441));
#11998=CARTESIAN_POINT('Ctrl Pts',(-1.45372898056346,2.5,4.82190259770073));
#11999=CARTESIAN_POINT('Ctrl Pts',(-1.49063491985867,2.5,4.76192357985326));
#12000=CARTESIAN_POINT('Ctrl Pts',(-1.52417445455585,2.5,4.70019324906169));
#12001=CARTESIAN_POINT('Ctrl Pts',(-1.55724799448755,2.5,4.63932059298981));
#12002=CARTESIAN_POINT('Ctrl Pts',(-1.58704824364224,2.5,4.57674389643576));
#12003=CARTESIAN_POINT('Ctrl Pts',(-1.61339223678792,2.5,4.51276105665826));
#12004=CARTESIAN_POINT('Ctrl Pts',(-1.6391925849168,2.5,4.45009859195879));
#12005=CARTESIAN_POINT('Ctrl Pts',(-1.66167798028648,2.5,4.38608652284999));
#12006=CARTESIAN_POINT('Ctrl Pts',(-1.68062808015966,2.5,4.32100573109058));
#12007=CARTESIAN_POINT('Ctrl Pts',(-1.68520397395377,2.5,4.30529062704781));
#12008=CARTESIAN_POINT('Ctrl Pts',(-1.6895735006115,2.5,4.28951324694272));
#12009=CARTESIAN_POINT('Ctrl Pts',(-1.69373310940874,2.5,4.27367764319859));
#12010=CARTESIAN_POINT('Ctrl Pts',(-1.69762827691426,2.5,4.25884876573892));
#12011=CARTESIAN_POINT('Ctrl Pts',(-1.70134027319327,2.5,4.24396443862568));
#12012=CARTESIAN_POINT('Ctrl Pts',(-1.70485982263115,2.5,4.22905603380731));
#12013=CARTESIAN_POINT('Ctrl Pts',(-1.72026850374742,2.5,4.16378664070643));
#12014=CARTESIAN_POINT('Ctrl Pts',(-1.73201964293625,2.5,4.09796147517623));
#12015=CARTESIAN_POINT('Ctrl Pts',(-1.73995104778309,2.5,4.03185909019967));
#12016=CARTESIAN_POINT('Ctrl Pts',(-1.74764478811313,2.5,3.9677374629435));
#12017=CARTESIAN_POINT('Ctrl Pts',(-1.751744263924,2.5,3.9033541748481));
#12018=CARTESIAN_POINT('Ctrl Pts',(-1.75205333162731,2.5,3.83896894622793));
#12019=CARTESIAN_POINT('Ctrl Pts',(-1.7522329238389,2.5,3.80155615453879));
#12020=CARTESIAN_POINT('Ctrl Pts',(-1.75113178109468,2.5,3.76414287275013));
#12021=CARTESIAN_POINT('Ctrl Pts',(-1.74870362584431,2.5,3.72678250885966));
#12022=CARTESIAN_POINT('Ctrl Pts',(-1.74647840079727,2.5,3.69254449319611));
#12023=CARTESIAN_POINT('Ctrl Pts',(-1.74313852381005,2.5,3.65835091190104));
#12024=CARTESIAN_POINT('Ctrl Pts',(-1.73870317030217,2.5,3.62424537115788));
#12025=CARTESIAN_POINT('Ctrl Pts',(-1.73685252518326,2.5,3.61001488143665));
#12026=CARTESIAN_POINT('Ctrl Pts',(-1.73481112807366,2.5,3.59579974532177));
#12027=CARTESIAN_POINT('Ctrl Pts',(-1.73258023476447,2.5,3.5816032511338));
#12028=CARTESIAN_POINT('Ctrl Pts',(-1.73102147713403,2.5,3.57168395398501));
#12029=CARTESIAN_POINT('Ctrl Pts',(-1.72937055372535,2.5,3.56177631077978));
#12030=CARTESIAN_POINT('Ctrl Pts',(-1.72762964037198,2.5,3.55188979170823));
#12031=CARTESIAN_POINT('Ctrl Pts',(-1.71638514771449,2.5,3.48803314376386));
#12032=CARTESIAN_POINT('Ctrl Pts',(-1.70137472204148,2.5,3.42495366737195));
#12033=CARTESIAN_POINT('Ctrl Pts',(-1.68279990506686,2.5,3.36291988638466));
#12034=CARTESIAN_POINT('Ctrl Pts',(-1.6640678406117,2.5,3.30036095051798));
#12035=CARTESIAN_POINT('Ctrl Pts',(-1.64171010531439,2.5,3.23886455924878));
#12036=CARTESIAN_POINT('Ctrl Pts',(-1.61588779042438,2.5,3.17873192052349));
#12037=CARTESIAN_POINT('Ctrl Pts',(-1.59790265814149,2.5,3.13684979389774));
#12038=CARTESIAN_POINT('Ctrl Pts',(-1.57823587689003,2.5,3.09562976391068));
#12039=CARTESIAN_POINT('Ctrl Pts',(-1.55693161087442,2.5,3.05518450517549));
#12040=CARTESIAN_POINT('Ctrl Pts',(-1.54404063803802,2.5,3.03071153195339));
#12041=CARTESIAN_POINT('Ctrl Pts',(-1.53054997830694,2.5,3.00652241595214));
#12042=CARTESIAN_POINT('Ctrl Pts',(-1.51646823518921,2.5,2.98264409713377));
#12043=CARTESIAN_POINT('Ctrl Pts',(-1.50751920801676,2.5,2.9674692908508));
#12044=CARTESIAN_POINT('Ctrl Pts',(-1.49832995810422,2.5,2.95241815434546));
#12045=CARTESIAN_POINT('Ctrl Pts',(-1.48892012002058,2.5,2.93752436847607));
#12046=CARTESIAN_POINT('Ctrl Pts',(-1.45509045248929,2.5,2.88397915125075));
#12047=CARTESIAN_POINT('Ctrl Pts',(-1.41836558695713,2.5,2.83238306268947));
#12048=CARTESIAN_POINT('Ctrl Pts',(-1.37888773636291,2.5,2.78302628084676));
#12049=CARTESIAN_POINT('Ctrl Pts',(-1.34707041524265,2.5,2.74324699819296));
#12050=CARTESIAN_POINT('Ctrl Pts',(-1.31346403250493,2.5,2.70492277456948));
#12051=CARTESIAN_POINT('Ctrl Pts',(-1.2781304993022,2.5,2.6682268367928));
#12052=CARTESIAN_POINT('Ctrl Pts',(-1.26549763847924,2.5,2.65510687304502));
#12053=CARTESIAN_POINT('Ctrl Pts',(-1.25264391285156,2.5,2.64219524938621));
#12054=CARTESIAN_POINT('Ctrl Pts',(-1.23957189875077,2.5,2.62950057751442));
#12055=CARTESIAN_POINT('Ctrl Pts',(-1.23011804990801,2.5,2.6203196274283));
#12056=CARTESIAN_POINT('Ctrl Pts',(-1.22055629637473,2.5,2.61125828180734));
#12057=CARTESIAN_POINT('Ctrl Pts',(-1.21089009783154,2.5,2.60232128125257));
#12058=CARTESIAN_POINT('Ctrl Pts',(-1.16593824479678,2.5,2.56076050286437));
#12059=CARTESIAN_POINT('Ctrl Pts',(-1.11871429572448,2.5,2.52187040319554));
#12060=CARTESIAN_POINT('Ctrl Pts',(-1.06933638089194,2.5,2.48594621693763));
#12061=CARTESIAN_POINT('Ctrl Pts',(-1.01995846605941,2.5,2.45002203067972));
#12062=CARTESIAN_POINT('Ctrl Pts',(-0.968425945006883,2.5,2.417063104816));
#12063=CARTESIAN_POINT('Ctrl Pts',(-0.914840821515225,2.5,2.38741840352973));
#12064=CARTESIAN_POINT('Ctrl Pts',(-0.911106104638903,2.5,2.38535225981347));
#12065=CARTESIAN_POINT('Ctrl Pts',(-0.907361412730045,2.5,2.38330223944491));
#12066=CARTESIAN_POINT('Ctrl Pts',(-0.903606778650209,2.5,2.38126847156104));
#12067=CARTESIAN_POINT('Origin',(-1.46549439250521E-15,6.6,3.64739446828387));
#12068=CARTESIAN_POINT('',(1.15470053837925,6.6,3.64739446828387));
#12069=CARTESIAN_POINT('',(0.577350269189624,6.6,4.64739446828387));
#12070=CARTESIAN_POINT('',(1.01036297108184,6.6,3.89739446828387));
#12071=CARTESIAN_POINT('',(-0.577350269189628,6.6,4.64739446828387));
#12072=CARTESIAN_POINT('',(0.288675134594811,6.6,4.64739446828387));
#12073=CARTESIAN_POINT('',(-1.15470053837925,6.6,3.64739446828387));
#12074=CARTESIAN_POINT('',(-0.721687836487034,6.6,4.39739446828387));
#12075=CARTESIAN_POINT('',(-0.577350269189627,6.6,2.64739446828387));
#12076=CARTESIAN_POINT('',(-1.01036297108185,6.6,3.39739446828387));
#12077=CARTESIAN_POINT('',(0.577350269189625,6.6,2.64739446828387));
#12078=CARTESIAN_POINT('',(-0.288675134594814,6.6,2.64739446828387));
#12079=CARTESIAN_POINT('',(0.721687836487031,6.6,2.89739446828387));
#12080=CARTESIAN_POINT('Origin',(1.15470053837925,6.6,3.64739446828387));
#12081=CARTESIAN_POINT('',(1.15470053837925,6.1,3.64739446828387));
#12082=CARTESIAN_POINT('',(1.15470053837925,6.6,3.64739446828387));
#12083=CARTESIAN_POINT('',(0.577350269189624,6.1,4.64739446828387));
#12084=CARTESIAN_POINT('',(0.577350269189624,6.1,4.64739446828387));
#12085=CARTESIAN_POINT('',(0.577350269189624,6.6,4.64739446828387));
#12086=CARTESIAN_POINT('Origin',(0.577350269189625,6.6,2.64739446828387));
#12087=CARTESIAN_POINT('',(0.577350269189625,6.1,2.64739446828387));
#12088=CARTESIAN_POINT('',(0.577350269189625,6.6,2.64739446828387));
#12089=CARTESIAN_POINT('',(1.15470053837925,6.1,3.64739446828387));
#12090=CARTESIAN_POINT('Origin',(-0.577350269189627,6.6,2.64739446828387));
#12091=CARTESIAN_POINT('',(-0.577350269189626,6.1,2.64739446828387));
#12092=CARTESIAN_POINT('',(-0.577350269189627,6.6,2.64739446828387));
#12093=CARTESIAN_POINT('',(0.577350269189625,6.1,2.64739446828387));
#12094=CARTESIAN_POINT('Origin',(-1.15470053837925,6.6,3.64739446828387));
#12095=CARTESIAN_POINT('',(-1.15470053837925,6.1,3.64739446828387));
#12096=CARTESIAN_POINT('',(-1.15470053837925,6.6,3.64739446828387));
#12097=CARTESIAN_POINT('',(-0.577350269189626,6.1,2.64739446828387));
#12098=CARTESIAN_POINT('Origin',(-0.577350269189628,6.6,4.64739446828387));
#12099=CARTESIAN_POINT('',(-0.577350269189628,6.1,4.64739446828387));
#12100=CARTESIAN_POINT('',(-0.577350269189628,6.6,4.64739446828387));
#12101=CARTESIAN_POINT('',(-1.15470053837925,6.1,3.64739446828387));
#12102=CARTESIAN_POINT('Origin',(0.577350269189624,6.6,4.64739446828387));
#12103=CARTESIAN_POINT('',(-0.577350269189628,6.1,4.64739446828387));
#12104=CARTESIAN_POINT('Origin',(-1.35447209004269E-15,6.1,3.64739446828387));
#12105=CARTESIAN_POINT('Origin',(-5.55111512312578E-16,2.5,3.64739446828387));
#12112=UNCERTAINTY_MEASURE_WITH_UNIT(LENGTH_MEASURE(0.01),#12119,
'DISTANCE_ACCURACY_VALUE',
'Maximum model space distance between geometric entities at asserted c
onnectivities');
#12113=UNCERTAINTY_MEASURE_WITH_UNIT(LENGTH_MEASURE(0.01),#12119,
'DISTANCE_ACCURACY_VALUE',
'Maximum model space distance between geometric entities at asserted c
onnectivities');
#12117=(
GEOMETRIC_REPRESENTATION_CONTEXT(3)
GLOBAL_UNCERTAINTY_ASSIGNED_CONTEXT((#12112))
GLOBAL_UNIT_ASSIGNED_CONTEXT((#12119,#12121,#12122))
REPRESENTATION_CONTEXT('','3D')
);
#12118=(
GEOMETRIC_REPRESENTATION_CONTEXT(3)
GLOBAL_UNCERTAINTY_ASSIGNED_CONTEXT((#12113))
GLOBAL_UNIT_ASSIGNED_CONTEXT((#12119,#12121,#12122))
REPRESENTATION_CONTEXT('','3D')
);
#12119=(
LENGTH_UNIT()
NAMED_UNIT(*)
SI_UNIT(.MILLI.,.METRE.)
);
#12121=(
NAMED_UNIT(*)
PLANE_ANGLE_UNIT()
SI_UNIT($,.RADIAN.)
);
#12122=(
NAMED_UNIT(*)
SI_UNIT($,.STERADIAN.)
SOLID_ANGLE_UNIT()
);
#12126=SHAPE_DEFINITION_REPRESENTATION(#12130,#12137);
#12130=PRODUCT_DEFINITION_SHAPE('',$,#12142);
#12137=SHAPE_REPRESENTATION('',(#2695),#12117);
#12138=PRODUCT_DEFINITION_CONTEXT('part definition',#12152,'design');
#12142=PRODUCT_DEFINITION('Screw_02','Screw_02',#12146,#12138);
#12146=PRODUCT_DEFINITION_FORMATION('',$,#12157);
#12152=APPLICATION_CONTEXT(
'Core Data for Automotive Mechanical Design Process');
#12153=PRODUCT_CONTEXT('part definition',#12152,'mechanical');
#12157=PRODUCT('Screw_02','Screw_02',$,(#12153));
#12159=PRESENTATION_STYLE_ASSIGNMENT((#12161));
#12161=SURFACE_STYLE_USAGE(.BOTH.,#12163);
#12163=SURFACE_SIDE_STYLE('',(#12165));
#12165=SURFACE_STYLE_FILL_AREA(#12167);
#12167=FILL_AREA_STYLE('Opaque(160,160,160)',(#12169));
#12169=FILL_AREA_STYLE_COLOUR('Opaque(160,160,160)',#12171);
#12171=COLOUR_RGB('Opaque(160,160,160)', 0.09019608, 0.27058824, 0.51372549);
ENDSEC;
END-ISO-10303-21;
